ISO-10303-21;
HEADER;
FILE_DESCRIPTION (('STEP AP214'),
    '1' );
FILE_NAME ('fast gear_ISO - Spur gear 2M 40T 20PA 10FW ---S40A75H50L38.0N.step',
    '2026-09-30T12:41:04',
    ( '' ),
    ( '' ),
    'SwSTEP 2.0',
    'SolidWorks 2026',
    '' );
FILE_SCHEMA (( 'AUTOMOTIVE_DESIGN' ));
ENDSEC;

DATA;
#2=EDGE_CURVE ( 'NONE', #44254, #29847, #44238, .T. ) ;
#33=VECTOR ( 'NONE', #5683, 1000.000000000000000 ) ;
#37=DIRECTION ( 'NONE',  ( -0.000000000000000000, -0.9945218953682741780, 0.1045284632676447834 ) ) ;
#49=EDGE_LOOP ( 'NONE', ( #19145, #44753, #19555, #4360 ) ) ;
#81=CIRCLE ( 'NONE', #41433, 15.99999999999999822 ) ;
#84=ORIENTED_EDGE ( 'NONE', *, *, #45252, .T. ) ;
#86=DIRECTION ( 'NONE',  ( 0.000000000000000000, -0.9510565162951500895, -0.3090169943749581649 ) ) ;
#87=CARTESIAN_POINT ( 'NONE',  ( 10.00000000000000000, 40.68715046381928602, 10.41901085202092503 ) ) ;
#93=DIRECTION ( 'NONE',  ( 0.000000000000000000, -0.8660254037844427044, 0.4999999999999929501 ) ) ;
#96=LINE ( 'NONE', #11386, #41562 ) ;
#106=CARTESIAN_POINT ( 'NONE',  ( 5.000000000000000000, -21.40280677340398086, 36.13751322684410638 ) ) ;
#107=AXIS2_PLACEMENT_3D ( 'NONE', #4062, #37590, #7958 ) ;
#109=EDGE_CURVE ( 'NONE', #16565, #7964, #26553, .T. ) ;
#112=AXIS2_PLACEMENT_3D ( 'NONE', #19745, #19502, #42285 ) ;
#116=ORIENTED_EDGE ( 'NONE', *, *, #2991, .T. ) ;
#124=CARTESIAN_POINT ( 'NONE',  ( 0.000000000000000000, 0.000000000000000000, 0.000000000000000000 ) ) ;
#128=ORIENTED_EDGE ( 'NONE', *, *, #23966, .T. ) ;
#130=CYLINDRICAL_SURFACE ( 'NONE', #29804, 16.00000000000000000 ) ;
#134=ORIENTED_EDGE ( 'NONE', *, *, #17388, .T. ) ;
#141=CARTESIAN_POINT ( 'NONE',  ( 0.000000000000000000, -37.16516213103273714, -4.992566952385376844 ) ) ;
#162=EDGE_CURVE ( 'NONE', #27382, #12203, #17667, .T. ) ;
#176=CARTESIAN_POINT ( 'NONE',  ( 10.00000000000000000, -37.01155633439053361, -6.555932627142825986 ) ) ;
#179=VECTOR ( 'NONE', #33994, 1000.000000000000227 ) ;
#183=DIRECTION ( 'NONE',  ( -1.000000000000000000, 0.000000000000000000, -0.000000000000000000 ) ) ;
#184=DIRECTION ( 'NONE',  ( -1.000000000000000000, 0.000000000000000000, 0.000000000000000000 ) ) ;
#186=CARTESIAN_POINT ( 'NONE',  ( -3.000000000000000000, 22.07842321921481243, 8.187992925817422218 ) ) ;
#191=CARTESIAN_POINT ( 'NONE',  ( -3.000000000000000000, 8.688484142254221609, -21.88630264137359660 ) ) ;
#196=LINE ( 'NONE', #26891, #33016 ) ;
#206=ORIENTED_EDGE ( 'NONE', *, *, #20064, .T. ) ;
#218=DIRECTION ( 'NONE',  ( 1.000000000000000000, -0.000000000000000000, 0.000000000000000000 ) ) ;
#228=VECTOR ( 'NONE', #26678, 1000.000000000000000 ) ;
#237=ORIENTED_EDGE ( 'NONE', *, *, #11573, .F. ) ;
#238=ORIENTED_EDGE ( 'NONE', *, *, #33137, .T. ) ;
#239=VERTEX_POINT ( 'NONE', #25711 ) ;
#245=AXIS2_PLACEMENT_3D ( 'NONE', #38051, #45152, #27276 ) ;
#247=ORIENTED_EDGE ( 'NONE', *, *, #3753, .T. ) ;
#248=CARTESIAN_POINT ( 'NONE',  ( 0.000000000000000000, -17.80606268964563554, 33.00180498840040855 ) ) ;
#249=AXIS2_PLACEMENT_3D ( 'NONE', #38479, #7888, #30651 ) ;
#262=FACE_OUTER_BOUND ( 'NONE', #8926, .T. ) ;
#277=ADVANCED_FACE ( 'NONE', ( #13989 ), #2725, .T. ) ;
#279=CARTESIAN_POINT ( 'NONE',  ( 10.00000000000000000, -26.79245525562738095, 32.34446384429961796 ) ) ;
#293=VERTEX_POINT ( 'NONE', #36498 ) ;
#308=LINE ( 'NONE', #34316, #47986 ) ;
#310=AXIS2_PLACEMENT_3D ( 'NONE', #28216, #39492, #24550 ) ;
#315=EDGE_CURVE ( 'NONE', #36078, #25303, #48171, .T. ) ;
#320=CYLINDRICAL_SURFACE ( 'NONE', #47599, 37.49900000000000233 ) ;
#326=EDGE_LOOP ( 'NONE', ( #36542, #32345 ) ) ;
#335=CARTESIAN_POINT ( 'NONE',  ( 10.00000000000000000, 0.000000000000000000, 0.000000000000000000 ) ) ;
#340=DIRECTION ( 'NONE',  ( -1.000000000000000000, 0.000000000000000000, -0.000000000000000000 ) ) ;
#354=DIRECTION ( 'NONE',  ( -1.000000000000000000, 0.000000000000000000, 0.000000000000000000 ) ) ;
#358=CIRCLE ( 'NONE', #28492, 42.00000000000000000 ) ;
#360=ORIENTED_EDGE ( 'NONE', *, *, #10558, .T. ) ;
#367=ORIENTED_EDGE ( 'NONE', *, *, #45108, .T. ) ;
#376=EDGE_CURVE ( 'NONE', #24228, #15279, #8089, .T. ) ;
#377=DIRECTION ( 'NONE',  ( 0.000000000000000000, 0.000000000000000000, 1.000000000000000000 ) ) ;
#380=CARTESIAN_POINT ( 'NONE',  ( -10.00000000000000000, 0.000000000000000000, 0.000000000000000000 ) ) ;
#390=VERTEX_POINT ( 'NONE', #37472 ) ;
#394=ORIENTED_EDGE ( 'NONE', *, *, #24277, .T. ) ;
#395=EDGE_CURVE ( 'NONE', #25211, #20236, #36366, .T. ) ;
#399=CARTESIAN_POINT ( 'NONE',  ( 10.00000000000000000, 17.80606268964585226, -33.00180498840028775 ) ) ;
#406=CARTESIAN_POINT ( 'NONE',  ( 10.00000000000000000, 0.000000000000000000, 0.000000000000000000 ) ) ;
#407=CIRCLE ( 'NONE', #6661, 16.00000000000000000 ) ;
#419=DIRECTION ( 'NONE',  ( -1.000000000000000000, 0.000000000000000000, 0.000000000000000000 ) ) ;
#420=AXIS2_PLACEMENT_3D ( 'NONE', #44361, #25025, #2755 ) ;
#421=CARTESIAN_POINT ( 'NONE',  ( 0.000000000000000000, -37.01155633439053361, -6.555932627142825986 ) ) ;
#426=CYLINDRICAL_SURFACE ( 'NONE', #16685, 16.00000000000000000 ) ;
#427=ORIENTED_EDGE ( 'NONE', *, *, #28237, .T. ) ;
#430=EDGE_LOOP ( 'NONE', ( #22082, #37942, #14548, #45186 ) ) ;
#450=CYLINDRICAL_SURFACE ( 'NONE', #508, 42.00000000000000000 ) ;
#465=ORIENTED_EDGE ( 'NONE', *, *, #395, .F. ) ;
#468=ORIENTED_EDGE ( 'NONE', *, *, #40787, .T. ) ;
#470=DIRECTION ( 'NONE',  ( 1.000000000000000000, -0.000000000000000000, 0.000000000000000000 ) ) ;
#472=DIRECTION ( 'NONE',  ( 0.000000000000000000, 0.000000000000000000, 1.000000000000000000 ) ) ;
#477=ADVANCED_FACE ( 'NONE', ( #20544 ), #17119, .F. ) ;
#483=CARTESIAN_POINT ( 'NONE',  ( 10.00000000000000000, 37.58145647212453611, 0.6853352020791767529 ) ) ;
#484=CARTESIAN_POINT ( 'NONE',  ( 10.00000000000000000, 0.000000000000000000, 0.000000000000000000 ) ) ;
#490=AXIS2_PLACEMENT_3D ( 'NONE', #7122, #21805, #36731 ) ;
#491=CARTESIAN_POINT ( 'NONE',  ( 10.00000000000000000, -33.00180498840035170, -17.80606268964575278 ) ) ;
#497=EDGE_CURVE ( 'NONE', #19153, #6597, #35001, .T. ) ;
#508=AXIS2_PLACEMENT_3D ( 'NONE', #33725, #41100, #29346 ) ;
#510=ORIENTED_EDGE ( 'NONE', *, *, #9166, .F. ) ;
#525=DIRECTION ( 'NONE',  ( 0.000000000000000000, 0.4539904997395412534, 0.8910065241883706744 ) ) ;
#529=LINE ( 'NONE', #8818, #19135 ) ;
#536=CIRCLE ( 'NONE', #37253, 37.49900000000000944 ) ;
#543=FACE_OUTER_BOUND ( 'NONE', #33687, .T. ) ;
#545=CARTESIAN_POINT ( 'NONE',  ( -10.00000000000000000, 0.000000000000000000, 0.000000000000000000 ) ) ;
#546=ORIENTED_EDGE ( 'NONE', *, *, #47429, .F. ) ;
#559=ORIENTED_EDGE ( 'NONE', *, *, #10857, .F. ) ;
#562=EDGE_CURVE ( 'NONE', #29283, #1846, #39411, .T. ) ;
#563=CIRCLE ( 'NONE', #16197, 37.49900000000000233 ) ;
#565=ORIENTED_EDGE ( 'NONE', *, *, #8773, .T. ) ;
#575=DIRECTION ( 'NONE',  ( 0.000000000000000000, 0.000000000000000000, -1.000000000000000000 ) ) ;
#584=DIRECTION ( 'NONE',  ( -1.000000000000000000, 0.000000000000000000, -0.000000000000000000 ) ) ;
#587=DIRECTION ( 'NONE',  ( -1.000000000000000000, -0.000000000000000000, -0.000000000000000000 ) ) ;
#599=VECTOR ( 'NONE', #28662, 1000.000000000000000 ) ;
#608=ADVANCED_FACE ( 'NONE', ( #40130 ), #32540, .F. ) ;
#609=EDGE_LOOP ( 'NONE', ( #7379, #41637, #36281, #24453 ) ) ;
#612=CIRCLE ( 'NONE', #38144, 16.00000000000000355 ) ;
#614=DIRECTION ( 'NONE',  ( 0.000000000000000000, 0.000000000000000000, 1.000000000000000000 ) ) ;
#620=CARTESIAN_POINT ( 'NONE',  ( 10.00000000000000000, -10.41901085202050403, -40.68715046381940681 ) ) ;
#627=LINE ( 'NONE', #33665, #22788 ) ;
#629=EDGE_CURVE ( 'NONE', #239, #20013, #47344, .T. ) ;
#635=DIRECTION ( 'NONE',  ( 0.000000000000000000, -0.1045284632676578424, 0.9945218953682729568 ) ) ;
#651=AXIS2_PLACEMENT_3D ( 'NONE', #9967, #24891, #25367 ) ;
#668=ORIENTED_EDGE ( 'NONE', *, *, #4841, .F. ) ;
#678=VECTOR ( 'NONE', #24830, 1000.000000000000114 ) ;
#681=ORIENTED_EDGE ( 'NONE', *, *, #2964, .F. ) ;
#682=CARTESIAN_POINT ( 'NONE',  ( 10.00000000000000000, -21.53537804866103045, 30.80686688397002371 ) ) ;
#687=CARTESIAN_POINT ( 'NONE',  ( -3.000000000000000000, -0.9646360437375307573, 23.52805723605590060 ) ) ;
#692=LINE ( 'NONE', #22726, #7106 ) ;
#703=CARTESIAN_POINT ( 'NONE',  ( 0.000000000000000000, -35.38097989696520074, 12.42422080174625520 ) ) ;
#717=ORIENTED_EDGE ( 'NONE', *, *, #17572, .F. ) ;
#723=LINE ( 'NONE', #22755, #12067 ) ;
#731=AXIS2_PLACEMENT_3D ( 'NONE', #30251, #12141, #377 ) ;
#739=LINE ( 'NONE', #4192, #39255 ) ;
#740=ORIENTED_EDGE ( 'NONE', *, *, #7261, .F. ) ;
#742=ORIENTED_EDGE ( 'NONE', *, *, #33981, .F. ) ;
#752=ADVANCED_FACE ( 'NONE', ( #11712 ), #22720, .F. ) ;
#757=LINE ( 'NONE', #37729, #2312 ) ;
#770=EDGE_CURVE ( 'NONE', #31111, #40387, #22091, .T. ) ;
#774=CIRCLE ( 'NONE', #21067, 37.49900000000001654 ) ;
#776=CIRCLE ( 'NONE', #14873, 15.99999999999999822 ) ;
#778=CARTESIAN_POINT ( 'NONE',  ( -3.000000000000000000, -26.23277895567245821, -4.042438405570103477 ) ) ;
#786=AXIS2_PLACEMENT_3D ( 'NONE', #16949, #35064, #31906 ) ;
#788=EDGE_CURVE ( 'NONE', #34900, #7136, #30324, .T. ) ;
#789=ORIENTED_EDGE ( 'NONE', *, *, #23042, .T. ) ;
#797=LINE ( 'NONE', #12088, #13433 ) ;
#801=ORIENTED_EDGE ( 'NONE', *, *, #27801, .T. ) ;
#822=DIRECTION ( 'NONE',  ( 0.000000000000000000, 0.000000000000000000, 1.000000000000000000 ) ) ;
#824=CARTESIAN_POINT ( 'NONE',  ( 10.00000000000000000, 37.48860685352291000, -0.8828120875901940279 ) ) ;
#829=CARTESIAN_POINT ( 'NONE',  ( 10.00000000000000000, 0.000000000000000000, 37.49900000000000233 ) ) ;
#833=LINE ( 'NONE', #11630, #4915 ) ;
#835=ADVANCED_FACE ( 'NONE', ( #4609 ), #34448, .T. ) ;
#843=DIRECTION ( 'NONE',  ( -1.000000000000000000, -0.000000000000000000, -0.000000000000000000 ) ) ;
#844=VERTEX_POINT ( 'NONE', #44749 ) ;
#845=AXIS2_PLACEMENT_3D ( 'NONE', #12506, #45535, #19573 ) ;
#849=LINE ( 'NONE', #7234, #16375 ) ;
#850=DIRECTION ( 'NONE',  ( 0.000000000000000000, -0.5877852522924689183, -0.8090169943749504489 ) ) ;
#852=FACE_OUTER_BOUND ( 'NONE', #8625, .T. ) ;
#868=DIRECTION ( 'NONE',  ( -1.000000000000000000, -0.000000000000000000, -0.000000000000000000 ) ) ;
#871=DIRECTION ( 'NONE',  ( 0.000000000000000000, 0.6691306063588569053, 0.7431448254773954654 ) ) ;
#876=DIRECTION ( 'NONE',  ( 0.000000000000000000, 0.5877852522924744694, -0.8090169943749465631 ) ) ;
#885=ORIENTED_EDGE ( 'NONE', *, *, #47454, .F. ) ;
#889=AXIS2_PLACEMENT_3D ( 'NONE', #38696, #5883, #2196 ) ;
#891=CARTESIAN_POINT ( 'NONE',  ( -10.00000000000000000, 0.000000000000000000, 0.000000000000000000 ) ) ;
#894=VERTEX_POINT ( 'NONE', #39345 ) ;
#904=VECTOR ( 'NONE', #28225, 999.9999999999998863 ) ;
#907=CARTESIAN_POINT ( 'NONE',  ( 10.00000000000000000, 22.48208911017551515, -35.47612816024499693 ) ) ;
#909=DIRECTION ( 'NONE',  ( 0.000000000000000000, 0.000000000000000000, 1.000000000000000000 ) ) ;
#910=EDGE_LOOP ( 'NONE', ( #134, #29416, #27347, #29269 ) ) ;
#911=VERTEX_POINT ( 'NONE', #5832 ) ;
#920=ADVANCED_FACE ( 'NONE', ( #35680 ), #31058, .T. ) ;
#926=DIRECTION ( 'NONE',  ( 1.000000000000000000, -0.000000000000000000, 0.000000000000000000 ) ) ;
#928=CARTESIAN_POINT ( 'NONE',  ( -3.000000000000000000, 16.61724383029390140, -20.69703378468903665 ) ) ;
#932=CARTESIAN_POINT ( 'NONE',  ( 0.000000000000000000, -19.89357724624986901, -12.59942793731086041 ) ) ;
#937=DIRECTION ( 'NONE',  ( -1.000000000000000000, 0.000000000000000000, -0.000000000000000000 ) ) ;
#939=CARTESIAN_POINT ( 'NONE',  ( 0.000000000000000000, -0.6853352020787742971, -37.58145647212455032 ) ) ;
#940=VECTOR ( 'NONE', #6028, 1000.000000000000000 ) ;
#951=AXIS2_PLACEMENT_3D ( 'NONE', #23413, #47391, #6503 ) ;
#953=EDGE_CURVE ( 'NONE', #32836, #15279, #24665, .T. ) ;
#956=VERTEX_POINT ( 'NONE', #20256 ) ;
#957=EDGE_CURVE ( 'NONE', #21733, #22651, #38640, .T. ) ;
#960=VERTEX_POINT ( 'NONE', #42297 ) ;
#961=ORIENTED_EDGE ( 'NONE', *, *, #33534, .T. ) ;
#962=VERTEX_POINT ( 'NONE', #31539 ) ;
#965=EDGE_CURVE ( 'NONE', #5424, #6597, #20017, .T. ) ;
#970=CYLINDRICAL_SURFACE ( 'NONE', #19200, 16.00000000000000000 ) ;
#971=ORIENTED_EDGE ( 'NONE', *, *, #12058, .F. ) ;
#981=ORIENTED_EDGE ( 'NONE', *, *, #24577, .T. ) ;
#994=VERTEX_POINT ( 'NONE', #33207 ) ;
#999=CARTESIAN_POINT ( 'NONE',  ( 4.999999999999999112, -40.68715046381937128, 10.41901085202062660 ) ) ;
#1000=CYLINDRICAL_SURFACE ( 'NONE', #43127, 37.49900000000000233 ) ;
#1008=CARTESIAN_POINT ( 'NONE',  ( -3.000000000000000000, 26.50000000000000000, -1.500000000000001332 ) ) ;
#1009=VECTOR ( 'NONE', #15720, 1000.000000000000000 ) ;
#1011=EDGE_CURVE ( 'NONE', #47351, #17279, #48133, .T. ) ;
#1027=VERTEX_POINT ( 'NONE', #25126 ) ;
#1029=CARTESIAN_POINT ( 'NONE',  ( 0.000000000000000000, -16.65560815589439159, 38.55633173627004595 ) ) ;
#1030=CYLINDRICAL_SURFACE ( 'NONE', #44594, 16.00000000000000000 ) ;
#1035=EDGE_CURVE ( 'NONE', #37389, #41148, #14338, .T. ) ;
#1047=EDGE_CURVE ( 'NONE', #15687, #30366, #2369, .T. ) ;
#1049=LINE ( 'NONE', #11840, #21553 ) ;
#1051=EDGE_LOOP ( 'NONE', ( #8665, #8541, #35186, #7160 ) ) ;
#1063=VECTOR ( 'NONE', #13673, 1000.000000000000000 ) ;
#1069=EDGE_CURVE ( 'NONE', #1265, #28940, #39365, .T. ) ;
#1070=DIRECTION ( 'NONE',  ( 0.000000000000000000, 0.000000000000000000, 1.000000000000000000 ) ) ;
#1081=CIRCLE ( 'NONE', #30024, 42.00000000000000000 ) ;
#1108=EDGE_LOOP ( 'NONE', ( #42456, #30771, #37756, #30253 ) ) ;
#1111=ORIENTED_EDGE ( 'NONE', *, *, #6339, .T. ) ;
#1117=AXIS2_PLACEMENT_3D ( 'NONE', #40933, #34964, #15238 ) ;
#1119=CARTESIAN_POINT ( 'NONE',  ( 10.00000000000000000, -10.96151621346461447, -35.95386929396268272 ) ) ;
#1123=DIRECTION ( 'NONE',  ( -1.000000000000000000, 0.000000000000000000, 0.000000000000000000 ) ) ;
#1125=CARTESIAN_POINT ( 'NONE',  ( 0.000000000000000000, -3.925862922256468046, 41.81611651403860463 ) ) ;
#1128=CARTESIAN_POINT ( 'NONE',  ( 10.00000000000000000, 0.000000000000000000, 0.000000000000000000 ) ) ;
#1135=PLANE ( 'NONE',  #15388 ) ;
#1138=DIRECTION ( 'NONE',  ( -1.000000000000000000, -0.000000000000000000, 0.000000000000000000 ) ) ;
#1146=ORIENTED_EDGE ( 'NONE', *, *, #27077, .F. ) ;
#1149=ORIENTED_EDGE ( 'NONE', *, *, #47202, .T. ) ;
#1153=EDGE_CURVE ( 'NONE', #46024, #36078, #21357, .T. ) ;
#1166=DIRECTION ( 'NONE',  ( 0.000000000000000000, -0.1564344650402380854, 0.9876883405951365491 ) ) ;
#1169=CIRCLE ( 'NONE', #12893, 42.00000000000000000 ) ;
#1173=ORIENTED_EDGE ( 'NONE', *, *, #17166, .T. ) ;
#1180=DIRECTION ( 'NONE',  ( -1.000000000000000000, 0.000000000000000000, 0.000000000000000000 ) ) ;
#1197=EDGE_LOOP ( 'NONE', ( #31822, #10125, #45167, #10166 ) ) ;
#1211=VECTOR ( 'NONE', #20604, 1000.000000000000000 ) ;
#1224=EDGE_CURVE ( 'NONE', #4717, #6044, #41761, .T. ) ;
#1250=EDGE_LOOP ( 'NONE', ( #31034, #1486, #9936, #25997 ) ) ;
#1251=LINE ( 'NONE', #31604, #45966 ) ;
#1255=DIRECTION ( 'NONE',  ( -1.000000000000000000, -0.000000000000000000, -0.000000000000000000 ) ) ;
#1257=VECTOR ( 'NONE', #6911, 1000.000000000000000 ) ;
#1262=CARTESIAN_POINT ( 'NONE',  ( 10.00000000000000000, 0.000000000000000000, 0.000000000000000000 ) ) ;
#1265=VERTEX_POINT ( 'NONE', #6423 ) ;
#1270=CIRCLE ( 'NONE', #2826, 37.49900000000000233 ) ;
#1275=CARTESIAN_POINT ( 'NONE',  ( 0.000000000000000000, 20.85821328998756385, -10.92862929874494959 ) ) ;
#1276=ORIENTED_EDGE ( 'NONE', *, *, #12127, .F. ) ;
#1279=FACE_OUTER_BOUND ( 'NONE', #14037, .T. ) ;
#1297=LINE ( 'NONE', #39215, #33 ) ;
#1300=ORIENTED_EDGE ( 'NONE', *, *, #4039, .F. ) ;
#1302=AXIS2_PLACEMENT_3D ( 'NONE', #45858, #8870, #25484 ) ;
#1303=CARTESIAN_POINT ( 'NONE',  ( 0.000000000000000000, 3.925862922256160736, 41.81611651403863306 ) ) ;
#1315=CARTESIAN_POINT ( 'NONE',  ( 10.00000000000000000, -17.67226234102849958, 33.17418723428301774 ) ) ;
#1318=CARTESIAN_POINT ( 'NONE',  ( 0.000000000000000000, 0.000000000000000000, 0.000000000000000000 ) ) ;
#1328=DIRECTION ( 'NONE',  ( 0.000000000000000000, 0.3090169943749573878, -0.9510565162951503115 ) ) ;
#1330=VERTEX_POINT ( 'NONE', #16061 ) ;
#1333=CARTESIAN_POINT ( 'NONE',  ( 5.000000000000000000, 39.04073710021366139, -15.48615015657542138 ) ) ;
#1338=DIRECTION ( 'NONE',  ( -1.000000000000000000, -0.000000000000000000, 0.000000000000000000 ) ) ;
#1342=EDGE_LOOP ( 'NONE', ( #36126, #36973, #5943, #20745 ) ) ;
#1345=VERTEX_POINT ( 'NONE', #5286 ) ;
#1349=CIRCLE ( 'NONE', #20109, 37.49900000000000944 ) ;
#1353=ORIENTED_EDGE ( 'NONE', *, *, #38597, .F. ) ;
#1357=VERTEX_POINT ( 'NONE', #16298 ) ;
#1363=ORIENTED_EDGE ( 'NONE', *, *, #20315, .T. ) ;
#1364=CIRCLE ( 'NONE', #16222, 37.49900000000000233 ) ;
#1368=CARTESIAN_POINT ( 'NONE',  ( -3.000000000000000000, -26.23277895567251505, 4.042438405569750870 ) ) ;
#1377=DIRECTION ( 'NONE',  ( 0.000000000000000000, 0.000000000000000000, 1.000000000000000000 ) ) ;
#1383=FACE_OUTER_BOUND ( 'NONE', #39454, .T. ) ;
#1387=CARTESIAN_POINT ( 'NONE',  ( 5.000000000000000000, 22.48208911017500355, 35.47612816024530957 ) ) ;
#1395=VECTOR ( 'NONE', #46062, 1000.000000000000000 ) ;
#1412=VERTEX_POINT ( 'NONE', #15225 ) ;
#1425=DIRECTION ( 'NONE',  ( -0.000000000000000000, -0.9135454576426004225, -0.4067366430758009854 ) ) ;
#1426=ORIENTED_EDGE ( 'NONE', *, *, #26746, .F. ) ;
#1446=EDGE_CURVE ( 'NONE', #11961, #15589, #10350, .T. ) ;
#1447=CARTESIAN_POINT ( 'NONE',  ( 0.000000000000000000, -10.45096189432314837, -21.10159698893440350 ) ) ;
#1452=ORIENTED_EDGE ( 'NONE', *, *, #17838, .T. ) ;
#1455=EDGE_CURVE ( 'NONE', #34210, #38706, #2977, .T. ) ;
#1459=VERTEX_POINT ( 'NONE', #18397 ) ;
#1463=LINE ( 'NONE', #24697, #23786 ) ;
#1466=ORIENTED_EDGE ( 'NONE', *, *, #41177, .F. ) ;
#1468=VERTEX_POINT ( 'NONE', #36512 ) ;
#1486=ORIENTED_EDGE ( 'NONE', *, *, #41177, .T. ) ;
#1487=DIRECTION ( 'NONE',  ( -0.000000000000000000, 0.4067366430758000417, -0.9135454576426009776 ) ) ;
#1495=EDGE_CURVE ( 'NONE', #34977, #6185, #20515, .T. ) ;
#1500=CYLINDRICAL_SURFACE ( 'NONE', #28134, 16.00000000000000000 ) ;
#1505=EDGE_CURVE ( 'NONE', #15600, #25099, #3710, .T. ) ;
#1509=CARTESIAN_POINT ( 'NONE',  ( 10.00000000000000000, 0.000000000000000000, 0.000000000000000000 ) ) ;
#1511=FACE_OUTER_BOUND ( 'NONE', #21140, .T. ) ;
#1514=MECHANICAL_DESIGN_GEOMETRIC_PRESENTATION_REPRESENTATION('',(#11679),#32024);
#1521=VERTEX_POINT ( 'NONE', #10583 ) ;
#1522=ADVANCED_FACE ( 'NONE', ( #25494 ), #45076, .T. ) ;
#1529=ORIENTED_EDGE ( 'NONE', *, *, #38033, .F. ) ;
#1535=CARTESIAN_POINT ( 'NONE',  ( 0.000000000000000000, 0.000000000000000000, 0.000000000000000000 ) ) ;
#1540=LINE ( 'NONE', #9354, #44111 ) ;
#1552=DIRECTION ( 'NONE',  ( -1.000000000000000000, 0.000000000000000000, 0.000000000000000000 ) ) ;
#1557=DIRECTION ( 'NONE',  ( 0.000000000000000000, 0.000000000000000000, 1.000000000000000000 ) ) ;
#1558=EDGE_CURVE ( 'NONE', #26085, #27526, #13495, .T. ) ;
#1575=ORIENTED_EDGE ( 'NONE', *, *, #31688, .T. ) ;
#1581=ORIENTED_EDGE ( 'NONE', *, *, #48014, .T. ) ;
#1592=ORIENTED_EDGE ( 'NONE', *, *, #16957, .T. ) ;
#1593=CARTESIAN_POINT ( 'NONE',  ( 10.00000000000000000, -37.48860685352291711, 0.8828120875899322373 ) ) ;
#1595=DIRECTION ( 'NONE',  ( 0.000000000000000000, 0.000000000000000000, 1.000000000000000000 ) ) ;
#1599=EDGE_LOOP ( 'NONE', ( #11213, #20244, #8248, #7101 ) ) ;
#1602=CARTESIAN_POINT ( 'NONE',  ( -3.000000000000000000, 18.84667830672605859, -18.68964196561243796 ) ) ;
#1609=DIRECTION ( 'NONE',  ( 0.000000000000000000, 0.000000000000000000, 1.000000000000000000 ) ) ;
#1618=VERTEX_POINT ( 'NONE', #30392 ) ;
#1619=EDGE_CURVE ( 'NONE', #31548, #15804, #18193, .T. ) ;
#1630=CARTESIAN_POINT ( 'NONE',  ( 10.00000000000000000, 31.52238457039599595, 27.75498641678753842 ) ) ;
#1638=ORIENTED_EDGE ( 'NONE', *, *, #26386, .T. ) ;
#1640=ORIENTED_EDGE ( 'NONE', *, *, #44773, .T. ) ;
#1647=ORIENTED_EDGE ( 'NONE', *, *, #19926, .F. ) ;
#1655=CARTESIAN_POINT ( 'NONE',  ( 0.000000000000000000, -21.53537804866058991, -30.80686688397033635 ) ) ;
#1661=DIRECTION ( 'NONE',  ( 0.000000000000000000, 0.9945218953682744001, -0.1045284632676436454 ) ) ;
#1664=DIRECTION ( 'NONE',  ( -1.000000000000000000, -0.000000000000000000, 0.000000000000000000 ) ) ;
#1670=EDGE_CURVE ( 'NONE', #20033, #47513, #16189, .T. ) ;
#1671=ORIENTED_EDGE ( 'NONE', *, *, #29612, .F. ) ;
#1682=CARTESIAN_POINT ( 'NONE',  ( -3.000000000000000000, 14.60985201121729737, -18.46759930825687945 ) ) ;
#1690=FACE_OUTER_BOUND ( 'NONE', #21535, .T. ) ;
#1698=AXIS2_PLACEMENT_3D ( 'NONE', #26577, #30262, #37106 ) ;
#1701=ORIENTED_EDGE ( 'NONE', *, *, #25743, .F. ) ;
#1705=DIRECTION ( 'NONE',  ( 1.000000000000000000, -0.000000000000000000, -0.000000000000000000 ) ) ;
#1708=EDGE_CURVE ( 'NONE', #41727, #22790, #24953, .T. ) ;
#1710=ORIENTED_EDGE ( 'NONE', *, *, #26861, .T. ) ;
#1711=VERTEX_POINT ( 'NONE', #6368 ) ;
#1715=CARTESIAN_POINT ( 'NONE',  ( -3.000000000000000000, -4.261787119645322974, 26.19803753235774835 ) ) ;
#1720=ORIENTED_EDGE ( 'NONE', *, *, #16957, .F. ) ;
#1724=ORIENTED_EDGE ( 'NONE', *, *, #15522, .T. ) ;
#1743=CYLINDRICAL_SURFACE ( 'NONE', #46601, 42.00000000000000000 ) ;
#1757=VECTOR ( 'NONE', #32623, 1000.000000000000000 ) ;
#1761=AXIS2_PLACEMENT_3D ( 'NONE', #9295, #16890, #17120 ) ;
#1763=PLANE ( 'NONE',  #44849 ) ;
#1764=EDGE_CURVE ( 'NONE', #6185, #36907, #24011, .T. ) ;
#1774=ORIENTED_EDGE ( 'NONE', *, *, #47202, .F. ) ;
#1779=EDGE_CURVE ( 'NONE', #22321, #38425, #24729, .T. ) ;
#1795=CARTESIAN_POINT ( 'NONE',  ( -3.000000000000000000, 16.83928648764923253, 16.46020748918050458 ) ) ;
#1797=VECTOR ( 'NONE', #7586, 1000.000000000000000 ) ;
#1804=CARTESIAN_POINT ( 'NONE',  ( 0.000000000000000000, 23.50000000000000000, 1.499999999999997780 ) ) ;
#1806=VECTOR ( 'NONE', #9245, 1000.000000000000000 ) ;
#1815=CARTESIAN_POINT ( 'NONE',  ( 10.00000000000000000, -35.95386929396248377, -10.96151621346525751 ) ) ;
#1825=EDGE_CURVE ( 'NONE', #1345, #9341, #2672, .T. ) ;
#1827=EDGE_CURVE ( 'NONE', #41993, #44214, #21996, .T. ) ;
#1842=DIRECTION ( 'NONE',  ( 0.000000000000000000, -0.8090169943749403458, -0.5877852522924830181 ) ) ;
#1844=VECTOR ( 'NONE', #3542, 1000.000000000000000 ) ;
#1846=VERTEX_POINT ( 'NONE', #47474 ) ;
#1847=DIRECTION ( 'NONE',  ( 0.000000000000000000, -0.5877852522924802425, 0.8090169943749422332 ) ) ;
#1851=DIRECTION ( 'NONE',  ( 0.000000000000000000, 0.000000000000000000, 1.000000000000000000 ) ) ;
#1853=LINE ( 'NONE', #35851, #18307 ) ;
#1865=ORIENTED_EDGE ( 'NONE', *, *, #2991, .F. ) ;
#1866=EDGE_LOOP ( 'NONE', ( #30052, #32484, #35977, #12365 ) ) ;
#1868=FACE_OUTER_BOUND ( 'NONE', #28081, .T. ) ;
#1872=VECTOR ( 'NONE', #43652, 1000.000000000000000 ) ;
#1879=DIRECTION ( 'NONE',  ( 0.000000000000000000, -0.1045284632676578285, 0.9945218953682729568 ) ) ;
#1881=VECTOR ( 'NONE', #24375, 1000.000000000000227 ) ;
#1889=CIRCLE ( 'NONE', #13614, 21.00000000000000000 ) ;
#1899=ADVANCED_FACE ( 'NONE', ( #44762 ), #41113, .T. ) ;
#1900=EDGE_CURVE ( 'NONE', #39824, #2611, #6462, .T. ) ;
#1908=CIRCLE ( 'NONE', #26143, 16.00000000000000000 ) ;
#1910=VERTEX_POINT ( 'NONE', #29103 ) ;
#1912=CARTESIAN_POINT ( 'NONE',  ( 0.000000000000000000, 23.59884966291521380, 12.14883922797262805 ) ) ;
#1919=CARTESIAN_POINT ( 'NONE',  ( 10.00000000000000000, -21.40280677340398441, 36.13751322684410638 ) ) ;
#1922=EDGE_LOOP ( 'NONE', ( #3443, #46352, #1671, #43044 ) ) ;
#1927=CIRCLE ( 'NONE', #8159, 42.00000000000000000 ) ;
#1933=DIRECTION ( 'NONE',  ( 0.000000000000000000, 0.5877852522924684742, 0.8090169943749506709 ) ) ;
#1942=DIRECTION ( 'NONE',  ( -1.000000000000000000, -0.000000000000000000, 0.000000000000000000 ) ) ;
#1946=ORIENTED_EDGE ( 'NONE', *, *, #26607, .T. ) ;
#1948=VECTOR ( 'NONE', #470, 1000.000000000000000 ) ;
#1951=AXIS2_PLACEMENT_3D ( 'NONE', #27045, #8427, #23352 ) ;
#1961=VERTEX_POINT ( 'NONE', #932 ) ;
#1963=AXIS2_PLACEMENT_3D ( 'NONE', #22793, #1255, #19356 ) ;
#1972=CYLINDRICAL_SURFACE ( 'NONE', #889, 42.00000000000000000 ) ;
#1975=DIRECTION ( 'NONE',  ( -1.000000000000000000, -0.000000000000000000, 0.000000000000000000 ) ) ;
#1983=ORIENTED_EDGE ( 'NONE', *, *, #26393, .F. ) ;
#1984=ORIENTED_EDGE ( 'NONE', *, *, #25087, .T. ) ;
#1994=LINE ( 'NONE', #5413, #17703 ) ;
#2007=DIRECTION ( 'NONE',  ( -1.000000000000000000, 0.000000000000000000, 0.000000000000000000 ) ) ;
#2013=EDGE_CURVE ( 'NONE', #44271, #47351, #45253, .T. ) ;
#2020=DIRECTION ( 'NONE',  ( 1.000000000000000000, 0.000000000000000000, 0.000000000000000000 ) ) ;
#2030=DIRECTION ( 'NONE',  ( 0.000000000000000000, -0.8090169943749508930, 0.5877852522924683631 ) ) ;
#2036=CARTESIAN_POINT ( 'NONE',  ( 10.00000000000000000, 33.17418723428333749, -17.67226234102790272 ) ) ;
#2040=VECTOR ( 'NONE', #22629, 1000.000000000000000 ) ;
#2051=CARTESIAN_POINT ( 'NONE',  ( -3.000000000000000000, 18.84667830672579925, 18.68964196561269020 ) ) ;
#2054=DIRECTION ( 'NONE',  ( -1.000000000000000000, -0.000000000000000000, 0.000000000000000000 ) ) ;
#2060=CARTESIAN_POINT ( 'NONE',  ( 10.00000000000000000, 35.95386929396256903, -10.96151621346501237 ) ) ;
#2074=CIRCLE ( 'NONE', #28621, 42.00000000000000000 ) ;
#2075=EDGE_LOOP ( 'NONE', ( #48356, #46035, #47019, #47935 ) ) ;
#2079=DIRECTION ( 'NONE',  ( -1.000000000000000000, 0.000000000000000000, 0.000000000000000000 ) ) ;
#2084=ORIENTED_EDGE ( 'NONE', *, *, #957, .F. ) ;
#2089=ORIENTED_EDGE ( 'NONE', *, *, #6752, .F. ) ;
#2094=FACE_BOUND ( 'NONE', #47440, .T. ) ;
#2104=VERTEX_POINT ( 'NONE', #39619 ) ;
#2127=EDGE_CURVE ( 'NONE', #43486, #44937, #20266, .T. ) ;
#2152=DIRECTION ( 'NONE',  ( -1.000000000000000000, 0.000000000000000000, 0.000000000000000000 ) ) ;
#2157=DIRECTION ( 'NONE',  ( 0.000000000000000000, 0.4999999999999920064, 0.8660254037844432595 ) ) ;
#2159=EDGE_CURVE ( 'NONE', #12132, #38104, #28102, .T. ) ;
#2173=CARTESIAN_POINT ( 'NONE',  ( 0.000000000000000000, 18.84667830672579925, 18.68964196561269020 ) ) ;
#2175=DIRECTION ( 'NONE',  ( -1.000000000000000000, -0.000000000000000000, -0.000000000000000000 ) ) ;
#2178=AXIS2_PLACEMENT_3D ( 'NONE', #33411, #33880, #14811 ) ;
#2181=CARTESIAN_POINT ( 'NONE',  ( 10.00000000000000000, 0.000000000000000000, 0.000000000000000000 ) ) ;
#2186=CARTESIAN_POINT ( 'NONE',  ( 0.000000000000000000, -23.29833615347109443, 3.418703333116492438 ) ) ;
#2188=VERTEX_POINT ( 'NONE', #9487 ) ;
#2194=DIRECTION ( 'NONE',  ( -1.000000000000000000, -0.000000000000000000, -0.000000000000000000 ) ) ;
#2195=ORIENTED_EDGE ( 'NONE', *, *, #33335, .F. ) ;
#2196=DIRECTION ( 'NONE',  ( 0.000000000000000000, 0.000000000000000000, 1.000000000000000000 ) ) ;
#2205=DIRECTION ( 'NONE',  ( 0.000000000000000000, -0.8660254037844432595, 0.4999999999999919509 ) ) ;
#2210=FACE_OUTER_BOUND ( 'NONE', #6578, .T. ) ;
#2211=VERTEX_POINT ( 'NONE', #46473 ) ;
#2212=CARTESIAN_POINT ( 'NONE',  ( 10.00000000000000000, -25.88420570971381807, -27.13269053701123212 ) ) ;
#2215=EDGE_CURVE ( 'NONE', #10144, #29882, #21222, .T. ) ;
#2216=DIRECTION ( 'NONE',  ( -1.000000000000000000, 0.000000000000000000, -0.000000000000000000 ) ) ;
#2220=EDGE_CURVE ( 'NONE', #2211, #48416, #47889, .T. ) ;
#2221=VECTOR ( 'NONE', #35904, 1000.000000000000000 ) ;
#2228=FACE_OUTER_BOUND ( 'NONE', #42464, .T. ) ;
#2232=ORIENTED_EDGE ( 'NONE', *, *, #18522, .T. ) ;
#2234=ORIENTED_EDGE ( 'NONE', *, *, #5363, .F. ) ;
#2236=FACE_OUTER_BOUND ( 'NONE', #34205, .T. ) ;
#2240=DIRECTION ( 'NONE',  ( -1.000000000000000000, 0.000000000000000000, -0.000000000000000000 ) ) ;
#2243=CARTESIAN_POINT ( 'NONE',  ( 0.000000000000000000, -37.58145647212455032, 16.68533520207890319 ) ) ;
#2252=DIRECTION ( 'NONE',  ( 1.000000000000000000, -0.000000000000000000, -0.000000000000000000 ) ) ;
#2253=CARTESIAN_POINT ( 'NONE',  ( 10.00000000000000000, 0.000000000000000000, 0.000000000000000000 ) ) ;
#2256=ORIENTED_EDGE ( 'NONE', *, *, #33435, .T. ) ;
#2267=ADVANCED_FACE ( 'NONE', ( #6546 ), #14630, .F. ) ;
#2272=CARTESIAN_POINT ( 'NONE',  ( 0.000000000000000000, 21.53537804866126137, -30.80686688396986028 ) ) ;
#2273=CARTESIAN_POINT ( 'NONE',  ( 10.00000000000000000, -35.95386929396264009, 10.96151621346475658 ) ) ;
#2279=ADVANCED_FACE ( 'NONE', ( #14861 ), #28817, .T. ) ;
#2287=CIRCLE ( 'NONE', #14031, 16.00000000000000000 ) ;
#2291=AXIS2_PLACEMENT_3D ( 'NONE', #3760, #29701, #13640 ) ;
#2294=ORIENTED_EDGE ( 'NONE', *, *, #27474, .F. ) ;
#2302=LINE ( 'NONE', #9897, #9762 ) ;
#2303=EDGE_CURVE ( 'NONE', #42424, #20927, #48337, .T. ) ;
#2312=VECTOR ( 'NONE', #45083, 1000.000000000000000 ) ;
#2316=DIRECTION ( 'NONE',  ( 1.000000000000000000, 0.000000000000000000, 0.000000000000000000 ) ) ;
#2317=VECTOR ( 'NONE', #42886, 999.9999999999998863 ) ;
#2322=PLANE ( 'NONE',  #39410 ) ;
#2328=DIRECTION ( 'NONE',  ( 0.000000000000000000, 0.000000000000000000, -1.000000000000000000 ) ) ;
#2334=CARTESIAN_POINT ( 'NONE',  ( 10.00000000000000000, -0.8828120875898013420, -37.48860685352291711 ) ) ;
#2336=ORIENTED_EDGE ( 'NONE', *, *, #22217, .T. ) ;
#2345=VECTOR ( 'NONE', #11005, 1000.000000000000000 ) ;
#2346=AXIS2_PLACEMENT_3D ( 'NONE', #28253, #47349, #2530 ) ;
#2354=EDGE_LOOP ( 'NONE', ( #23080, #740, #45841, #45075 ) ) ;
#2369=LINE ( 'NONE', #29046, #9614 ) ;
#2382=CIRCLE ( 'NONE', #8631, 42.00000000000000000 ) ;
#2383=CARTESIAN_POINT ( 'NONE',  ( -3.000000000000000000, -3.948201729842348850, 23.21447184625293048 ) ) ;
#2392=LINE ( 'NONE', #17316, #41983 ) ;
#2394=CARTESIAN_POINT ( 'NONE',  ( -3.000000000000000000, 26.50000000000000000, -1.500000000000001332 ) ) ;
#2397=ORIENTED_EDGE ( 'NONE', *, *, #36484, .T. ) ;
#2405=EDGE_CURVE ( 'NONE', #20033, #27870, #28836, .T. ) ;
#2406=LINE ( 'NONE', #23985, #37436 ) ;
#2416=ADVANCED_FACE ( 'NONE', ( #41298 ), #4567, .T. ) ;
#2419=AXIS2_PLACEMENT_3D ( 'NONE', #11238, #15624, #19764 ) ;
#2422=EDGE_CURVE ( 'NONE', #18553, #25783, #42693, .T. ) ;
#2432=EDGE_LOOP ( 'NONE', ( #42071, #36793, #3083, #5232 ) ) ;
#2441=CARTESIAN_POINT ( 'NONE',  ( -10.00000000000000000, 0.000000000000000000, 0.000000000000000000 ) ) ;
#2447=CARTESIAN_POINT ( 'NONE',  ( 10.00000000000000000, 22.64427369931169309, 30.00120703465213623 ) ) ;
#2449=AXIS2_PLACEMENT_3D ( 'NONE', #22440, #23156, #15812 ) ;
#2459=ADVANCED_FACE ( 'NONE', ( #1383 ), #16309, .F. ) ;
#2460=DIRECTION ( 'NONE',  ( 0.000000000000000000, -0.4539904997395540764, 0.8910065241883642351 ) ) ;
#2461=AXIS2_PLACEMENT_3D ( 'NONE', #3445, #47737, #22306 ) ;
#2469=DIRECTION ( 'NONE',  ( 0.000000000000000000, 0.8090169943749426773, 0.5877852522924797984 ) ) ;
#2475=CARTESIAN_POINT ( 'NONE',  ( -3.000000000000000000, 9.615535125378775305, 24.73947219025917121 ) ) ;
#2476=AXIS2_PLACEMENT_3D ( 'NONE', #31661, #35304, #46580 ) ;
#2480=CARTESIAN_POINT ( 'NONE',  ( 0.000000000000000000, -19.89357724625003598, 12.59942793731059574 ) ) ;
#2484=DIRECTION ( 'NONE',  ( -1.000000000000000000, -0.000000000000000000, -0.000000000000000000 ) ) ;
#2485=AXIS2_PLACEMENT_3D ( 'NONE', #19707, #871, #42490 ) ;
#2511=CARTESIAN_POINT ( 'NONE',  ( 10.00000000000000000, 3.925862922256160736, 41.81611651403863306 ) ) ;
#2517=AXIS2_PLACEMENT_3D ( 'NONE', #12737, #12498, #39162 ) ;
#2528=ORIENTED_EDGE ( 'NONE', *, *, #37622, .T. ) ;
#2530=DIRECTION ( 'NONE',  ( 0.000000000000000000, 0.9510565162951544194, -0.3090169943749446757 ) ) ;
#2534=CARTESIAN_POINT ( 'NONE',  ( 10.00000000000000000, 0.8828120875905820508, -37.48860685352290290 ) ) ;
#2545=DIRECTION ( 'NONE',  ( -1.000000000000000000, 0.000000000000000000, -0.000000000000000000 ) ) ;
#2553=CARTESIAN_POINT ( 'NONE',  ( 10.00000000000000000, -0.8828120875903202602, 37.48860685352291000 ) ) ;
#2556=LINE ( 'NONE', #12874, #11941 ) ;
#2560=DIRECTION ( 'NONE',  ( -0.000000000000000000, 0.9781476007338042455, 0.2079116908177664758 ) ) ;
#2567=DIRECTION ( 'NONE',  ( 0.000000000000000000, 0.9135454576426063067, -0.4067366430757881068 ) ) ;
#2570=EDGE_CURVE ( 'NONE', #29511, #40610, #48160, .T. ) ;
#2571=CARTESIAN_POINT ( 'NONE',  ( -3.000000000000000000, 20.85821328998741109, 10.92862929874522315 ) ) ;
#2575=EDGE_CURVE ( 'NONE', #39350, #13463, #33307, .T. ) ;
#2580=AXIS2_PLACEMENT_3D ( 'NONE', #18650, #14996, #11331 ) ;
#2588=VECTOR ( 'NONE', #17187, 1000.000000000000000 ) ;
#2589=DIRECTION ( 'NONE',  ( -1.000000000000000000, 0.000000000000000000, 0.000000000000000000 ) ) ;
#2591=LINE ( 'NONE', #32234, #17552 ) ;
#2602=DIRECTION ( 'NONE',  ( 0.000000000000000000, 0.000000000000000000, 1.000000000000000000 ) ) ;
#2606=VECTOR ( 'NONE', #3164, 1000.000000000000000 ) ;
#2607=DIRECTION ( 'NONE',  ( 0.000000000000000000, 0.1564344650402242354, 0.9876883405951387696 ) ) ;
#2611=VERTEX_POINT ( 'NONE', #28995 ) ;
#2612=VECTOR ( 'NONE', #19901, 1000.000000000000000 ) ;
#2619=DIRECTION ( 'NONE',  ( 0.000000000000000000, 0.000000000000000000, 1.000000000000000000 ) ) ;
#2622=AXIS2_PLACEMENT_3D ( 'NONE', #18703, #29726, #25804 ) ;
#2636=EDGE_CURVE ( 'NONE', #38237, #4028, #32905, .T. ) ;
#2639=ORIENTED_EDGE ( 'NONE', *, *, #39527, .F. ) ;
#2650=ORIENTED_EDGE ( 'NONE', *, *, #23966, .F. ) ;
#2657=FACE_OUTER_BOUND ( 'NONE', #430, .T. ) ;
#2672=LINE ( 'NONE', #10264, #36156 ) ;
#2687=AXIS2_PLACEMENT_3D ( 'NONE', #20900, #35823, #31443 ) ;
#2695=ORIENTED_EDGE ( 'NONE', *, *, #36836, .F. ) ;
#2696=ORIENTED_EDGE ( 'NONE', *, *, #38867, .T. ) ;
#2703=DIRECTION ( 'NONE',  ( 0.000000000000000000, -0.9135454576426059736, 0.4067366430757887730 ) ) ;
#2719=DIRECTION ( 'NONE',  ( 1.000000000000000000, 0.000000000000000000, 0.000000000000000000 ) ) ;
#2725=CYLINDRICAL_SURFACE ( 'NONE', #26202, 16.00000000000000000 ) ;
#2729=DIRECTION ( 'NONE',  ( 0.000000000000000000, 0.4539904997395479702, -0.8910065241883673437 ) ) ;
#2753=CIRCLE ( 'NONE', #23904, 15.99999999999999822 ) ;
#2754=CARTESIAN_POINT ( 'NONE',  ( 10.00000000000000000, -37.58145647212455032, 16.68533520207890319 ) ) ;
#2755=DIRECTION ( 'NONE',  ( 0.000000000000000000, -0.5877852522924802425, 0.8090169943749422332 ) ) ;
#2768=VERTEX_POINT ( 'NONE', #18700 ) ;
#2771=CARTESIAN_POINT ( 'NONE',  ( -3.000000000000000000, 9.615535125378775305, 24.73947219025917121 ) ) ;
#2783=DIRECTION ( 'NONE',  ( 0.000000000000000000, 0.000000000000000000, 1.000000000000000000 ) ) ;
#2786=CIRCLE ( 'NONE', #39536, 42.00000000000000000 ) ;
#2790=CARTESIAN_POINT ( 'NONE',  ( 10.00000000000000000, 0.000000000000000000, 0.000000000000000000 ) ) ;
#2792=VECTOR ( 'NONE', #8362, 1000.000000000000000 ) ;
#2804=FACE_OUTER_BOUND ( 'NONE', #1197, .T. ) ;
#2809=LINE ( 'NONE', #28992, #28577 ) ;
#2811=ORIENTED_EDGE ( 'NONE', *, *, #376, .T. ) ;
#2813=EDGE_CURVE ( 'NONE', #27530, #30209, #96, .T. ) ;
#2814=CIRCLE ( 'NONE', #19999, 16.00000000000000355 ) ;
#2816=DIRECTION ( 'NONE',  ( 1.000000000000000000, -0.000000000000000000, -0.000000000000000000 ) ) ;
#2819=DIRECTION ( 'NONE',  ( -1.000000000000000000, 0.000000000000000000, 0.000000000000000000 ) ) ;
#2821=CARTESIAN_POINT ( 'NONE',  ( 10.00000000000000000, 12.42422080174688404, -35.38097989696498047 ) ) ;
#2826=AXIS2_PLACEMENT_3D ( 'NONE', #6439, #14512, #29438 ) ;
#2827=EDGE_CURVE ( 'NONE', #1961, #41810, #27273, .T. ) ;
#2832=AXIS2_PLACEMENT_3D ( 'NONE', #19530, #11257, #26182 ) ;
#2838=AXIS2_PLACEMENT_3D ( 'NONE', #24658, #12927, #27865 ) ;
#2840=DIRECTION ( 'NONE',  ( 0.000000000000000000, 0.8090169943749447867, 0.5877852522924769119 ) ) ;
#2848=CARTESIAN_POINT ( 'NONE',  ( 10.00000000000000000, -40.98264845739755913, 9.188173127307164734 ) ) ;
#2852=EDGE_LOOP ( 'NONE', ( #39309, #23407, #28239, #34567 ) ) ;
#2853=AXIS2_PLACEMENT_3D ( 'NONE', #19303, #34713, #5118 ) ;
#2856=ORIENTED_EDGE ( 'NONE', *, *, #3753, .F. ) ;
#2860=DIRECTION ( 'NONE',  ( 1.000000000000000000, 0.000000000000000000, -0.000000000000000000 ) ) ;
#2866=DIRECTION ( 'NONE',  ( 0.000000000000000000, -0.4067366430757887730, -0.9135454576426059736 ) ) ;
#2874=EDGE_CURVE ( 'NONE', #35343, #1265, #18099, .T. ) ;
#2894=ORIENTED_EDGE ( 'NONE', *, *, #22285, .F. ) ;
#2906=CARTESIAN_POINT ( 'NONE',  ( -10.00000000000000000, 0.000000000000000000, 0.000000000000000000 ) ) ;
#2907=EDGE_LOOP ( 'NONE', ( #43189, #29272, #16232, #46805 ) ) ;
#2921=ORIENTED_EDGE ( 'NONE', *, *, #34868, .T. ) ;
#2922=DIRECTION ( 'NONE',  ( 0.000000000000000000, 0.000000000000000000, 1.000000000000000000 ) ) ;
#2928=CARTESIAN_POINT ( 'NONE',  ( 10.00000000000000000, -25.88420570971419821, 27.13269053701087330 ) ) ;
#2931=MANIFOLD_SOLID_BREP ( 'CirPattern1', #42702 ) ;
#2938=CYLINDRICAL_SURFACE ( 'NONE', #26975, 16.00000000000000000 ) ;
#2940=ORIENTED_EDGE ( 'NONE', *, *, #33243, .T. ) ;
#2948=LINE ( 'NONE', #29622, #39084 ) ;
#2955=LINE ( 'NONE', #47038, #10214 ) ;
#2959=ORIENTED_EDGE ( 'NONE', *, *, #11459, .T. ) ;
#2961=CARTESIAN_POINT ( 'NONE',  ( 0.000000000000000000, 0.6853352020795618893, -37.58145647212453611 ) ) ;
#2964=EDGE_CURVE ( 'NONE', #35055, #239, #2753, .T. ) ;
#2966=LINE ( 'NONE', #6178, #33174 ) ;
#2967=CARTESIAN_POINT ( 'NONE',  ( 10.00000000000000000, 37.58145647212453611, 0.6853352020791767529 ) ) ;
#2969=DIRECTION ( 'NONE',  ( 0.000000000000000000, -1.000000000000000000, -1.047444401652940007E-14 ) ) ;
#2970=EDGE_LOOP ( 'NONE', ( #24185, #4959, #11162, #29695 ) ) ;
#2973=DIRECTION ( 'NONE',  ( -1.000000000000000000, 0.000000000000000000, 0.000000000000000000 ) ) ;
#2975=ORIENTED_EDGE ( 'NONE', *, *, #33524, .T. ) ;
#2977=LINE ( 'NONE', #40668, #21307 ) ;
#2982=LINE ( 'NONE', #39966, #35994 ) ;
#2991=EDGE_CURVE ( 'NONE', #1412, #35361, #21518, .T. ) ;
#2992=DIRECTION ( 'NONE',  ( 0.000000000000000000, 0.3090169943749412340, 0.9510565162951556406 ) ) ;
#3013=ORIENTED_EDGE ( 'NONE', *, *, #22436, .T. ) ;
#3025=EDGE_CURVE ( 'NONE', #6278, #8792, #6915, .T. ) ;
#3027=DIRECTION ( 'NONE',  ( 1.000000000000000000, 0.000000000000000000, -0.000000000000000000 ) ) ;
#3035=EDGE_CURVE ( 'NONE', #14490, #47828, #10597, .T. ) ;
#3037=CARTESIAN_POINT ( 'NONE',  ( 10.00000000000000000, -40.68715046381921496, -10.41901085202121457 ) ) ;
#3038=DIRECTION ( 'NONE',  ( 0.000000000000000000, 0.000000000000000000, 1.000000000000000000 ) ) ;
#3044=DIRECTION ( 'NONE',  ( 0.000000000000000000, 0.000000000000000000, 1.000000000000000000 ) ) ;
#3049=AXIS2_PLACEMENT_3D ( 'NONE', #34196, #38122, #45452 ) ;
#3072=ORIENTED_EDGE ( 'NONE', *, *, #1558, .T. ) ;
#3074=ORIENTED_EDGE ( 'NONE', *, *, #1825, .T. ) ;
#3081=DIRECTION ( 'NONE',  ( -1.000000000000000000, 0.000000000000000000, 0.000000000000000000 ) ) ;
#3083=ORIENTED_EDGE ( 'NONE', *, *, #35874, .F. ) ;
#3084=AXIS2_PLACEMENT_3D ( 'NONE', #38500, #45349, #34824 ) ;
#3095=DIRECTION ( 'NONE',  ( 0.000000000000000000, 0.000000000000000000, 1.000000000000000000 ) ) ;
#3112=( NAMED_UNIT ( * ) SI_UNIT ( $, .STERADIAN. ) SOLID_ANGLE_UNIT ( ) );
#3113=CARTESIAN_POINT ( 'NONE',  ( 0.000000000000000000, 21.32104025579158701, -30.84782396557194772 ) ) ;
#3119=ADVANCED_FACE ( 'NONE', ( #26248 ), #11071, .F. ) ;
#3120=LINE ( 'NONE', #32281, #46045 ) ;
#3129=VECTOR ( 'NONE', #34152, 1000.000000000000000 ) ;
#3131=AXIS2_PLACEMENT_3D ( 'NONE', #24523, #28434, #24993 ) ;
#3134=VERTEX_POINT ( 'NONE', #26486 ) ;
#3141=DIRECTION ( 'NONE',  ( 0.000000000000000000, -0.000000000000000000, 1.000000000000000000 ) ) ;
#3144=VECTOR ( 'NONE', #39462, 1000.000000000000000 ) ;
#3154=VERTEX_POINT ( 'NONE', #29907 ) ;
#3155=EDGE_LOOP ( 'NONE', ( #31976, #33090, #13576, #3342 ) ) ;
#3164=DIRECTION ( 'NONE',  ( -1.000000000000000000, 0.000000000000000000, -0.000000000000000000 ) ) ;
#3166=LINE ( 'NONE', #33035, #20124 ) ;
#3169=EDGE_LOOP ( 'NONE', ( #29021, #30776, #30545, #35616 ) ) ;
#3171=EDGE_CURVE ( 'NONE', #17403, #911, #15209, .T. ) ;
#3172=VECTOR ( 'NONE', #38870, 1000.000000000000000 ) ;
#3177=EDGE_CURVE ( 'NONE', #8888, #40065, #43342, .T. ) ;
#3180=VERTEX_POINT ( 'NONE', #1447 ) ;
#3181=CIRCLE ( 'NONE', #34453, 42.00000000000000000 ) ;
#3183=APPLICATION_CONTEXT ( 'automotive_design' ) ;
#3186=DIRECTION ( 'NONE',  ( -1.000000000000000000, -0.000000000000000000, 0.000000000000000000 ) ) ;
#3192=CARTESIAN_POINT ( 'NONE',  ( 10.00000000000000000, 0.000000000000000000, 0.000000000000000000 ) ) ;
#3196=CARTESIAN_POINT ( 'NONE',  ( 10.00000000000000000, 33.17418723428307459, 17.67226234102837878 ) ) ;
#3197=FACE_OUTER_BOUND ( 'NONE', #22845, .T. ) ;
#3199=LINE ( 'NONE', #11300, #14336 ) ;
#3216=DIRECTION ( 'NONE',  ( -1.000000000000000000, -0.000000000000000000, 0.000000000000000000 ) ) ;
#3229=ORIENTED_EDGE ( 'NONE', *, *, #4162, .F. ) ;
#3239=EDGE_CURVE ( 'NONE', #15601, #16667, #29023, .T. ) ;
#3242=EDGE_CURVE ( 'NONE', #22090, #15687, #42569, .T. ) ;
#3245=AXIS2_PLACEMENT_3D ( 'NONE', #22206, #33934, #18533 ) ;
#3252=EDGE_CURVE ( 'NONE', #20905, #10988, #16860, .T. ) ;
#3253=ADVANCED_FACE ( 'NONE', ( #28108 ), #9496, .T. ) ;
#3254=DIRECTION ( 'NONE',  ( 0.000000000000000000, -0.9945218953682742891, 0.1045284632676436315 ) ) ;
#3270=VERTEX_POINT ( 'NONE', #35206 ) ;
#3272=FACE_OUTER_BOUND ( 'NONE', #33366, .T. ) ;
#3273=CARTESIAN_POINT ( 'NONE',  ( 0.000000000000000000, 35.95386929396241271, 10.96151621346552751 ) ) ;
#3279=CYLINDRICAL_SURFACE ( 'NONE', #41601, 16.00000000000000000 ) ;
#3282=DIRECTION ( 'NONE',  ( 0.000000000000000000, -0.9876883405951358830, -0.1564344650402420822 ) ) ;
#3304=EDGE_CURVE ( 'NONE', #18104, #15496, #22065, .T. ) ;
#3317=ORIENTED_EDGE ( 'NONE', *, *, #11839, .F. ) ;
#3336=LINE ( 'NONE', #18022, #26437 ) ;
#3337=LINE ( 'NONE', #36871, #30485 ) ;
#3342=ORIENTED_EDGE ( 'NONE', *, *, #39541, .T. ) ;
#3353=LINE ( 'NONE', #3852, #33138 ) ;
#3360=EDGE_CURVE ( 'NONE', #26085, #31548, #30236, .T. ) ;
#3367=CARTESIAN_POINT ( 'NONE',  ( -3.000000000000000000, 22.07842321921481243, 8.187992925817422218 ) ) ;
#3374=DIRECTION ( 'NONE',  ( 0.000000000000000000, 0.9876883405951372152, 0.1564344650402346160 ) ) ;
#3389=VECTOR ( 'NONE', #25566, 1000.000000000000000 ) ;
#3393=DIRECTION ( 'NONE',  ( -1.000000000000000000, -0.000000000000000000, 0.000000000000000000 ) ) ;
#3398=CARTESIAN_POINT ( 'NONE',  ( 10.00000000000000000, 41.91543099594818500, 2.663952781846293139 ) ) ;
#3420=ADVANCED_FACE ( 'NONE', ( #21485 ), #7027, .T. ) ;
#3421=CIRCLE ( 'NONE', #5007, 42.00000000000000000 ) ;
#3443=ORIENTED_EDGE ( 'NONE', *, *, #497, .T. ) ;
#3445=CARTESIAN_POINT ( 'NONE',  ( 0.000000000000000000, 12.26510123303259725, 35.53030884539089840 ) ) ;
#3446=ORIENTED_EDGE ( 'NONE', *, *, #17332, .F. ) ;
#3454=CIRCLE ( 'NONE', #21457, 42.00000000000000000 ) ;
#3457=ORIENTED_EDGE ( 'NONE', *, *, #18170, .F. ) ;
#3464=CIRCLE ( 'NONE', #1951, 16.00000000000000355 ) ;
#3479=CARTESIAN_POINT ( 'NONE',  ( 0.000000000000000000, 20.85821328998756385, -10.92862929874494959 ) ) ;
#3481=DIRECTION ( 'NONE',  ( 1.000000000000000000, 0.000000000000000000, -0.000000000000000000 ) ) ;
#3483=AXIS2_PLACEMENT_3D ( 'NONE', #39367, #6551, #5847 ) ;
#3486=DIRECTION ( 'NONE',  ( -1.000000000000000000, 0.000000000000000000, -0.000000000000000000 ) ) ;
#3493=ADVANCED_FACE ( 'NONE', ( #30288 ), #1135, .F. ) ;
#3505=VECTOR ( 'NONE', #28967, 1000.000000000000000 ) ;
#3509=ORIENTED_EDGE ( 'NONE', *, *, #2215, .T. ) ;
#3518=EDGE_CURVE ( 'NONE', #46278, #12381, #42027, .T. ) ;
#3521=ORIENTED_EDGE ( 'NONE', *, *, #21613, .T. ) ;
#3534=CARTESIAN_POINT ( 'NONE',  ( 0.000000000000000000, 12.26510123303308752, -35.53030884539072787 ) ) ;
#3537=DIRECTION ( 'NONE',  ( -1.000000000000000000, -0.000000000000000000, 0.000000000000000000 ) ) ;
#3542=DIRECTION ( 'NONE',  ( 1.000000000000000000, -0.000000000000000000, -0.000000000000000000 ) ) ;
#3551=CIRCLE ( 'NONE', #27824, 37.49900000000000233 ) ;
#3580=ORIENTED_EDGE ( 'NONE', *, *, #2827, .F. ) ;
#3594=ORIENTED_EDGE ( 'NONE', *, *, #15647, .F. ) ;
#3601=DIRECTION ( 'NONE',  ( 1.000000000000000000, 0.000000000000000000, 0.000000000000000000 ) ) ;
#3614=VERTEX_POINT ( 'NONE', #2334 ) ;
#3618=EDGE_LOOP ( 'NONE', ( #40947, #27259, #40984, #24700 ) ) ;
#3627=ORIENTED_EDGE ( 'NONE', *, *, #35868, .F. ) ;
#3628=VECTOR ( 'NONE', #38463, 1000.000000000000000 ) ;
#3632=CARTESIAN_POINT ( 'NONE',  ( 10.00000000000000000, 0.000000000000000000, 0.000000000000000000 ) ) ;
#3646=DIRECTION ( 'NONE',  ( -1.000000000000000000, -0.000000000000000000, -0.000000000000000000 ) ) ;
#3661=CARTESIAN_POINT ( 'NONE',  ( 0.000000000000000000, 30.84782396557248418, -21.32104025579081252 ) ) ;
#3666=DIRECTION ( 'NONE',  ( -1.000000000000000000, -0.000000000000000000, -0.000000000000000000 ) ) ;
#3667=DIRECTION ( 'NONE',  ( 1.000000000000000000, 0.000000000000000000, 0.000000000000000000 ) ) ;
#3673=PRODUCT_DEFINITION_CONTEXT ( 'detailed design', #5717, 'design' ) ;
#3675=LINE ( 'NONE', #18604, #18253 ) ;
#3676=LINE ( 'NONE', #7346, #40175 ) ;
#3682=ORIENTED_EDGE ( 'NONE', *, *, #44489, .T. ) ;
#3685=ORIENTED_EDGE ( 'NONE', *, *, #42156, .F. ) ;
#3689=VECTOR ( 'NONE', #20571, 1000.000000000000000 ) ;
#3693=CYLINDRICAL_SURFACE ( 'NONE', #8717, 16.00000000000000000 ) ;
#3710=LINE ( 'NONE', #40202, #11931 ) ;
#3717=CARTESIAN_POINT ( 'NONE',  ( 0.000000000000000000, 6.762365576493643893, -25.66652317338391853 ) ) ;
#3719=CIRCLE ( 'NONE', #31093, 16.00000000000000355 ) ;
#3738=LINE ( 'NONE', #18662, #9623 ) ;
#3744=ADVANCED_FACE ( 'NONE', ( #6978 ), #10406, .T. ) ;
#3745=CIRCLE ( 'NONE', #17818, 15.99999999999999645 ) ;
#3750=EDGE_LOOP ( 'NONE', ( #25235, #38923, #17432, #39153 ) ) ;
#3752=CARTESIAN_POINT ( 'NONE',  ( 10.00000000000000000, -35.53030884539094103, 12.26510123303246935 ) ) ;
#3753=EDGE_CURVE ( 'NONE', #42541, #956, #43481, .T. ) ;
#3756=EDGE_CURVE ( 'NONE', #30305, #25221, #19984, .T. ) ;
#3760=CARTESIAN_POINT ( 'NONE',  ( 10.00000000000000000, 37.22597642581150268, 5.202137450157037435 ) ) ;
#3772=CARTESIAN_POINT ( 'NONE',  ( -10.00000000000000000, 0.000000000000000000, 0.000000000000000000 ) ) ;
#3774=DIRECTION ( 'NONE',  ( 0.000000000000000000, 0.9876883405951372152, 0.1564344650402346160 ) ) ;
#3775=CARTESIAN_POINT ( 'NONE',  ( 10.00000000000000000, 37.22597642581158084, 10.79786254984347593 ) ) ;
#3780=CARTESIAN_POINT ( 'NONE',  ( 0.000000000000000000, -26.08949754953005495, -27.05870788708258701 ) ) ;
#3782=FACE_OUTER_BOUND ( 'NONE', #7092, .T. ) ;
#3784=EDGE_LOOP ( 'NONE', ( #45526, #13775, #39141, #11597 ) ) ;
#3788=DIRECTION ( 'NONE',  ( -1.000000000000000000, -0.000000000000000000, 0.000000000000000000 ) ) ;
#3790=VECTOR ( 'NONE', #48382, 999.9999999999998863 ) ;
#3811=CARTESIAN_POINT ( 'NONE',  ( 0.000000000000000000, 33.80338159004307386, -16.23288003029461279 ) ) ;
#3818=DIRECTION ( 'NONE',  ( -1.000000000000000000, 0.000000000000000000, 0.000000000000000000 ) ) ;
#3832=CARTESIAN_POINT ( 'NONE',  ( -3.000000000000000000, 20.85821328998756385, -10.92862929874494959 ) ) ;
#3837=CARTESIAN_POINT ( 'NONE',  ( -3.000000000000000000, 16.83928648764945279, -16.46020748918028076 ) ) ;
#3840=ORIENTED_EDGE ( 'NONE', *, *, #22653, .T. ) ;
#3844=ORIENTED_EDGE ( 'NONE', *, *, #12127, .T. ) ;
#3849=CARTESIAN_POINT ( 'NONE',  ( 10.00000000000000000, -10.96151621346461447, -35.95386929396268272 ) ) ;
#3851=DIRECTION ( 'NONE',  ( 1.000000000000000000, -0.000000000000000000, -0.000000000000000000 ) ) ;
#3852=CARTESIAN_POINT ( 'NONE',  ( -3.000000000000000000, 8.688484142253939169, 21.88630264137371029 ) ) ;
#3869=ORIENTED_EDGE ( 'NONE', *, *, #17877, .F. ) ;
#3870=EDGE_CURVE ( 'NONE', #27962, #26444, #39801, .T. ) ;
#3873=CARTESIAN_POINT ( 'NONE',  ( 10.00000000000000000, -35.95386929396264009, 10.96151621346475658 ) ) ;
#3880=DIRECTION ( 'NONE',  ( 0.000000000000000000, -0.2079116908177653100, 0.9781476007338044676 ) ) ;
#3889=ORIENTED_EDGE ( 'NONE', *, *, #2570, .T. ) ;
#3895=VECTOR ( 'NONE', #22639, 1000.000000000000000 ) ;
#3896=DIRECTION ( 'NONE',  ( 0.000000000000000000, 0.000000000000000000, 1.000000000000000000 ) ) ;
#3898=DIRECTION ( 'NONE',  ( 0.000000000000000000, 0.000000000000000000, -1.000000000000000000 ) ) ;
#3901=AXIS2_PLACEMENT_3D ( 'NONE', #33212, #14624, #29539 ) ;
#3905=LINE ( 'NONE', #33999, #37144 ) ;
#3908=DIRECTION ( 'NONE',  ( -1.000000000000000000, 0.000000000000000000, 0.000000000000000000 ) ) ;
#3925=DIRECTION ( 'NONE',  ( -1.000000000000000000, 0.000000000000000000, 0.000000000000000000 ) ) ;
#3933=AXIS2_PLACEMENT_3D ( 'NONE', #3273, #18204, #47818 ) ;
#3940=EDGE_LOOP ( 'NONE', ( #42106, #27417, #41222, #3943 ) ) ;
#3943=ORIENTED_EDGE ( 'NONE', *, *, #25757, .T. ) ;
#3944=ORIENTED_EDGE ( 'NONE', *, *, #13761, .F. ) ;
#3953=LINE ( 'NONE', #18861, #43618 ) ;
#3992=EDGE_CURVE ( 'NONE', #1521, #16286, #31660, .T. ) ;
#3993=EDGE_CURVE ( 'NONE', #21082, #44212, #18445, .T. ) ;
#3998=CIRCLE ( 'NONE', #42287, 15.99999999999999467 ) ;
#3999=LINE ( 'NONE', #19157, #32103 ) ;
#4007=DIRECTION ( 'NONE',  ( -1.000000000000000000, -0.000000000000000000, 0.000000000000000000 ) ) ;
#4020=LINE ( 'NONE', #4272, #32846 ) ;
#4022=CYLINDRICAL_SURFACE ( 'NONE', #5789, 42.00000000000000000 ) ;
#4028=VERTEX_POINT ( 'NONE', #27979 ) ;
#4031=CARTESIAN_POINT ( 'NONE',  ( 10.00000000000000000, 4.992566952384984269, 37.16516213103279398 ) ) ;
#4039=EDGE_CURVE ( 'NONE', #38706, #45887, #7485, .T. ) ;
#4055=ADVANCED_FACE ( 'NONE', ( #35062 ), #38257, .T. ) ;
#4056=ORIENTED_EDGE ( 'NONE', *, *, #2874, .T. ) ;
#4058=ORIENTED_EDGE ( 'NONE', *, *, #44385, .T. ) ;
#4061=CYLINDRICAL_SURFACE ( 'NONE', #24898, 16.00000000000000000 ) ;
#4062=CARTESIAN_POINT ( 'NONE',  ( -3.000000000000000000, -13.04903810567647682, -19.60159698893442481 ) ) ;
#4067=ORIENTED_EDGE ( 'NONE', *, *, #788, .F. ) ;
#4069=EDGE_LOOP ( 'NONE', ( #11121, #19683, #17058, #33040 ) ) ;
#4075=DIRECTION ( 'NONE',  ( -1.000000000000000000, -0.000000000000000000, 0.000000000000000000 ) ) ;
#4076=CARTESIAN_POINT ( 'NONE',  ( -3.000000000000000000, -3.948201729842038432, -23.21447184625298021 ) ) ;
#4082=CARTESIAN_POINT ( 'NONE',  ( 10.00000000000000000, 16.23288003029497162, 33.80338159004289622 ) ) ;
#4104=EDGE_CURVE ( 'NONE', #45931, #18858, #38019, .T. ) ;
#4115=AXIS2_PLACEMENT_3D ( 'NONE', #23159, #868, #22910 ) ;
#4116=DIRECTION ( 'NONE',  ( 0.000000000000000000, -0.8090169943749426773, -0.5877852522924797984 ) ) ;
#4119=DIRECTION ( 'NONE',  ( 0.000000000000000000, 0.000000000000000000, -1.000000000000000000 ) ) ;
#4120=DIRECTION ( 'NONE',  ( -1.000000000000000000, 0.000000000000000000, 0.000000000000000000 ) ) ;
#4130=DIRECTION ( 'NONE',  ( -1.000000000000000000, -0.000000000000000000, -0.000000000000000000 ) ) ;
#4131=ORIENTED_EDGE ( 'NONE', *, *, #15428, .T. ) ;
#4137=EDGE_CURVE ( 'NONE', #41352, #39824, #9097, .T. ) ;
#4145=DIRECTION ( 'NONE',  ( -1.000000000000000000, -0.000000000000000000, -0.000000000000000000 ) ) ;
#4147=DIRECTION ( 'NONE',  ( 0.000000000000000000, 0.000000000000000000, 1.000000000000000000 ) ) ;
#4158=LINE ( 'NONE', #48445, #2606 ) ;
#4162=EDGE_CURVE ( 'NONE', #29283, #24216, #6750, .T. ) ;
#4170=VECTOR ( 'NONE', #24251, 1000.000000000000000 ) ;
#4179=VERTEX_POINT ( 'NONE', #32129 ) ;
#4184=VECTOR ( 'NONE', #26548, 1000.000000000000000 ) ;
#4192=CARTESIAN_POINT ( 'NONE',  ( -3.000000000000000000, -25.60904388321925396, 6.976881207771172377 ) ) ;
#4201=ORIENTED_EDGE ( 'NONE', *, *, #25950, .F. ) ;
#4215=DIRECTION ( 'NONE',  ( 0.000000000000000000, 0.5877852522924689183, 0.8090169943749504489 ) ) ;
#4218=DIRECTION ( 'NONE',  ( -1.000000000000000000, -0.000000000000000000, -0.000000000000000000 ) ) ;
#4219=CIRCLE ( 'NONE', #31580, 16.00000000000000000 ) ;
#4226=VERTEX_POINT ( 'NONE', #10573 ) ;
#4237=DIRECTION ( 'NONE',  ( -1.000000000000000000, -0.000000000000000000, -0.000000000000000000 ) ) ;
#4238=VECTOR ( 'NONE', #45848, 1000.000000000000000 ) ;
#4240=EDGE_CURVE ( 'NONE', #43656, #43844, #34906, .T. ) ;
#4246=CARTESIAN_POINT ( 'NONE',  ( 0.000000000000000000, -4.261787119644969479, -26.19803753235780519 ) ) ;
#4249=ORIENTED_EDGE ( 'NONE', *, *, #34403, .F. ) ;
#4262=DIRECTION ( 'NONE',  ( 0.000000000000000000, -0.9876883405951358830, -0.1564344650402421932 ) ) ;
#4263=ORIENTED_EDGE ( 'NONE', *, *, #47960, .T. ) ;
#4272=CARTESIAN_POINT ( 'NONE',  ( -3.000000000000000000, 5.835314593368772229, -22.81335362449846826 ) ) ;
#4276=DIRECTION ( 'NONE',  ( 0.000000000000000000, 0.7431448254773960205, -0.6691306063588563502 ) ) ;
#4296=DIRECTION ( 'NONE',  ( 1.000000000000000000, -0.000000000000000000, 0.000000000000000000 ) ) ;
#4304=DIRECTION ( 'NONE',  ( 0.000000000000000000, 0.000000000000000000, 1.000000000000000000 ) ) ;
#4311=DIRECTION ( 'NONE',  ( 0.000000000000000000, -0.8090169943749402348, -0.5877852522924830181 ) ) ;
#4314=PLANE ( 'NONE',  #107 ) ;
#4315=AXIS2_PLACEMENT_3D ( 'NONE', #11496, #37428, #3896 ) ;
#4325=DIRECTION ( 'NONE',  ( 1.000000000000000000, -0.000000000000000000, -0.000000000000000000 ) ) ;
#4329=ADVANCED_FACE ( 'NONE', ( #22547 ), #37477, .T. ) ;
#4336=CARTESIAN_POINT ( 'NONE',  ( -3.000000000000000000, 8.688484142254221609, -21.88630264137359660 ) ) ;
#4340=ORIENTED_EDGE ( 'NONE', *, *, #41488, .T. ) ;
#4360=ORIENTED_EDGE ( 'NONE', *, *, #23706, .T. ) ;
#4372=EDGE_CURVE ( 'NONE', #23243, #48285, #32531, .T. ) ;
#4375=PLANE ( 'NONE',  #18825 ) ;
#4378=ORIENTED_EDGE ( 'NONE', *, *, #1900, .F. ) ;
#4382=VERTEX_POINT ( 'NONE', #7127 ) ;
#4388=VECTOR ( 'NONE', #27248, 1000.000000000000000 ) ;
#4389=ORIENTED_EDGE ( 'NONE', *, *, #14264, .F. ) ;
#4394=AXIS2_PLACEMENT_3D ( 'NONE', #17690, #11069, #14257 ) ;
#4411=DIRECTION ( 'NONE',  ( 0.000000000000000000, 0.000000000000000000, 1.000000000000000000 ) ) ;
#4425=ORIENTED_EDGE ( 'NONE', *, *, #109, .F. ) ;
#4432=ORIENTED_EDGE ( 'NONE', *, *, #40707, .F. ) ;
#4433=ORIENTED_EDGE ( 'NONE', *, *, #47454, .T. ) ;
#4435=ORIENTED_EDGE ( 'NONE', *, *, #24594, .T. ) ;
#4439=EDGE_LOOP ( 'NONE', ( #4724, #31097, #7764, #12357 ) ) ;
#4443=ORIENTED_EDGE ( 'NONE', *, *, #35276, .T. ) ;
#4464=ORIENTED_EDGE ( 'NONE', *, *, #3239, .T. ) ;
#4466=CARTESIAN_POINT ( 'NONE',  ( -3.000000000000000000, -22.67460108101783334, 6.353146135317912169 ) ) ;
#4471=LINE ( 'NONE', #41923, #22236 ) ;
#4499=EDGE_CURVE ( 'NONE', #45945, #13250, #46208, .T. ) ;
#4501=AXIS2_PLACEMENT_3D ( 'NONE', #34406, #419, #26372 ) ;
#4510=EDGE_CURVE ( 'NONE', #36037, #34495, #45532, .T. ) ;
#4513=DIRECTION ( 'NONE',  ( 0.000000000000000000, 0.7071067811865437980, 0.7071067811865512365 ) ) ;
#4516=CARTESIAN_POINT ( 'NONE',  ( 0.000000000000000000, 0.000000000000000000, 0.000000000000000000 ) ) ;
#4542=DIRECTION ( 'NONE',  ( 0.000000000000000000, -0.9510565162951543083, 0.3090169943749448977 ) ) ;
#4544=EDGE_LOOP ( 'NONE', ( #18045, #5491, #30306, #6998 ) ) ;
#4545=EDGE_LOOP ( 'NONE', ( #9000, #1149, #30941, #9109 ) ) ;
#4558=CARTESIAN_POINT ( 'NONE',  ( 10.00000000000000000, 0.000000000000000000, 0.000000000000000000 ) ) ;
#4567=CYLINDRICAL_SURFACE ( 'NONE', #45840, 16.00000000000000000 ) ;
#4576=EDGE_CURVE ( 'NONE', #44846, #29574, #35268, .T. ) ;
#4579=DIRECTION ( 'NONE',  ( -1.000000000000000000, 0.000000000000000000, 0.000000000000000000 ) ) ;
#4581=DIRECTION ( 'NONE',  ( 0.000000000000000000, 0.000000000000000000, 1.000000000000000000 ) ) ;
#4583=AXIS2_PLACEMENT_3D ( 'NONE', #545, #23058, #12298 ) ;
#4590=EDGE_LOOP ( 'NONE', ( #38749, #25039, #39816, #33011 ) ) ;
#4599=CARTESIAN_POINT ( 'NONE',  ( -3.000000000000000000, -20.55727247249748046, 16.78983467731285018 ) ) ;
#4601=DIRECTION ( 'NONE',  ( -1.000000000000000000, -0.000000000000000000, -0.000000000000000000 ) ) ;
#4603=DIRECTION ( 'NONE',  ( 0.000000000000000000, 0.000000000000000000, -1.000000000000000000 ) ) ;
#4606=LINE ( 'NONE', #191, #16586 ) ;
#4609=FACE_OUTER_BOUND ( 'NONE', #19287, .T. ) ;
#4620=DIRECTION ( 'NONE',  ( -1.000000000000000000, 0.000000000000000000, 0.000000000000000000 ) ) ;
#4639=ORIENTED_EDGE ( 'NONE', *, *, #47082, .T. ) ;
#4654=DIRECTION ( 'NONE',  ( -1.000000000000000000, 0.000000000000000000, -0.000000000000000000 ) ) ;
#4676=DIRECTION ( 'NONE',  ( 1.000000000000000000, 0.000000000000000000, 0.000000000000000000 ) ) ;
#4680=PLANE ( 'NONE',  #7907 ) ;
#4683=DIRECTION ( 'NONE',  ( -1.000000000000000000, 0.000000000000000000, 0.000000000000000000 ) ) ;
#4686=CARTESIAN_POINT ( 'NONE',  ( -3.000000000000000000, -13.04903810567647682, -19.60159698893442481 ) ) ;
#4687=LINE ( 'NONE', #34530, #27181 ) ;
#4692=CARTESIAN_POINT ( 'NONE',  ( -3.000000000000000000, 0.000000000000000000, 0.000000000000000000 ) ) ;
#4700=ORIENTED_EDGE ( 'NONE', *, *, #30300, .T. ) ;
#4707=EDGE_CURVE ( 'NONE', #44212, #1265, #7741, .T. ) ;
#4717=VERTEX_POINT ( 'NONE', #7970 ) ;
#4718=VERTEX_POINT ( 'NONE', #3832 ) ;
#4722=CIRCLE ( 'NONE', #30518, 37.49900000000000233 ) ;
#4724=ORIENTED_EDGE ( 'NONE', *, *, #38571, .T. ) ;
#4725=VECTOR ( 'NONE', #27484, 1000.000000000000000 ) ;
#4726=DIRECTION ( 'NONE',  ( -1.000000000000000000, 0.000000000000000000, 0.000000000000000000 ) ) ;
#4744=EDGE_CURVE ( 'NONE', #44883, #43819, #23554, .T. ) ;
#4746=DIRECTION ( 'NONE',  ( -0.000000000000000000, 0.4999999999999919509, 0.8660254037844432595 ) ) ;
#4747=SURFACE_STYLE_USAGE ( .BOTH. , #9610 ) ;
#4750=DIRECTION ( 'NONE',  ( 0.000000000000000000, 0.000000000000000000, 1.000000000000000000 ) ) ;
#4769=ORIENTED_EDGE ( 'NONE', *, *, #28237, .F. ) ;
#4770=ORIENTED_EDGE ( 'NONE', *, *, #17122, .T. ) ;
#4775=EDGE_CURVE ( 'NONE', #15212, #15797, #37613, .T. ) ;
#4781=CYLINDRICAL_SURFACE ( 'NONE', #36755, 42.00000000000000000 ) ;
#4783=ORIENTED_EDGE ( 'NONE', *, *, #37222, .F. ) ;
#4784=DIRECTION ( 'NONE',  ( -1.000000000000000000, 0.000000000000000000, -0.000000000000000000 ) ) ;
#4786=DIRECTION ( 'NONE',  ( 0.000000000000000000, -0.5877852522924624790, -0.8090169943749550008 ) ) ;
#4819=AXIS2_PLACEMENT_3D ( 'NONE', #9293, #31594, #16175 ) ;
#4836=COLOUR_RGB ( '', 0.66274510, 0.83137255, 0.94901961) ;
#4838=CARTESIAN_POINT ( 'NONE',  ( -3.000000000000000000, 0.000000000000000000, 0.000000000000000000 ) ) ;
#4841=EDGE_CURVE ( 'NONE', #9394, #23424, #38828, .T. ) ;
#4842=FACE_OUTER_BOUND ( 'NONE', #29012, .T. ) ;
#4868=EDGE_CURVE ( 'NONE', #26745, #26652, #19551, .T. ) ;
#4878=EDGE_LOOP ( 'NONE', ( #45223, #33983, #40826, #789 ) ) ;
#4880=VECTOR ( 'NONE', #8257, 1000.000000000000000 ) ;
#4883=ORIENTED_EDGE ( 'NONE', *, *, #17913, .F. ) ;
#4887=ORIENTED_EDGE ( 'NONE', *, *, #35298, .T. ) ;
#4899=CARTESIAN_POINT ( 'NONE',  ( 0.000000000000000000, -13.04903810567647682, -19.60159698893442126 ) ) ;
#4908=VECTOR ( 'NONE', #42486, 1000.000000000000000 ) ;
#4913=CARTESIAN_POINT ( 'NONE',  ( 0.000000000000000000, -37.22597642581153821, -5.202137450156795850 ) ) ;
#4915=VECTOR ( 'NONE', #4296, 1000.000000000000000 ) ;
#4933=LINE ( 'NONE', #19850, #29587 ) ;
#4941=VECTOR ( 'NONE', #27372, 1000.000000000000000 ) ;
#4947=CIRCLE ( 'NONE', #47152, 16.00000000000000000 ) ;
#4956=ORIENTED_EDGE ( 'NONE', *, *, #315, .F. ) ;
#4959=ORIENTED_EDGE ( 'NONE', *, *, #46112, .T. ) ;
#4963=DIRECTION ( 'NONE',  ( 1.000000000000000000, 0.000000000000000000, 0.000000000000000000 ) ) ;
#4967=ORIENTED_EDGE ( 'NONE', *, *, #5434, .F. ) ;
#4968=CARTESIAN_POINT ( 'NONE',  ( 0.000000000000000000, -3.948201729842038432, -23.21447184625298021 ) ) ;
#4971=VECTOR ( 'NONE', #21884, 1000.000000000000000 ) ;
#4975=DIRECTION ( 'NONE',  ( -0.000000000000000000, -0.3090169943749573878, 0.9510565162951503115 ) ) ;
#4978=ORIENTED_EDGE ( 'NONE', *, *, #46852, .F. ) ;
#4990=( LENGTH_UNIT ( ) NAMED_UNIT ( * ) SI_UNIT ( .MILLI., .METRE. ) );
#5007=AXIS2_PLACEMENT_3D ( 'NONE', #39002, #46103, #5237 ) ;
#5014=AXIS2_PLACEMENT_3D ( 'NONE', #43167, #13542, #9616 ) ;
#5019=DIRECTION ( 'NONE',  ( -1.000000000000000000, -0.000000000000000000, 0.000000000000000000 ) ) ;
#5020=ORIENTED_EDGE ( 'NONE', *, *, #35027, .T. ) ;
#5021=EDGE_CURVE ( 'NONE', #13181, #7846, #34413, .T. ) ;
#5024=EDGE_CURVE ( 'NONE', #43844, #23166, #2382, .T. ) ;
#5031=ORIENTED_EDGE ( 'NONE', *, *, #16588, .T. ) ;
#5046=CARTESIAN_POINT ( 'NONE',  ( 10.00000000000000000, 0.000000000000000000, 0.000000000000000000 ) ) ;
#5047=DIRECTION ( 'NONE',  ( -1.000000000000000000, 0.000000000000000000, -0.000000000000000000 ) ) ;
#5048=CYLINDRICAL_SURFACE ( 'NONE', #19703, 37.49900000000000233 ) ;
#5053=AXIS2_PLACEMENT_3D ( 'NONE', #40769, #31832, #33427 ) ;
#5067=VERTEX_POINT ( 'NONE', #2553 ) ;
#5069=ORIENTED_EDGE ( 'NONE', *, *, #11174, .F. ) ;
#5085=ORIENTED_EDGE ( 'NONE', *, *, #43004, .F. ) ;
#5100=DIRECTION ( 'NONE',  ( -1.000000000000000000, 0.000000000000000000, 0.000000000000000000 ) ) ;
#5103=DIRECTION ( 'NONE',  ( 1.000000000000000000, -0.000000000000000000, -0.000000000000000000 ) ) ;
#5113=ORIENTED_EDGE ( 'NONE', *, *, #27834, .T. ) ;
#5118=DIRECTION ( 'NONE',  ( 0.000000000000000000, 0.000000000000000000, 1.000000000000000000 ) ) ;
#5121=FACE_OUTER_BOUND ( 'NONE', #38688, .T. ) ;
#5123=DIRECTION ( 'NONE',  ( 0.000000000000000000, 0.000000000000000000, 1.000000000000000000 ) ) ;
#5135=AXIS2_PLACEMENT_3D ( 'NONE', #14569, #42430, #27511 ) ;
#5139=ORIENTED_EDGE ( 'NONE', *, *, #3870, .F. ) ;
#5143=LINE ( 'NONE', #16628, #39016 ) ;
#5144=VERTEX_POINT ( 'NONE', #11605 ) ;
#5147=ORIENTED_EDGE ( 'NONE', *, *, #3993, .T. ) ;
#5179=FACE_OUTER_BOUND ( 'NONE', #35692, .T. ) ;
#5182=EDGE_CURVE ( 'NONE', #28663, #40104, #4020, .T. ) ;
#5184=CARTESIAN_POINT ( 'NONE',  ( 10.00000000000000000, -30.84782396557233142, 21.32104025579104345 ) ) ;
#5200=DIRECTION ( 'NONE',  ( 0.000000000000000000, -0.4539904997395351471, -0.8910065241883737830 ) ) ;
#5213=AXIS2_PLACEMENT_3D ( 'NONE', #17310, #40742, #46950 ) ;
#5215=CYLINDRICAL_SURFACE ( 'NONE', #8626, 16.00000000000000000 ) ;
#5217=DIRECTION ( 'NONE',  ( 0.000000000000000000, 0.000000000000000000, 1.000000000000000000 ) ) ;
#5229=EDGE_LOOP ( 'NONE', ( #10292, #13984, #30464, #42160 ) ) ;
#5231=LINE ( 'NONE', #34829, #34858 ) ;
#5232=ORIENTED_EDGE ( 'NONE', *, *, #26861, .F. ) ;
#5233=CARTESIAN_POINT ( 'NONE',  ( 0.000000000000000000, 40.98264845739749518, 9.188173127307448951 ) ) ;
#5234=FACE_OUTER_BOUND ( 'NONE', #33563, .T. ) ;
#5237=DIRECTION ( 'NONE',  ( 0.000000000000000000, 0.000000000000000000, 1.000000000000000000 ) ) ;
#5238=DIRECTION ( 'NONE',  ( -1.000000000000000000, -0.000000000000000000, -0.000000000000000000 ) ) ;
#5239=CARTESIAN_POINT ( 'NONE',  ( 10.00000000000000000, 2.663952781846149254, 41.91543099594818500 ) ) ;
#5248=FACE_OUTER_BOUND ( 'NONE', #30473, .T. ) ;
#5251=CARTESIAN_POINT ( 'NONE',  ( 0.000000000000000000, 0.000000000000000000, 0.000000000000000000 ) ) ;
#5254=FACE_OUTER_BOUND ( 'NONE', #25274, .T. ) ;
#5259=ORIENTED_EDGE ( 'NONE', *, *, #31573, .T. ) ;
#5262=EDGE_CURVE ( 'NONE', #44202, #844, #43063, .T. ) ;
#5263=ORIENTED_EDGE ( 'NONE', *, *, #13128, .F. ) ;
#5265=EDGE_CURVE ( 'NONE', #5635, #27337, #7098, .T. ) ;
#5267=CARTESIAN_POINT ( 'NONE',  ( 0.000000000000000000, 5.835314593368772229, -22.81335362449846826 ) ) ;
#5268=ORIENTED_EDGE ( 'NONE', *, *, #16498, .F. ) ;
#5269=DIRECTION ( 'NONE',  ( -1.000000000000000000, 0.000000000000000000, 0.000000000000000000 ) ) ;
#5277=CARTESIAN_POINT ( 'NONE',  ( 0.000000000000000000, 21.40280677340371795, 36.13751322684426270 ) ) ;
#5280=CIRCLE ( 'NONE', #46728, 15.99999999999999822 ) ;
#5281=VERTEX_POINT ( 'NONE', #27505 ) ;
#5285=DIRECTION ( 'NONE',  ( -1.000000000000000000, -0.000000000000000000, 0.000000000000000000 ) ) ;
#5286=CARTESIAN_POINT ( 'NONE',  ( 10.00000000000000000, -12.42422080174614862, -35.38097989696524337 ) ) ;
#5287=DIRECTION ( 'NONE',  ( -1.000000000000000000, 0.000000000000000000, 0.000000000000000000 ) ) ;
#5291=EDGE_LOOP ( 'NONE', ( #20284, #4067, #21062, #29196 ) ) ;
#5306=EDGE_CURVE ( 'NONE', #34900, #4717, #19594, .T. ) ;
#5307=FACE_OUTER_BOUND ( 'NONE', #27252, .T. ) ;
#5310=EDGE_CURVE ( 'NONE', #10117, #30305, #23571, .T. ) ;
#5321=EDGE_CURVE ( 'NONE', #21795, #34900, #25051, .T. ) ;
#5331=CARTESIAN_POINT ( 'NONE',  ( 0.000000000000000000, -4.261787119645322974, 26.19803753235775190 ) ) ;
#5333=AXIS2_PLACEMENT_3D ( 'NONE', #11546, #34043, #525 ) ;
#5336=CARTESIAN_POINT ( 'NONE',  ( 10.00000000000000000, 10.74501242461282757, 35.92658777277515014 ) ) ;
#5343=CARTESIAN_POINT ( 'NONE',  ( -3.000000000000000000, 8.688484142253939169, 21.88630264137371029 ) ) ;
#5347=ORIENTED_EDGE ( 'NONE', *, *, #35422, .F. ) ;
#5357=CYLINDRICAL_SURFACE ( 'NONE', #33057, 37.49900000000000233 ) ;
#5359=CARTESIAN_POINT ( 'NONE',  ( 10.00000000000000000, 6.555932627142952995, -37.01155633439051940 ) ) ;
#5361=DIRECTION ( 'NONE',  ( 0.000000000000000000, 0.000000000000000000, 1.000000000000000000 ) ) ;
#5363=EDGE_CURVE ( 'NONE', #39037, #17758, #16003, .T. ) ;
#5366=ORIENTED_EDGE ( 'NONE', *, *, #15708, .F. ) ;
#5383=VERTEX_POINT ( 'NONE', #25200 ) ;
#5386=ORIENTED_EDGE ( 'NONE', *, *, #29081, .T. ) ;
#5396=CARTESIAN_POINT ( 'NONE',  ( 10.00000000000000000, 0.000000000000000000, 0.000000000000000000 ) ) ;
#5403=ORIENTED_EDGE ( 'NONE', *, *, #22500, .T. ) ;
#5413=CARTESIAN_POINT ( 'NONE',  ( 10.00000000000000000, 16.23288003029497162, 33.80338159004289622 ) ) ;
#5424=VERTEX_POINT ( 'NONE', #18140 ) ;
#5434=EDGE_CURVE ( 'NONE', #2104, #19636, #14135, .T. ) ;
#5435=CYLINDRICAL_SURFACE ( 'NONE', #32775, 42.00000000000000000 ) ;
#5437=CIRCLE ( 'NONE', #11689, 42.00000000000000000 ) ;
#5438=ORIENTED_EDGE ( 'NONE', *, *, #42067, .F. ) ;
#5440=ADVANCED_FACE ( 'NONE', ( #36036 ), #21824, .F. ) ;
#5445=FACE_OUTER_BOUND ( 'NONE', #12976, .T. ) ;
#5447=CARTESIAN_POINT ( 'NONE',  ( 10.00000000000000000, -16.23288003029521320, 33.80338159004277543 ) ) ;
#5450=DIRECTION ( 'NONE',  ( 0.000000000000000000, 0.000000000000000000, -1.000000000000000000 ) ) ;
#5451=EDGE_CURVE ( 'NONE', #48002, #37265, #2982, .T. ) ;
#5461=ORIENTED_EDGE ( 'NONE', *, *, #20226, .F. ) ;
#5475=CARTESIAN_POINT ( 'NONE',  ( 10.00000000000000000, 0.000000000000000000, 0.000000000000000000 ) ) ;
#5485=ADVANCED_FACE ( 'NONE', ( #10589 ), #28926, .T. ) ;
#5488=EDGE_LOOP ( 'NONE', ( #7913, #40715, #15550, #23949 ) ) ;
#5491=ORIENTED_EDGE ( 'NONE', *, *, #23362, .T. ) ;
#5494=CIRCLE ( 'NONE', #11750, 42.00000000000000000 ) ;
#5503=ORIENTED_EDGE ( 'NONE', *, *, #37007, .T. ) ;
#5513=DIRECTION ( 'NONE',  ( 0.000000000000000000, 0.7071067811865487940, -0.7071067811865462405 ) ) ;
#5515=FACE_OUTER_BOUND ( 'NONE', #36818, .T. ) ;
#5521=CARTESIAN_POINT ( 'NONE',  ( 10.00000000000000000, 0.000000000000000000, 0.000000000000000000 ) ) ;
#5522=ORIENTED_EDGE ( 'NONE', *, *, #3171, .F. ) ;
#5526=CARTESIAN_POINT ( 'NONE',  ( 5.000000000000000000, -15.48615015657555993, -39.04073710021360455 ) ) ;
#5529=DIRECTION ( 'NONE',  ( 0.000000000000000000, 0.1564344650402243742, 0.9876883405951387696 ) ) ;
#5530=DIRECTION ( 'NONE',  ( 0.000000000000000000, 0.000000000000000000, 1.000000000000000000 ) ) ;
#5536=CARTESIAN_POINT ( 'NONE',  ( -3.000000000000000000, 6.762365576493310826, 25.66652317338401090 ) ) ;
#5540=DIRECTION ( 'NONE',  ( 0.000000000000000000, 0.3090169943749411230, 0.9510565162951555296 ) ) ;
#5541=AXIS2_PLACEMENT_3D ( 'NONE', #21601, #3216, #32142 ) ;
#5542=CIRCLE ( 'NONE', #45390, 37.49900000000001654 ) ;
#5548=VERTEX_POINT ( 'NONE', #17677 ) ;
#5551=EDGE_LOOP ( 'NONE', ( #18316, #29263, #16885, #14009 ) ) ;
#5569=ORIENTED_EDGE ( 'NONE', *, *, #16625, .F. ) ;
#5578=ORIENTED_EDGE ( 'NONE', *, *, #42683, .F. ) ;
#5580=DIRECTION ( 'NONE',  ( 0.000000000000000000, 0.000000000000000000, 1.000000000000000000 ) ) ;
#5590=ORIENTED_EDGE ( 'NONE', *, *, #32644, .T. ) ;
#5592=DIRECTION ( 'NONE',  ( 0.000000000000000000, -0.8910065241883627918, -0.4539904997395569630 ) ) ;
#5593=CARTESIAN_POINT ( 'NONE',  ( -3.000000000000000000, 24.81905959214261514, 9.408202855044825341 ) ) ;
#5600=DIRECTION ( 'NONE',  ( 0.000000000000000000, 0.3090169943749580539, -0.9510565162951500895 ) ) ;
#5606=FACE_OUTER_BOUND ( 'NONE', #10182, .T. ) ;
#5624=DIRECTION ( 'NONE',  ( 0.000000000000000000, 0.000000000000000000, 1.000000000000000000 ) ) ;
#5633=FACE_OUTER_BOUND ( 'NONE', #32791, .T. ) ;
#5635=VERTEX_POINT ( 'NONE', #29898 ) ;
#5645=DIRECTION ( 'NONE',  ( -1.000000000000000000, -0.000000000000000000, -0.000000000000000000 ) ) ;
#5649=LINE ( 'NONE', #8581, #41714 ) ;
#5657=CARTESIAN_POINT ( 'NONE',  ( 0.000000000000000000, -13.04903810567675038, 19.60159698893425428 ) ) ;
#5673=AXIS2_PLACEMENT_3D ( 'NONE', #11055, #29893, #21820 ) ;
#5676=VERTEX_POINT ( 'NONE', #15231 ) ;
#5683=DIRECTION ( 'NONE',  ( -0.000000000000000000, -0.8660254037844427044, 0.4999999999999929501 ) ) ;
#5686=ORIENTED_EDGE ( 'NONE', *, *, #33838, .F. ) ;
#5698=EDGE_CURVE ( 'NONE', #26745, #38886, #5649, .T. ) ;
#5704=ORIENTED_EDGE ( 'NONE', *, *, #31177, .T. ) ;
#5708=CARTESIAN_POINT ( 'NONE',  ( 10.00000000000000000, 0.000000000000000000, 0.000000000000000000 ) ) ;
#5710=AXIS2_PLACEMENT_3D ( 'NONE', #483, #10775, #37440 ) ;
#5717=APPLICATION_CONTEXT ( 'automotive_design' ) ;
#5719=CIRCLE ( 'NONE', #16683, 16.00000000000000000 ) ;
#5721=DIRECTION ( 'NONE',  ( 1.000000000000000000, 0.000000000000000000, 0.000000000000000000 ) ) ;
#5723=VERTEX_POINT ( 'NONE', #9083 ) ;
#5728=CARTESIAN_POINT ( 'NONE',  ( 5.000000000000000000, -35.47612816024506088, -22.48208911017539435 ) ) ;
#5733=EDGE_LOOP ( 'NONE', ( #2894, #20657, #21930, #1720 ) ) ;
#5735=ORIENTED_EDGE ( 'NONE', *, *, #44041, .T. ) ;
#5742=DIRECTION ( 'NONE',  ( -1.000000000000000000, -0.000000000000000000, 0.000000000000000000 ) ) ;
#5748=CARTESIAN_POINT ( 'NONE',  ( 0.000000000000000000, 0.000000000000000000, 0.000000000000000000 ) ) ;
#5749=AXIS2_PLACEMENT_3D ( 'NONE', #47639, #6538, #10203 ) ;
#5757=CIRCLE ( 'NONE', #22164, 37.49900000000000944 ) ;
#5764=PLANE ( 'NONE',  #17590 ) ;
#5774=DIRECTION ( 'NONE',  ( 0.000000000000000000, -0.8090169943749531134, 0.5877852522924654766 ) ) ;
#5783=AXIS2_PLACEMENT_3D ( 'NONE', #33233, #40573, #48159 ) ;
#5788=ORIENTED_EDGE ( 'NONE', *, *, #35521, .T. ) ;
#5789=AXIS2_PLACEMENT_3D ( 'NONE', #3772, #587, #7685 ) ;
#5797=ORIENTED_EDGE ( 'NONE', *, *, #35027, .F. ) ;
#5803=ORIENTED_EDGE ( 'NONE', *, *, #3360, .F. ) ;
#5826=EDGE_CURVE ( 'NONE', #40027, #23243, #41901, .T. ) ;
#5828=AXIS2_PLACEMENT_3D ( 'NONE', #15167, #41587, #30093 ) ;
#5832=CARTESIAN_POINT ( 'NONE',  ( 0.000000000000000000, -21.40280677340398086, 36.13751322684410638 ) ) ;
#5839=CYLINDRICAL_SURFACE ( 'NONE', #11063, 16.00000000000000000 ) ;
#5847=DIRECTION ( 'NONE',  ( 0.000000000000000000, 0.8910065241883656784, 0.4539904997395511899 ) ) ;
#5851=DIRECTION ( 'NONE',  ( 0.000000000000000000, 0.000000000000000000, 1.000000000000000000 ) ) ;
#5852=DIRECTION ( 'NONE',  ( -0.000000000000000000, 0.1045284632676570929, -0.9945218953682730678 ) ) ;
#5865=DIRECTION ( 'NONE',  ( -1.000000000000000000, -0.000000000000000000, -0.000000000000000000 ) ) ;
#5871=CARTESIAN_POINT ( 'NONE',  ( 0.000000000000000000, -27.13269053701114331, 25.88420570971391754 ) ) ;
#5874=ORIENTED_EDGE ( 'NONE', *, *, #25487, .F. ) ;
#5875=ADVANCED_FACE ( 'NONE', ( #9796 ), #40149, .F. ) ;
#5880=VERTEX_POINT ( 'NONE', #47245 ) ;
#5881=LINE ( 'NONE', #17830, #20780 ) ;
#5883=DIRECTION ( 'NONE',  ( -1.000000000000000000, -0.000000000000000000, -0.000000000000000000 ) ) ;
#5896=VERTEX_POINT ( 'NONE', #2928 ) ;
#5898=CARTESIAN_POINT ( 'NONE',  ( 10.00000000000000000, -27.05870788708213226, -26.08949754953053102 ) ) ;
#5901=DIRECTION ( 'NONE',  ( -1.000000000000000000, 0.000000000000000000, 0.000000000000000000 ) ) ;
#5909=CARTESIAN_POINT ( 'NONE',  ( -3.000000000000000000, -1.278221433540502217, 26.51162292216071847 ) ) ;
#5915=VECTOR ( 'NONE', #43201, 1000.000000000000000 ) ;
#5919=ADVANCED_FACE ( 'NONE', ( #10035 ), #9544, .T. ) ;
#5928=ADVANCED_FACE ( 'NONE', ( #40392 ), #47702, .T. ) ;
#5930=ORIENTED_EDGE ( 'NONE', *, *, #8418, .T. ) ;
#5933=DIRECTION ( 'NONE',  ( -1.000000000000000000, 0.000000000000000000, 0.000000000000000000 ) ) ;
#5942=LINE ( 'NONE', #2480, #30920 ) ;
#5943=ORIENTED_EDGE ( 'NONE', *, *, #4510, .T. ) ;
#5966=LINE ( 'NONE', #1795, #2588 ) ;
#5971=ORIENTED_EDGE ( 'NONE', *, *, #33757, .T. ) ;
#5975=LINE ( 'NONE', #38588, #37901 ) ;
#5976=ORIENTED_EDGE ( 'NONE', *, *, #40959, .T. ) ;
#5979=AXIS2_PLACEMENT_3D ( 'NONE', #21891, #21169, #3282 ) ;
#5986=CIRCLE ( 'NONE', #7508, 16.00000000000000355 ) ;
#5993=VERTEX_POINT ( 'NONE', #48204 ) ;
#5997=EDGE_CURVE ( 'NONE', #19709, #42613, #33144, .T. ) ;
#6006=ORIENTED_EDGE ( 'NONE', *, *, #39525, .T. ) ;
#6007=CYLINDRICAL_SURFACE ( 'NONE', #39763, 37.49900000000000233 ) ;
#6008=DIRECTION ( 'NONE',  ( 0.000000000000000000, 0.1564344650402312298, -0.9876883405951375483 ) ) ;
#6015=FACE_BOUND ( 'NONE', #26383, .T. ) ;
#6024=DIRECTION ( 'NONE',  ( -1.000000000000000000, -0.000000000000000000, -0.000000000000000000 ) ) ;
#6028=DIRECTION ( 'NONE',  ( -0.000000000000000000, 0.2079116908177543743, 0.9781476007338066880 ) ) ;
#6029=CARTESIAN_POINT ( 'NONE',  ( 10.00000000000000000, -35.53030884539094103, 12.26510123303246935 ) ) ;
#6034=LINE ( 'NONE', #24856, #1881 ) ;
#6044=VERTEX_POINT ( 'NONE', #41118 ) ;
#6050=DIRECTION ( 'NONE',  ( -0.000000000000000000, 0.8090169943749504489, -0.5877852522924689183 ) ) ;
#6053=VECTOR ( 'NONE', #3481, 1000.000000000000000 ) ;
#6059=ORIENTED_EDGE ( 'NONE', *, *, #6753, .T. ) ;
#6068=DIRECTION ( 'NONE',  ( 1.000000000000000000, -0.000000000000000000, 0.000000000000000000 ) ) ;
#6072=CARTESIAN_POINT ( 'NONE',  ( -3.000000000000000000, -23.29833615347104825, -3.418703333116803744 ) ) ;
#6074=CYLINDRICAL_SURFACE ( 'NONE', #33855, 16.00000000000000000 ) ;
#6085=CARTESIAN_POINT ( 'NONE',  ( 0.000000000000000000, 5.835314593368772229, -22.81335362449846826 ) ) ;
#6102=EDGE_CURVE ( 'NONE', #40367, #13990, #8297, .T. ) ;
#6115=CYLINDRICAL_SURFACE ( 'NONE', #40356, 42.00000000000000000 ) ;
#6132=DIRECTION ( 'NONE',  ( -1.000000000000000000, 0.000000000000000000, 0.000000000000000000 ) ) ;
#6134=CARTESIAN_POINT ( 'NONE',  ( -10.00000000000000000, 0.000000000000000000, 0.000000000000000000 ) ) ;
#6135=CYLINDRICAL_SURFACE ( 'NONE', #14828, 42.00000000000000000 ) ;
#6147=EDGE_CURVE ( 'NONE', #29882, #41810, #15637, .T. ) ;
#6160=CARTESIAN_POINT ( 'NONE',  ( 0.000000000000000000, 24.81905959214274660, -9.408202855044498492 ) ) ;
#6175=AXIS2_PLACEMENT_3D ( 'NONE', #26837, #7521, #876 ) ;
#6178=CARTESIAN_POINT ( 'NONE',  ( 4.999999999999999112, -9.188173127307592836, 40.98264845739746676 ) ) ;
#6185=VERTEX_POINT ( 'NONE', #16603 ) ;
#6187=VERTEX_POINT ( 'NONE', #1682 ) ;
#6189=VECTOR ( 'NONE', #5600, 1000.000000000000227 ) ;
#6191=DIRECTION ( 'NONE',  ( 0.000000000000000000, -0.5000000000000046629, 0.8660254037844359321 ) ) ;
#6204=CARTESIAN_POINT ( 'NONE',  ( 10.00000000000000000, -27.05870788708250885, 26.08949754953014022 ) ) ;
#6213=VECTOR ( 'NONE', #12285, 1000.000000000000000 ) ;
#6217=CARTESIAN_POINT ( 'NONE',  ( 10.00000000000000000, -33.79645857604525361, 16.45098606841114730 ) ) ;
#6222=CIRCLE ( 'NONE', #19495, 16.00000000000000355 ) ;
#6235=CARTESIAN_POINT ( 'NONE',  ( -3.000000000000000000, -19.89357724625003598, 12.59942793731059574 ) ) ;
#6236=DIRECTION ( 'NONE',  ( -1.000000000000000000, 0.000000000000000000, -0.000000000000000000 ) ) ;
#6242=FACE_OUTER_BOUND ( 'NONE', #609, .T. ) ;
#6243=ORIENTED_EDGE ( 'NONE', *, *, #26144, .F. ) ;
#6246=EDGE_CURVE ( 'NONE', #30662, #40104, #24424, .T. ) ;
#6255=FACE_OUTER_BOUND ( 'NONE', #2970, .T. ) ;
#6264=EDGE_CURVE ( 'NONE', #9557, #18553, #13655, .T. ) ;
#6267=DIRECTION ( 'NONE',  ( 0.000000000000000000, 0.9135454576426060846, -0.4067366430757888285 ) ) ;
#6274=ADVANCED_FACE ( 'NONE', ( #46723 ), #47186, .T. ) ;
#6278=VERTEX_POINT ( 'NONE', #43523 ) ;
#6279=VECTOR ( 'NONE', #24449, 999.9999999999998863 ) ;
#6281=EDGE_LOOP ( 'NONE', ( #10052, #25733, #43902, #30184 ) ) ;
#6284=EDGE_LOOP ( 'NONE', ( #36652, #41436, #33837, #12563 ) ) ;
#6285=CIRCLE ( 'NONE', #20347, 37.49900000000001654 ) ;
#6286=CARTESIAN_POINT ( 'NONE',  ( 0.000000000000000000, -6.555932627142676772, 37.01155633439056203 ) ) ;
#6302=DIRECTION ( 'NONE',  ( -1.000000000000000000, 0.000000000000000000, -0.000000000000000000 ) ) ;
#6305=CARTESIAN_POINT ( 'NONE',  ( 10.00000000000000000, -35.95386929396248377, -10.96151621346525751 ) ) ;
#6308=CARTESIAN_POINT ( 'NONE',  ( 0.000000000000000000, 0.000000000000000000, 0.000000000000000000 ) ) ;
#6315=CIRCLE ( 'NONE', #35196, 42.00000000000000000 ) ;
#6321=ADVANCED_FACE ( 'NONE', ( #36408, #32033 ), #28337, .F. ) ;
#6324=CARTESIAN_POINT ( 'NONE',  ( -3.000000000000000000, -1.278221433540502217, 26.51162292216071847 ) ) ;
#6331=ORIENTED_EDGE ( 'NONE', *, *, #8245, .F. ) ;
#6339=EDGE_CURVE ( 'NONE', #33751, #3180, #14137, .T. ) ;
#6344=ORIENTED_EDGE ( 'NONE', *, *, #34800, .T. ) ;
#6358=ORIENTED_EDGE ( 'NONE', *, *, #37322, .F. ) ;
#6368=CARTESIAN_POINT ( 'NONE',  ( 10.00000000000000000, -37.48860685352290290, -0.8828120875904512665 ) ) ;
#6372=CARTESIAN_POINT ( 'NONE',  ( 0.000000000000000000, -4.992566952384716927, -37.16516213103282951 ) ) ;
#6375=CARTESIAN_POINT ( 'NONE',  ( 10.00000000000000000, -22.48208911017525580, 35.47612816024516036 ) ) ;
#6383=LINE ( 'NONE', #21290, #4170 ) ;
#6384=CARTESIAN_POINT ( 'NONE',  ( -10.00000000000000000, 0.000000000000000000, 0.000000000000000000 ) ) ;
#6385=DIRECTION ( 'NONE',  ( -0.000000000000000000, -1.156482317317870936E-15, -1.000000000000000000 ) ) ;
#6389=DIRECTION ( 'NONE',  ( -1.000000000000000000, 0.000000000000000000, 0.000000000000000000 ) ) ;
#6395=LINE ( 'NONE', #18609, #39884 ) ;
#6397=CARTESIAN_POINT ( 'NONE',  ( -10.00000000000000000, 0.000000000000000000, 0.000000000000000000 ) ) ;
#6398=ORIENTED_EDGE ( 'NONE', *, *, #12184, .T. ) ;
#6403=CARTESIAN_POINT ( 'NONE',  ( 10.00000000000000000, 38.55633173627034438, -16.65560815589369881 ) ) ;
#6419=LINE ( 'NONE', #25236, #21713 ) ;
#6421=EDGE_LOOP ( 'NONE', ( #19900, #47515, #17849, #4464 ) ) ;
#6423=CARTESIAN_POINT ( 'NONE',  ( 0.000000000000000000, -40.68715046381921496, -10.41901085202121280 ) ) ;
#6431=CARTESIAN_POINT ( 'NONE',  ( 0.000000000000000000, 22.07842321921481243, 8.187992925817422218 ) ) ;
#6435=ORIENTED_EDGE ( 'NONE', *, *, #41297, .F. ) ;
#6437=DIRECTION ( 'NONE',  ( 0.000000000000000000, -0.1564344650402382242, 0.9876883405951366601 ) ) ;
#6439=CARTESIAN_POINT ( 'NONE',  ( 10.00000000000000000, 0.000000000000000000, 0.000000000000000000 ) ) ;
#6441=DIRECTION ( 'NONE',  ( 0.000000000000000000, 0.1564344650402311743, -0.9876883405951377704 ) ) ;
#6447=DIRECTION ( 'NONE',  ( 0.000000000000000000, -6.938893903907228378E-15, 1.000000000000000000 ) ) ;
#6454=EDGE_CURVE ( 'NONE', #27530, #26745, #19890, .T. ) ;
#6462=CIRCLE ( 'NONE', #33813, 42.00000000000000000 ) ;
#6467=VERTEX_POINT ( 'NONE', #44965 ) ;
#6486=CARTESIAN_POINT ( 'NONE',  ( 0.000000000000000000, -22.48208911017525580, 35.47612816024516036 ) ) ;
#6490=DIRECTION ( 'NONE',  ( 0.000000000000000000, 0.000000000000000000, 1.000000000000000000 ) ) ;
#6494=CIRCLE ( 'NONE', #39301, 37.49900000000001654 ) ;
#6495=LINE ( 'NONE', #21414, #940 ) ;
#6496=DIRECTION ( 'NONE',  ( -1.000000000000000000, 0.000000000000000000, 0.000000000000000000 ) ) ;
#6500=ORIENTED_EDGE ( 'NONE', *, *, #32399, .T. ) ;
#6503=DIRECTION ( 'NONE',  ( 0.000000000000000000, 0.4539904997395414754, 0.8910065241883706744 ) ) ;
#6504=ORIENTED_EDGE ( 'NONE', *, *, #34702, .F. ) ;
#6505=ORIENTED_EDGE ( 'NONE', *, *, #42634, .F. ) ;
#6517=AXIS2_PLACEMENT_3D ( 'NONE', #9676, #39067, #5530 ) ;
#6525=ORIENTED_EDGE ( 'NONE', *, *, #39348, .T. ) ;
#6526=ORIENTED_EDGE ( 'NONE', *, *, #26275, .T. ) ;
#6527=AXIS2_PLACEMENT_3D ( 'NONE', #26680, #41605, #22523 ) ;
#6538=DIRECTION ( 'NONE',  ( -1.000000000000000000, -0.000000000000000000, -0.000000000000000000 ) ) ;
#6542=CIRCLE ( 'NONE', #12800, 42.00000000000000000 ) ;
#6546=FACE_OUTER_BOUND ( 'NONE', #18308, .T. ) ;
#6551=DIRECTION ( 'NONE',  ( -1.000000000000000000, 0.000000000000000000, 0.000000000000000000 ) ) ;
#6557=AXIS2_PLACEMENT_3D ( 'NONE', #9151, #24084, #36299 ) ;
#6558=DIRECTION ( 'NONE',  ( 0.000000000000000000, 0.1564344650402243742, 0.9876883405951387696 ) ) ;
#6564=CIRCLE ( 'NONE', #31598, 16.00000000000000000 ) ;
#6578=EDGE_LOOP ( 'NONE', ( #20952, #45917, #31199, #13156 ) ) ;
#6580=ORIENTED_EDGE ( 'NONE', *, *, #30120, .F. ) ;
#6588=EDGE_LOOP ( 'NONE', ( #801, #12507, #1276, #31279 ) ) ;
#6591=CIRCLE ( 'NONE', #8166, 37.49900000000000233 ) ;
#6594=VECTOR ( 'NONE', #11990, 1000.000000000000000 ) ;
#6597=VERTEX_POINT ( 'NONE', #30759 ) ;
#6599=EDGE_CURVE ( 'NONE', #21733, #3134, #5975, .T. ) ;
#6604=LINE ( 'NONE', #26834, #19928 ) ;
#6607=FACE_OUTER_BOUND ( 'NONE', #36212, .T. ) ;
#6612=EDGE_CURVE ( 'NONE', #30788, #44254, #41820, .T. ) ;
#6619=DIRECTION ( 'NONE',  ( 0.000000000000000000, 0.000000000000000000, 1.000000000000000000 ) ) ;
#6622=ORIENTED_EDGE ( 'NONE', *, *, #14535, .T. ) ;
#6644=AXIS2_PLACEMENT_3D ( 'NONE', #43037, #39122, #5592 ) ;
#6647=DIRECTION ( 'NONE',  ( 0.000000000000000000, 0.000000000000000000, 1.000000000000000000 ) ) ;
#6661=AXIS2_PLACEMENT_3D ( 'NONE', #28506, #10132, #36076 ) ;
#6676=DIRECTION ( 'NONE',  ( 1.000000000000000000, 0.000000000000000000, 0.000000000000000000 ) ) ;
#6696=DIRECTION ( 'NONE',  ( -1.000000000000000000, 0.000000000000000000, 0.000000000000000000 ) ) ;
#6707=CARTESIAN_POINT ( 'NONE',  ( -3.000000000000000000, 0.000000000000000000, 0.000000000000000000 ) ) ;
#6711=ORIENTED_EDGE ( 'NONE', *, *, #25405, .F. ) ;
#6716=DIRECTION ( 'NONE',  ( 0.000000000000000000, 0.000000000000000000, 1.000000000000000000 ) ) ;
#6720=CARTESIAN_POINT ( 'NONE',  ( 0.000000000000000000, 16.65560815589464028, -38.55633173626993226 ) ) ;
#6734=VECTOR ( 'NONE', #19810, 1000.000000000000000 ) ;
#6735=ORIENTED_EDGE ( 'NONE', *, *, #1825, .F. ) ;
#6746=ORIENTED_EDGE ( 'NONE', *, *, #17388, .F. ) ;
#6750=CIRCLE ( 'NONE', #38801, 37.49900000000000944 ) ;
#6752=EDGE_CURVE ( 'NONE', #19028, #19153, #48026, .T. ) ;
#6753=EDGE_CURVE ( 'NONE', #42541, #844, #44363, .T. ) ;
#6758=EDGE_LOOP ( 'NONE', ( #14043, #10490, #47477, #40623 ) ) ;
#6759=EDGE_CURVE ( 'NONE', #25280, #12928, #1270, .T. ) ;
#6761=ORIENTED_EDGE ( 'NONE', *, *, #40078, .T. ) ;
#6764=PLANE ( 'NONE',  #5053 ) ;
#6769=CARTESIAN_POINT ( 'NONE',  ( -10.00000000000000000, 0.000000000000000000, 0.000000000000000000 ) ) ;
#6771=VERTEX_POINT ( 'NONE', #14260 ) ;
#6800=DIRECTION ( 'NONE',  ( 0.000000000000000000, 0.000000000000000000, 1.000000000000000000 ) ) ;
#6808=AXIS2_PLACEMENT_3D ( 'NONE', #20276, #42811, #27896 ) ;
#6810=SURFACE_STYLE_FILL_AREA ( #40575 ) ;
#6815=EDGE_LOOP ( 'NONE', ( #15189, #36678 ) ) ;
#6821=EDGE_CURVE ( 'NONE', #12203, #1459, #2074, .T. ) ;
#6824=ORIENTED_EDGE ( 'NONE', *, *, #15473, .T. ) ;
#6826=VECTOR ( 'NONE', #9927, 1000.000000000000000 ) ;
#6828=CARTESIAN_POINT ( 'NONE',  ( 10.00000000000000000, -15.48615015657555816, -39.04073710021360455 ) ) ;
#6831=ORIENTED_EDGE ( 'NONE', *, *, #28959, .T. ) ;
#6837=ORIENTED_EDGE ( 'NONE', *, *, #46106, .F. ) ;
#6845=DIRECTION ( 'NONE',  ( -1.000000000000000000, -0.000000000000000000, -0.000000000000000000 ) ) ;
#6848=ORIENTED_EDGE ( 'NONE', *, *, #46487, .F. ) ;
#6851=CARTESIAN_POINT ( 'NONE',  ( -3.000000000000000000, 9.615535125379096826, -24.73947219025905042 ) ) ;
#6861=DIRECTION ( 'NONE',  ( -1.000000000000000000, -0.000000000000000000, -0.000000000000000000 ) ) ;
#6870=DIRECTION ( 'NONE',  ( 0.000000000000000000, -0.9945218953682745111, 0.1045284632676429237 ) ) ;
#6875=EDGE_CURVE ( 'NONE', #46585, #32891, #37498, .T. ) ;
#6878=VERTEX_POINT ( 'NONE', #41651 ) ;
#6879=FACE_OUTER_BOUND ( 'NONE', #17165, .T. ) ;
#6882=DIRECTION ( 'NONE',  ( 1.000000000000000000, -0.000000000000000000, -0.000000000000000000 ) ) ;
#6894=CARTESIAN_POINT ( 'NONE',  ( 10.00000000000000000, 0.000000000000000000, 0.000000000000000000 ) ) ;
#6896=CYLINDRICAL_SURFACE ( 'NONE', #42826, 37.49900000000000233 ) ;
#6898=ORIENTED_EDGE ( 'NONE', *, *, #25907, .F. ) ;
#6905=DIRECTION ( 'NONE',  ( 0.000000000000000000, -0.9510565162951506446, -0.3090169943749562775 ) ) ;
#6906=EDGE_LOOP ( 'NONE', ( #31444, #42845, #4249, #15924 ) ) ;
#6911=DIRECTION ( 'NONE',  ( -1.000000000000000000, 0.000000000000000000, 0.000000000000000000 ) ) ;
#6915=LINE ( 'NONE', #17434, #41098 ) ;
#6949=FACE_OUTER_BOUND ( 'NONE', #31585, .T. ) ;
#6956=ORIENTED_EDGE ( 'NONE', *, *, #31688, .F. ) ;
#6964=LINE ( 'NONE', #40503, #4971 ) ;
#6966=EDGE_CURVE ( 'NONE', #44214, #22321, #13243, .T. ) ;
#6970=ORIENTED_EDGE ( 'NONE', *, *, #48014, .F. ) ;
#6976=CARTESIAN_POINT ( 'NONE',  ( 0.000000000000000000, 17.80606268964540106, 33.00180498840052934 ) ) ;
#6978=FACE_OUTER_BOUND ( 'NONE', #25053, .T. ) ;
#6981=ORIENTED_EDGE ( 'NONE', *, *, #37282, .F. ) ;
#6988=EDGE_LOOP ( 'NONE', ( #6761, #5085, #36501, #43392 ) ) ;
#6989=DIRECTION ( 'NONE',  ( 1.000000000000000000, 0.000000000000000000, -0.000000000000000000 ) ) ;
#6990=ORIENTED_EDGE ( 'NONE', *, *, #9385, .T. ) ;
#6998=ORIENTED_EDGE ( 'NONE', *, *, #42342, .F. ) ;
#7006=DIRECTION ( 'NONE',  ( 0.000000000000000000, 0.4539904997395477482, -0.8910065241883673437 ) ) ;
#7027=CYLINDRICAL_SURFACE ( 'NONE', #20049, 16.00000000000000000 ) ;
#7030=DIRECTION ( 'NONE',  ( -1.000000000000000000, 0.000000000000000000, 0.000000000000000000 ) ) ;
#7035=SURFACE_SIDE_STYLE ('',( #6810 ) ) ;
#7045=EDGE_CURVE ( 'NONE', #17031, #45751, #39435, .T. ) ;
#7048=ORIENTED_EDGE ( 'NONE', *, *, #16774, .T. ) ;
#7052=DIRECTION ( 'NONE',  ( 0.000000000000000000, -0.9781476007338040235, -0.2079116908177671419 ) ) ;
#7056=ORIENTED_EDGE ( 'NONE', *, *, #46680, .F. ) ;
#7062=DIRECTION ( 'NONE',  ( 0.000000000000000000, 0.000000000000000000, 1.000000000000000000 ) ) ;
#7069=CARTESIAN_POINT ( 'NONE',  ( 0.000000000000000000, -18.13022148937263012, 15.02647892043544608 ) ) ;
#7088=FACE_OUTER_BOUND ( 'NONE', #44344, .T. ) ;
#7092=EDGE_LOOP ( 'NONE', ( #35154, #29854, #1146, #37376 ) ) ;
#7094=ORIENTED_EDGE ( 'NONE', *, *, #28534, .F. ) ;
#7098=CIRCLE ( 'NONE', #30548, 15.99999999999999645 ) ;
#7101=ORIENTED_EDGE ( 'NONE', *, *, #32614, .T. ) ;
#7104=EDGE_LOOP ( 'NONE', ( #3521, #24258, #10065, #1452 ) ) ;
#7106=VECTOR ( 'NONE', #926, 1000.000000000000000 ) ;
#7111=ADVANCED_FACE ( 'NONE', ( #21546 ), #44055, .T. ) ;
#7121=ORIENTED_EDGE ( 'NONE', *, *, #37222, .T. ) ;
#7122=CARTESIAN_POINT ( 'NONE',  ( 0.000000000000000000, -5.202137450156129717, -37.22597642581163768 ) ) ;
#7126=DIRECTION ( 'NONE',  ( 0.000000000000000000, 0.9510565162951503115, 0.3090169943749573878 ) ) ;
#7127=CARTESIAN_POINT ( 'NONE',  ( 0.000000000000000000, -21.40280677340345505, -36.13751322684441192 ) ) ;
#7134=VECTOR ( 'NONE', #10138, 1000.000000000000000 ) ;
#7136=VERTEX_POINT ( 'NONE', #25677 ) ;
#7160=ORIENTED_EDGE ( 'NONE', *, *, #38812, .T. ) ;
#7162=LINE ( 'NONE', #25998, #48007 ) ;
#7172=ADVANCED_FACE ( 'NONE', ( #25196 ), #28877, .T. ) ;
#7193=EDGE_CURVE ( 'NONE', #1357, #17758, #43581, .T. ) ;
#7196=CARTESIAN_POINT ( 'NONE',  ( -3.000000000000000000, -19.89357724624987256, -12.59942793731086041 ) ) ;
#7211=CARTESIAN_POINT ( 'NONE',  ( 4.999999999999999112, 36.13751322684449008, -21.40280677340332716 ) ) ;
#7219=LINE ( 'NONE', #22404, #15264 ) ;
#7225=ORIENTED_EDGE ( 'NONE', *, *, #36714, .T. ) ;
#7234=CARTESIAN_POINT ( 'NONE',  ( 0.000000000000000000, -22.67460108101783334, 6.353146135317912169 ) ) ;
#7239=AXIS2_PLACEMENT_3D ( 'NONE', #34947, #2152, #9007 ) ;
#7246=AXIS2_PLACEMENT_3D ( 'NONE', #5521, #31736, #32198 ) ;
#7247=ORIENTED_EDGE ( 'NONE', *, *, #19926, .T. ) ;
#7253=CARTESIAN_POINT ( 'NONE',  ( 10.00000000000000000, 0.000000000000000000, 0.000000000000000000 ) ) ;
#7261=EDGE_CURVE ( 'NONE', #10144, #1961, #3905, .T. ) ;
#7262=EDGE_LOOP ( 'NONE', ( #2811, #46865, #10780, #16393 ) ) ;
#7263=DIRECTION ( 'NONE',  ( 0.000000000000000000, -0.5000000000000039968, 0.8660254037844363761 ) ) ;
#7266=CIRCLE ( 'NONE', #39312, 37.49900000000000233 ) ;
#7268=CARTESIAN_POINT ( 'NONE',  ( 10.00000000000000000, -6.555932627142676772, 37.01155633439056203 ) ) ;
#7280=CIRCLE ( 'NONE', #40901, 16.00000000000000000 ) ;
#7283=ORIENTED_EDGE ( 'NONE', *, *, #34702, .T. ) ;
#7286=CARTESIAN_POINT ( 'NONE',  ( 10.00000000000000000, 27.13269053701132094, -25.88420570971372570 ) ) ;
#7296=LINE ( 'NONE', #186, #33691 ) ;
#7301=PLANE ( 'NONE',  #42378 ) ;
#7303=VECTOR ( 'NONE', #1664, 1000.000000000000000 ) ;
#7329=CARTESIAN_POINT ( 'NONE',  ( -3.000000000000000000, 24.81905959214275370, -9.408202855044498492 ) ) ;
#7332=ADVANCED_FACE ( 'NONE', ( #29846 ), #22989, .T. ) ;
#7334=DIRECTION ( 'NONE',  ( 0.000000000000000000, 0.000000000000000000, 1.000000000000000000 ) ) ;
#7346=CARTESIAN_POINT ( 'NONE',  ( 4.999999999999999112, -40.98264845739755202, 9.188173127307159405 ) ) ;
#7354=DIRECTION ( 'NONE',  ( -1.000000000000000000, 0.000000000000000000, 0.000000000000000000 ) ) ;
#7374=CARTESIAN_POINT ( 'NONE',  ( 10.00000000000000000, 22.74946021919133088, 29.81001611431016229 ) ) ;
#7379=ORIENTED_EDGE ( 'NONE', *, *, #3035, .F. ) ;
#7380=DIRECTION ( 'NONE',  ( 0.000000000000000000, 0.000000000000000000, 1.000000000000000000 ) ) ;
#7389=DIRECTION ( 'NONE',  ( 0.000000000000000000, -0.9510565162951544194, 0.3090169943749450088 ) ) ;
#7396=ORIENTED_EDGE ( 'NONE', *, *, #48049, .T. ) ;
#7413=ORIENTED_EDGE ( 'NONE', *, *, #38182, .F. ) ;
#7428=EDGE_CURVE ( 'NONE', #36706, #37915, #8253, .T. ) ;
#7430=AXIS2_PLACEMENT_3D ( 'NONE', #19072, #41129, #22515 ) ;
#7432=CARTESIAN_POINT ( 'NONE',  ( 10.00000000000000000, 0.000000000000000000, 0.000000000000000000 ) ) ;
#7433=CYLINDRICAL_SURFACE ( 'NONE', #47295, 42.00000000000000000 ) ;
#7437=VERTEX_POINT ( 'NONE', #27397 ) ;
#7438=AXIS2_PLACEMENT_3D ( 'NONE', #44948, #40789, #635 ) ;
#7443=ORIENTED_EDGE ( 'NONE', *, *, #46869, .T. ) ;
#7444=CARTESIAN_POINT ( 'NONE',  ( 10.00000000000000000, 33.00180498840046539, 17.80606268964551120 ) ) ;
#7449=VECTOR ( 'NONE', #9803, 1000.000000000000000 ) ;
#7455=CARTESIAN_POINT ( 'NONE',  ( 0.000000000000000000, 10.96151621346487914, 35.95386929396260456 ) ) ;
#7458=DIRECTION ( 'NONE',  ( 1.000000000000000000, 0.000000000000000000, -0.000000000000000000 ) ) ;
#7459=DIRECTION ( 'NONE',  ( 0.000000000000000000, 0.000000000000000000, 1.000000000000000000 ) ) ;
#7466=ADVANCED_FACE ( 'NONE', ( #5606 ), #35454, .T. ) ;
#7472=DIRECTION ( 'NONE',  ( 0.000000000000000000, -0.8910065241883721177, 0.4539904997395382003 ) ) ;
#7473=DIRECTION ( 'NONE',  ( 1.000000000000000000, -0.000000000000000000, -0.000000000000000000 ) ) ;
#7482=ORIENTED_EDGE ( 'NONE', *, *, #22050, .T. ) ;
#7485=CIRCLE ( 'NONE', #23911, 42.00000000000000000 ) ;
#7492=ORIENTED_EDGE ( 'NONE', *, *, #25150, .F. ) ;
#7498=EDGE_LOOP ( 'NONE', ( #46385, #33662, #35742, #35879 ) ) ;
#7503=VERTEX_POINT ( 'NONE', #2173 ) ;
#7508=AXIS2_PLACEMENT_3D ( 'NONE', #19415, #27762, #34340 ) ;
#7509=CYLINDRICAL_SURFACE ( 'NONE', #33471, 42.00000000000000000 ) ;
#7513=DIRECTION ( 'NONE',  ( -0.000000000000000000, -0.9135454576426059736, 0.4067366430757887730 ) ) ;
#7515=CARTESIAN_POINT ( 'NONE',  ( 0.000000000000000000, 40.68715046381927891, 10.41901085202092858 ) ) ;
#7521=DIRECTION ( 'NONE',  ( -1.000000000000000000, 0.000000000000000000, -0.000000000000000000 ) ) ;
#7529=EDGE_CURVE ( 'NONE', #41033, #30788, #2786, .T. ) ;
#7530=DIRECTION ( 'NONE',  ( 0.000000000000000000, 0.000000000000000000, -1.000000000000000000 ) ) ;
#7534=CARTESIAN_POINT ( 'NONE',  ( 0.000000000000000000, 0.000000000000000000, 0.000000000000000000 ) ) ;
#7554=CIRCLE ( 'NONE', #27911, 16.00000000000000000 ) ;
#7565=ORIENTED_EDGE ( 'NONE', *, *, #12999, .T. ) ;
#7572=CARTESIAN_POINT ( 'NONE',  ( 10.00000000000000000, 0.000000000000000000, 0.000000000000000000 ) ) ;
#7574=DIRECTION ( 'NONE',  ( 0.000000000000000000, -0.9876883405951361050, -0.1564344650402419989 ) ) ;
#7575=CARTESIAN_POINT ( 'NONE',  ( -10.00000000000000000, 0.000000000000000000, 0.000000000000000000 ) ) ;
#7586=DIRECTION ( 'NONE',  ( 1.000000000000000000, -0.000000000000000000, -0.000000000000000000 ) ) ;
#7590=ORIENTED_EDGE ( 'NONE', *, *, #29243, .F. ) ;
#7591=CIRCLE ( 'NONE', #20908, 16.00000000000000000 ) ;
#7595=CARTESIAN_POINT ( 'NONE',  ( 5.000000000000000000, 41.91543099594818500, -2.663952781846291362 ) ) ;
#7597=ORIENTED_EDGE ( 'NONE', *, *, #43605, .F. ) ;
#7600=ORIENTED_EDGE ( 'NONE', *, *, #1779, .T. ) ;
#7602=ORIENTED_EDGE ( 'NONE', *, *, #5262, .T. ) ;
#7605=CARTESIAN_POINT ( 'NONE',  ( 4.999999999999999112, 41.81611651403861885, 3.925862922256313503 ) ) ;
#7612=ORIENTED_EDGE ( 'NONE', *, *, #7428, .T. ) ;
#7617=CARTESIAN_POINT ( 'NONE',  ( 10.00000000000000000, 0.000000000000000000, 0.000000000000000000 ) ) ;
#7630=CARTESIAN_POINT ( 'NONE',  ( 10.00000000000000000, 33.00180498840072829, -17.80606268964504935 ) ) ;
#7641=CARTESIAN_POINT ( 'NONE',  ( 0.000000000000000000, 0.000000000000000000, 0.000000000000000000 ) ) ;
#7645=FACE_OUTER_BOUND ( 'NONE', #17780, .T. ) ;
#7658=CARTESIAN_POINT ( 'NONE',  ( -3.000000000000000000, -19.89357724625003598, 12.59942793731059574 ) ) ;
#7659=ORIENTED_EDGE ( 'NONE', *, *, #9546, .F. ) ;
#7667=EDGE_CURVE ( 'NONE', #4717, #16717, #28595, .T. ) ;
#7674=CARTESIAN_POINT ( 'NONE',  ( 0.000000000000000000, -33.00180498840060039, 17.80606268964528027 ) ) ;
#7678=VERTEX_POINT ( 'NONE', #5277 ) ;
#7685=DIRECTION ( 'NONE',  ( 0.000000000000000000, 0.000000000000000000, 1.000000000000000000 ) ) ;
#7694=FACE_OUTER_BOUND ( 'NONE', #20717, .T. ) ;
#7695=CARTESIAN_POINT ( 'NONE',  ( 0.000000000000000000, 36.88895765772633695, 6.736453364083687667 ) ) ;
#7700=LINE ( 'NONE', #1333, #25368 ) ;
#7701=DIRECTION ( 'NONE',  ( -1.000000000000000000, 0.000000000000000000, 0.000000000000000000 ) ) ;
#7711=LINE ( 'NONE', #30245, #3895 ) ;
#7712=ORIENTED_EDGE ( 'NONE', *, *, #24277, .F. ) ;
#7715=VECTOR ( 'NONE', #35988, 1000.000000000000000 ) ;
#7717=PLANE ( 'NONE',  #45716 ) ;
#7723=DIRECTION ( 'NONE',  ( 0.000000000000000000, 0.000000000000000000, -1.000000000000000000 ) ) ;
#7728=FACE_OUTER_BOUND ( 'NONE', #27967, .T. ) ;
#7729=DIRECTION ( 'NONE',  ( -1.000000000000000000, -0.000000000000000000, 0.000000000000000000 ) ) ;
#7734=DIRECTION ( 'NONE',  ( 0.000000000000000000, 0.000000000000000000, 1.000000000000000000 ) ) ;
#7735=VERTEX_POINT ( 'NONE', #36796 ) ;
#7737=AXIS2_PLACEMENT_3D ( 'NONE', #24446, #5865, #20783 ) ;
#7739=DIRECTION ( 'NONE',  ( -1.000000000000000000, -0.000000000000000000, 0.000000000000000000 ) ) ;
#7741=LINE ( 'NONE', #41521, #11057 ) ;
#7745=EDGE_CURVE ( 'NONE', #22843, #24574, #12977, .T. ) ;
#7751=VERTEX_POINT ( 'NONE', #35842 ) ;
#7756=DIRECTION ( 'NONE',  ( 1.000000000000000000, 0.000000000000000000, -0.000000000000000000 ) ) ;
#7761=LINE ( 'NONE', #32734, #39403 ) ;
#7763=CARTESIAN_POINT ( 'NONE',  ( 10.00000000000000000, -16.45098606841149902, 33.79645857604508308 ) ) ;
#7764=ORIENTED_EDGE ( 'NONE', *, *, #21484, .F. ) ;
#7774=CARTESIAN_POINT ( 'NONE',  ( -3.000000000000000000, -19.89357724624987256, -12.59942793731086041 ) ) ;
#7778=ADVANCED_FACE ( 'NONE', ( #17230 ), #32649, .F. ) ;
#7781=CARTESIAN_POINT ( 'NONE',  ( 0.000000000000000000, -30.80686688397025108, 21.53537804866070715 ) ) ;
#7789=CARTESIAN_POINT ( 'NONE',  ( 0.000000000000000000, -0.6853352020793173072, 37.58145647212453611 ) ) ;
#7794=CYLINDRICAL_SURFACE ( 'NONE', #2419, 16.00000000000000000 ) ;
#7798=VECTOR ( 'NONE', #33602, 1000.000000000000000 ) ;
#7800=EDGE_CURVE ( 'NONE', #14425, #8228, #16339, .T. ) ;
#7802=VERTEX_POINT ( 'NONE', #25296 ) ;
#7803=FACE_OUTER_BOUND ( 'NONE', #32080, .T. ) ;
#7804=AXIS2_PLACEMENT_3D ( 'NONE', #22159, #18236, #614 ) ;
#7805=CARTESIAN_POINT ( 'NONE',  ( 10.00000000000000000, 0.000000000000000000, 0.000000000000000000 ) ) ;
#7808=DIRECTION ( 'NONE',  ( 0.000000000000000000, -0.6691306063588569053, -0.7431448254773954654 ) ) ;
#7810=CIRCLE ( 'NONE', #22762, 42.00000000000000000 ) ;
#7811=CARTESIAN_POINT ( 'NONE',  ( 10.00000000000000000, 27.75498641678742473, 31.52238457039609898 ) ) ;
#7812=ADVANCED_FACE ( 'NONE', ( #6949 ), #28748, .T. ) ;
#7818=CARTESIAN_POINT ( 'NONE',  ( -3.000000000000000000, -11.95096189432345390, 23.69967320028757385 ) ) ;
#7829=FACE_OUTER_BOUND ( 'NONE', #25649, .T. ) ;
#7833=ADVANCED_FACE ( 'NONE', ( #47357 ), #33134, .F. ) ;
#7836=ORIENTED_EDGE ( 'NONE', *, *, #24553, .F. ) ;
#7840=CARTESIAN_POINT ( 'NONE',  ( 10.00000000000000000, 0.6853352020790449695, 37.58145647212454321 ) ) ;
#7846=VERTEX_POINT ( 'NONE', #11831 ) ;
#7848=CARTESIAN_POINT ( 'NONE',  ( 10.00000000000000000, 22.48208911017500355, 35.47612816024531668 ) ) ;
#7857=ORIENTED_EDGE ( 'NONE', *, *, #24978, .F. ) ;
#7860=DIRECTION ( 'NONE',  ( -1.000000000000000000, -0.000000000000000000, 0.000000000000000000 ) ) ;
#7869=FACE_OUTER_BOUND ( 'NONE', #41514, .T. ) ;
#7873=AXIS2_PLACEMENT_3D ( 'NONE', #45360, #18922, #33861 ) ;
#7874=CIRCLE ( 'NONE', #14136, 16.00000000000000000 ) ;
#7875=FACE_OUTER_BOUND ( 'NONE', #6758, .T. ) ;
#7878=DIRECTION ( 'NONE',  ( 0.000000000000000000, 0.9510565162951503115, 0.3090169943749573878 ) ) ;
#7881=CIRCLE ( 'NONE', #15667, 16.00000000000000355 ) ;
#7888=DIRECTION ( 'NONE',  ( -1.000000000000000000, 0.000000000000000000, 0.000000000000000000 ) ) ;
#7892=VERTEX_POINT ( 'NONE', #30431 ) ;
#7900=ORIENTED_EDGE ( 'NONE', *, *, #43224, .T. ) ;
#7907=AXIS2_PLACEMENT_3D ( 'NONE', #34520, #45811, #42129 ) ;
#7909=DIRECTION ( 'NONE',  ( -1.000000000000000000, 0.000000000000000000, 0.000000000000000000 ) ) ;
#7913=ORIENTED_EDGE ( 'NONE', *, *, #11871, .T. ) ;
#7927=CARTESIAN_POINT ( 'NONE',  ( 10.00000000000000000, -26.08949754953044220, 27.05870788708222818 ) ) ;
#7928=CARTESIAN_POINT ( 'NONE',  ( -3.000000000000000000, -13.04903810567675038, 19.60159698893425428 ) ) ;
#7934=CARTESIAN_POINT ( 'NONE',  ( 10.00000000000000000, 25.88420570971400991, 27.13269053701105449 ) ) ;
#7940=ADVANCED_FACE ( 'NONE', ( #14782 ), #320, .T. ) ;
#7943=ORIENTED_EDGE ( 'NONE', *, *, #770, .T. ) ;
#7944=CIRCLE ( 'NONE', #4819, 16.00000000000000000 ) ;
#7945=DIRECTION ( 'NONE',  ( -1.000000000000000000, 0.000000000000000000, -0.000000000000000000 ) ) ;
#7955=ORIENTED_EDGE ( 'NONE', *, *, #31884, .F. ) ;
#7957=LINE ( 'NONE', #15800, #8438 ) ;
#7958=DIRECTION ( 'NONE',  ( 0.000000000000000000, 0.8660254037844432595, -0.4999999999999920064 ) ) ;
#7964=VERTEX_POINT ( 'NONE', #41686 ) ;
#7966=DIRECTION ( 'NONE',  ( -1.000000000000000000, -0.000000000000000000, 0.000000000000000000 ) ) ;
#7970=CARTESIAN_POINT ( 'NONE',  ( 10.00000000000000000, 35.38097989696528600, -12.42422080174602605 ) ) ;
#7976=DIRECTION ( 'NONE',  ( 0.000000000000000000, -0.7431448254773856954, -0.6691306063588676745 ) ) ;
#7979=ORIENTED_EDGE ( 'NONE', *, *, #30187, .T. ) ;
#7982=VECTOR ( 'NONE', #33256, 1000.000000000000000 ) ;
#7985=CARTESIAN_POINT ( 'NONE',  ( 4.999999999999999112, -16.65560815589383381, -38.55633173627028754 ) ) ;
#7987=CARTESIAN_POINT ( 'NONE',  ( -3.000000000000000000, 23.59884966291538078, -12.14883922797231541 ) ) ;
#7991=CARTESIAN_POINT ( 'NONE',  ( 0.000000000000000000, 35.47612816024523852, 22.48208911017513145 ) ) ;
#7993=ADVANCED_FACE ( 'NONE', ( #44397 ), #25774, .T. ) ;
#8019=CARTESIAN_POINT ( 'NONE',  ( -3.000000000000000000, -22.67460108101774807, -6.353146135318215038 ) ) ;
#8021=CARTESIAN_POINT ( 'NONE',  ( 0.000000000000000000, 40.98264845739763018, -9.188173127306864529 ) ) ;
#8024=DIRECTION ( 'NONE',  ( 0.000000000000000000, 0.9781476007338044676, 0.2079116908177653100 ) ) ;
#8025=VECTOR ( 'NONE', #32081, 1000.000000000000000 ) ;
#8026=CARTESIAN_POINT ( 'NONE',  ( 10.00000000000000000, 35.92658777277525672, -10.74501242461245809 ) ) ;
#8028=CARTESIAN_POINT ( 'NONE',  ( 0.000000000000000000, 0.000000000000000000, 0.000000000000000000 ) ) ;
#8030=ORIENTED_EDGE ( 'NONE', *, *, #3870, .T. ) ;
#8038=ORIENTED_EDGE ( 'NONE', *, *, #17529, .F. ) ;
#8042=AXIS2_PLACEMENT_3D ( 'NONE', #7789, #18796, #19510 ) ;
#8049=AXIS2_PLACEMENT_3D ( 'NONE', #43634, #5238, #13786 ) ;
#8054=FACE_OUTER_BOUND ( 'NONE', #18067, .T. ) ;
#8059=ORIENTED_EDGE ( 'NONE', *, *, #11573, .T. ) ;
#8080=DIRECTION ( 'NONE',  ( 0.000000000000000000, 0.000000000000000000, 1.000000000000000000 ) ) ;
#8084=ORIENTED_EDGE ( 'NONE', *, *, #17122, .F. ) ;
#8089=LINE ( 'NONE', #46030, #9811 ) ;
#8095=ADVANCED_FACE ( 'NONE', ( #22708 ), #30066, .F. ) ;
#8116=VECTOR ( 'NONE', #30218, 1000.000000000000000 ) ;
#8119=EDGE_CURVE ( 'NONE', #4226, #10700, #24071, .T. ) ;
#8131=ADVANCED_FACE ( 'NONE', ( #46925 ), #39597, .T. ) ;
#8141=ORIENTED_EDGE ( 'NONE', *, *, #31357, .T. ) ;
#8149=VERTEX_POINT ( 'NONE', #9232 ) ;
#8157=DIRECTION ( 'NONE',  ( 0.000000000000000000, 0.5877852522924744694, -0.8090169943749465631 ) ) ;
#8159=AXIS2_PLACEMENT_3D ( 'NONE', #25932, #3666, #40871 ) ;
#8160=ORIENTED_EDGE ( 'NONE', *, *, #23403, .F. ) ;
#8163=ORIENTED_EDGE ( 'NONE', *, *, #10017, .F. ) ;
#8166=AXIS2_PLACEMENT_3D ( 'NONE', #2181, #39387, #34980 ) ;
#8183=EDGE_CURVE ( 'NONE', #6187, #38183, #13151, .T. ) ;
#8193=DIRECTION ( 'NONE',  ( -1.000000000000000000, 0.000000000000000000, -0.000000000000000000 ) ) ;
#8195=CIRCLE ( 'NONE', #32416, 42.00000000000000000 ) ;
#8197=AXIS2_PLACEMENT_3D ( 'NONE', #27330, #37856, #16077 ) ;
#8200=ORIENTED_EDGE ( 'NONE', *, *, #41255, .F. ) ;
#8205=FACE_OUTER_BOUND ( 'NONE', #49, .T. ) ;
#8207=CARTESIAN_POINT ( 'NONE',  ( 10.00000000000000000, 16.45098606841173705, -33.79645857604496229 ) ) ;
#8228=VERTEX_POINT ( 'NONE', #20246 ) ;
#8233=CARTESIAN_POINT ( 'NONE',  ( 10.00000000000000000, -17.67226234102849958, 33.17418723428301774 ) ) ;
#8236=ORIENTED_EDGE ( 'NONE', *, *, #33873, .T. ) ;
#8245=EDGE_CURVE ( 'NONE', #43819, #35770, #15502, .T. ) ;
#8248=ORIENTED_EDGE ( 'NONE', *, *, #19161, .T. ) ;
#8253=CIRCLE ( 'NONE', #41839, 42.00000000000000000 ) ;
#8255=ORIENTED_EDGE ( 'NONE', *, *, #40959, .F. ) ;
#8257=DIRECTION ( 'NONE',  ( -1.000000000000000000, 0.000000000000000000, 0.000000000000000000 ) ) ;
#8270=AXIS2_PLACEMENT_3D ( 'NONE', #15032, #41226, #17958 ) ;
#8271=DIRECTION ( 'NONE',  ( 0.000000000000000000, 0.000000000000000000, 1.000000000000000000 ) ) ;
#8275=EDGE_CURVE ( 'NONE', #24885, #19183, #12431, .T. ) ;
#8276=ORIENTED_EDGE ( 'NONE', *, *, #38456, .T. ) ;
#8280=ORIENTED_EDGE ( 'NONE', *, *, #1764, .F. ) ;
#8296=DIRECTION ( 'NONE',  ( 0.000000000000000000, 0.9781476007338069101, -0.2079116908177532086 ) ) ;
#8297=LINE ( 'NONE', #34229, #36296 ) ;
#8306=DIRECTION ( 'NONE',  ( 0.000000000000000000, 0.000000000000000000, 1.000000000000000000 ) ) ;
#8322=CARTESIAN_POINT ( 'NONE',  ( 0.000000000000000000, -13.04903810567647682, -19.60159698893442481 ) ) ;
#8331=ORIENTED_EDGE ( 'NONE', *, *, #2303, .F. ) ;
#8346=ORIENTED_EDGE ( 'NONE', *, *, #22707, .T. ) ;
#8352=DIRECTION ( 'NONE',  ( 0.000000000000000000, -0.9135454576426005335, -0.4067366430758010409 ) ) ;
#8356=EDGE_CURVE ( 'NONE', #23469, #38800, #16278, .T. ) ;
#8362=DIRECTION ( 'NONE',  ( 1.000000000000000000, -0.000000000000000000, 0.000000000000000000 ) ) ;
#8387=DIRECTION ( 'NONE',  ( 0.000000000000000000, 0.000000000000000000, 1.000000000000000000 ) ) ;
#8400=VERTEX_POINT ( 'NONE', #2848 ) ;
#8405=DIRECTION ( 'NONE',  ( 0.000000000000000000, 0.000000000000000000, 1.000000000000000000 ) ) ;
#8418=EDGE_CURVE ( 'NONE', #3180, #44307, #7957, .T. ) ;
#8420=DIRECTION ( 'NONE',  ( -1.000000000000000000, 0.000000000000000000, 0.000000000000000000 ) ) ;
#8421=CYLINDRICAL_SURFACE ( 'NONE', #37698, 42.00000000000000000 ) ;
#8427=DIRECTION ( 'NONE',  ( -1.000000000000000000, 0.000000000000000000, -0.000000000000000000 ) ) ;
#8428=ORIENTED_EDGE ( 'NONE', *, *, #24594, .F. ) ;
#8431=EDGE_LOOP ( 'NONE', ( #30089, #4978, #37426, #116 ) ) ;
#8433=VECTOR ( 'NONE', #3095, 1000.000000000000000 ) ;
#8438=VECTOR ( 'NONE', #30259, 1000.000000000000227 ) ;
#8448=ORIENTED_EDGE ( 'NONE', *, *, #31071, .F. ) ;
#8466=VERTEX_POINT ( 'NONE', #11889 ) ;
#8474=AXIS2_PLACEMENT_3D ( 'NONE', #8510, #5100, #34694 ) ;
#8484=ORIENTED_EDGE ( 'NONE', *, *, #4372, .F. ) ;
#8498=ORIENTED_EDGE ( 'NONE', *, *, #38131, .T. ) ;
#8506=ORIENTED_EDGE ( 'NONE', *, *, #31357, .F. ) ;
#8510=CARTESIAN_POINT ( 'NONE',  ( 10.00000000000000000, 10.96151621346487914, 35.95386929396260456 ) ) ;
#8541=ORIENTED_EDGE ( 'NONE', *, *, #11813, .F. ) ;
#8543=FACE_OUTER_BOUND ( 'NONE', #3169, .T. ) ;
#8545=ADVANCED_FACE ( 'NONE', ( #7728 ), #4061, .T. ) ;
#8546=VERTEX_POINT ( 'NONE', #16049 ) ;
#8550=ORIENTED_EDGE ( 'NONE', *, *, #33803, .F. ) ;
#8565=ORIENTED_EDGE ( 'NONE', *, *, #5310, .T. ) ;
#8572=ORIENTED_EDGE ( 'NONE', *, *, #30080, .F. ) ;
#8574=ORIENTED_EDGE ( 'NONE', *, *, #35298, .F. ) ;
#8575=CIRCLE ( 'NONE', #10964, 37.49900000000000233 ) ;
#8581=CARTESIAN_POINT ( 'NONE',  ( 5.000000000000000000, 32.34446384430010113, -26.79245525562679831 ) ) ;
#8584=FACE_OUTER_BOUND ( 'NONE', #46441, .T. ) ;
#8586=DIRECTION ( 'NONE',  ( -1.000000000000000000, 0.000000000000000000, 0.000000000000000000 ) ) ;
#8594=ORIENTED_EDGE ( 'NONE', *, *, #43947, .F. ) ;
#8621=CARTESIAN_POINT ( 'NONE',  ( 10.00000000000000000, 38.55633173627010990, 16.65560815589424593 ) ) ;
#8622=EDGE_CURVE ( 'NONE', #13463, #15338, #23376, .T. ) ;
#8625=EDGE_LOOP ( 'NONE', ( #17114, #16348, #18367, #8816 ) ) ;
#8626=AXIS2_PLACEMENT_3D ( 'NONE', #30660, #15980, #8387 ) ;
#8628=ORIENTED_EDGE ( 'NONE', *, *, #2405, .F. ) ;
#8631=AXIS2_PLACEMENT_3D ( 'NONE', #17240, #32660, #25309 ) ;
#8634=DIRECTION ( 'NONE',  ( -1.000000000000000000, -0.000000000000000000, 0.000000000000000000 ) ) ;
#8636=CARTESIAN_POINT ( 'NONE',  ( 10.00000000000000000, 0.000000000000000000, 0.000000000000000000 ) ) ;
#8639=PLANE ( 'NONE',  #30739 ) ;
#8646=LINE ( 'NONE', #1804, #10732 ) ;
#8659=AXIS2_PLACEMENT_3D ( 'NONE', #7455, #37312, #3774 ) ;
#8660=AXIS2_PLACEMENT_3D ( 'NONE', #9233, #43015, #35414 ) ;
#8665=ORIENTED_EDGE ( 'NONE', *, *, #46582, .T. ) ;
#8672=DIRECTION ( 'NONE',  ( -0.000000000000000000, -1.156482317317870936E-15, -1.000000000000000000 ) ) ;
#8683=ORIENTED_EDGE ( 'NONE', *, *, #1619, .T. ) ;
#8687=CARTESIAN_POINT ( 'NONE',  ( 10.00000000000000000, -16.45098606841102651, -33.79645857604531045 ) ) ;
#8696=CIRCLE ( 'NONE', #34477, 42.00000000000000000 ) ;
#8700=ORIENTED_EDGE ( 'NONE', *, *, #16027, .F. ) ;
#8709=CIRCLE ( 'NONE', #46250, 37.49900000000000233 ) ;
#8717=AXIS2_PLACEMENT_3D ( 'NONE', #44566, #21323, #25477 ) ;
#8724=ORIENTED_EDGE ( 'NONE', *, *, #9608, .T. ) ;
#8732=CARTESIAN_POINT ( 'NONE',  ( -3.000000000000000000, 20.85821328998741109, 10.92862929874522315 ) ) ;
#8733=CIRCLE ( 'NONE', #47043, 16.00000000000000000 ) ;
#8738=AXIS2_PLACEMENT_3D ( 'NONE', #16542, #39789, #20441 ) ;
#8739=CARTESIAN_POINT ( 'NONE',  ( 4.999999999999999112, -41.91543099594819921, 2.663952781846001816 ) ) ;
#8741=ORIENTED_EDGE ( 'NONE', *, *, #25087, .F. ) ;
#8769=CARTESIAN_POINT ( 'NONE',  ( 10.00000000000000000, 30.80686688397010542, 21.53537804866092387 ) ) ;
#8773=EDGE_CURVE ( 'NONE', #32853, #24228, #36561, .T. ) ;
#8774=CIRCLE ( 'NONE', #36129, 16.00000000000000355 ) ;
#8785=DIRECTION ( 'NONE',  ( -1.000000000000000000, 0.000000000000000000, -0.000000000000000000 ) ) ;
#8787=CARTESIAN_POINT ( 'NONE',  ( 0.000000000000000000, -23.29833615347104825, -3.418703333116803744 ) ) ;
#8792=VERTEX_POINT ( 'NONE', #43909 ) ;
#8802=AXIS2_PLACEMENT_3D ( 'NONE', #8028, #15621, #11485 ) ;
#8807=ORIENTED_EDGE ( 'NONE', *, *, #7261, .T. ) ;
#8810=CYLINDRICAL_SURFACE ( 'NONE', #40696, 37.49900000000000233 ) ;
#8816=ORIENTED_EDGE ( 'NONE', *, *, #27008, .T. ) ;
#8817=DIRECTION ( 'NONE',  ( -1.000000000000000000, -0.000000000000000000, 0.000000000000000000 ) ) ;
#8818=CARTESIAN_POINT ( 'NONE',  ( -3.000000000000000000, -10.45096189432344147, 21.10159698893426494 ) ) ;
#8819=AXIS2_PLACEMENT_3D ( 'NONE', #19921, #31937, #13080 ) ;
#8828=ORIENTED_EDGE ( 'NONE', *, *, #5434, .T. ) ;
#8836=ADVANCED_FACE ( 'NONE', ( #32648 ), #28974, .F. ) ;
#8838=ADVANCED_FACE ( 'NONE', ( #18187 ), #25295, .F. ) ;
#8842=EDGE_LOOP ( 'NONE', ( #5259, #18747, #10996, #32828 ) ) ;
#8850=ADVANCED_FACE ( 'NONE', ( #9647 ), #6007, .T. ) ;
#8855=CIRCLE ( 'NONE', #29195, 42.00000000000000000 ) ;
#8856=AXIS2_PLACEMENT_3D ( 'NONE', #2771, #17704, #21849 ) ;
#8869=DIRECTION ( 'NONE',  ( 1.000000000000000000, -0.000000000000000000, -0.000000000000000000 ) ) ;
#8870=DIRECTION ( 'NONE',  ( -1.000000000000000000, 0.000000000000000000, 0.000000000000000000 ) ) ;
#8873=AXIS2_PLACEMENT_3D ( 'NONE', #15649, #15420, #19534 ) ;
#8876=ORIENTED_EDGE ( 'NONE', *, *, #35276, .F. ) ;
#8888=VERTEX_POINT ( 'NONE', #33381 ) ;
#8893=DIRECTION ( 'NONE',  ( 0.000000000000000000, 0.000000000000000000, 1.000000000000000000 ) ) ;
#8895=AXIS2_PLACEMENT_3D ( 'NONE', #39459, #5933, #24986 ) ;
#8896=DIRECTION ( 'NONE',  ( 0.000000000000000000, 0.000000000000000000, 1.000000000000000000 ) ) ;
#8909=DIRECTION ( 'NONE',  ( -1.000000000000000000, 0.000000000000000000, -0.000000000000000000 ) ) ;
#8910=CYLINDRICAL_SURFACE ( 'NONE', #33835, 16.00000000000000000 ) ;
#8916=AXIS2_PLACEMENT_3D ( 'NONE', #31499, #6267, #24142 ) ;
#8919=ORIENTED_EDGE ( 'NONE', *, *, #23422, .F. ) ;
#8925=CARTESIAN_POINT ( 'NONE',  ( 0.000000000000000000, 35.47612816024556537, -22.48208911017461631 ) ) ;
#8926=EDGE_LOOP ( 'NONE', ( #19517, #2084, #42197, #43588 ) ) ;
#8943=CARTESIAN_POINT ( 'NONE',  ( 5.000000000000000000, 38.55633173627010279, 16.65560815589424593 ) ) ;
#8946=CARTESIAN_POINT ( 'NONE',  ( -3.000000000000000000, -11.95096189432345390, 23.69967320028757385 ) ) ;
#8952=DIRECTION ( 'NONE',  ( 0.000000000000000000, 1.000000000000000000, 3.491481338843133750E-15 ) ) ;
#8956=ORIENTED_EDGE ( 'NONE', *, *, #44310, .T. ) ;
#8957=ORIENTED_EDGE ( 'NONE', *, *, #7193, .F. ) ;
#8968=CYLINDRICAL_SURFACE ( 'NONE', #24780, 16.00000000000000355 ) ;
#8977=CIRCLE ( 'NONE', #37908, 16.00000000000000000 ) ;
#8999=DIRECTION ( 'NONE',  ( 0.000000000000000000, -0.9876883405951393247, 0.1564344650402204329 ) ) ;
#9000=ORIENTED_EDGE ( 'NONE', *, *, #41955, .T. ) ;
#9007=DIRECTION ( 'NONE',  ( 0.000000000000000000, 0.000000000000000000, 1.000000000000000000 ) ) ;
#9008=CARTESIAN_POINT ( 'NONE',  ( 10.00000000000000000, -33.17418723428294669, -17.67226234102862747 ) ) ;
#9012=ORIENTED_EDGE ( 'NONE', *, *, #47960, .F. ) ;
#9031=LINE ( 'NONE', #46729, #33296 ) ;
#9033=EDGE_CURVE ( 'NONE', #38628, #44271, #1540, .T. ) ;
#9043=CARTESIAN_POINT ( 'NONE',  ( 10.00000000000000000, 27.05870788708231700, 26.08949754953034272 ) ) ;
#9050=ORIENTED_EDGE ( 'NONE', *, *, #42011, .T. ) ;
#9055=EDGE_CURVE ( 'NONE', #42613, #7751, #35302, .T. ) ;
#9056=CIRCLE ( 'NONE', #34842, 16.00000000000000000 ) ;
#9080=CARTESIAN_POINT ( 'NONE',  ( 10.00000000000000000, 0.8828120875905820508, -37.48860685352290290 ) ) ;
#9082=FACE_OUTER_BOUND ( 'NONE', #42956, .T. ) ;
#9083=CARTESIAN_POINT ( 'NONE',  ( 0.000000000000000000, -39.04073710021356192, 15.48615015657568073 ) ) ;
#9086=CYLINDRICAL_SURFACE ( 'NONE', #37607, 37.49900000000000233 ) ;
#9088=CARTESIAN_POINT ( 'NONE',  ( -10.00000000000000000, 0.000000000000000000, 0.000000000000000000 ) ) ;
#9097=CIRCLE ( 'NONE', #34865, 16.00000000000000000 ) ;
#9099=ORIENTED_EDGE ( 'NONE', *, *, #19542, .T. ) ;
#9101=DIRECTION ( 'NONE',  ( 0.000000000000000000, 0.000000000000000000, 1.000000000000000000 ) ) ;
#9109=ORIENTED_EDGE ( 'NONE', *, *, #21977, .T. ) ;
#9113=VECTOR ( 'NONE', #20270, 1000.000000000000000 ) ;
#9115=ORIENTED_EDGE ( 'NONE', *, *, #6246, .F. ) ;
#9126=AXIS2_PLACEMENT_3D ( 'NONE', #12465, #23968, #5361 ) ;
#9131=ORIENTED_EDGE ( 'NONE', *, *, #29081, .F. ) ;
#9132=ADVANCED_FACE ( 'NONE', ( #34821 ), #16236, .T. ) ;
#9136=LINE ( 'NONE', #16959, #23458 ) ;
#9143=DIRECTION ( 'NONE',  ( -1.000000000000000000, 0.000000000000000000, -0.000000000000000000 ) ) ;
#9148=CARTESIAN_POINT ( 'NONE',  ( 10.00000000000000000, -25.88420570971419821, 27.13269053701087330 ) ) ;
#9151=CARTESIAN_POINT ( 'NONE',  ( 10.00000000000000000, 0.000000000000000000, 0.000000000000000000 ) ) ;
#9156=CYLINDRICAL_SURFACE ( 'NONE', #19074, 16.00000000000000000 ) ;
#9161=ORIENTED_EDGE ( 'NONE', *, *, #18170, .T. ) ;
#9162=ADVANCED_FACE ( 'NONE', ( #47290 ), #21085, .F. ) ;
#9164=ORIENTED_EDGE ( 'NONE', *, *, #42891, .T. ) ;
#9166=EDGE_CURVE ( 'NONE', #15496, #44922, #2966, .T. ) ;
#9186=VERTEX_POINT ( 'NONE', #9585 ) ;
#9195=CARTESIAN_POINT ( 'NONE',  ( 10.00000000000000000, -33.79645857604525361, 16.45098606841114730 ) ) ;
#9196=EDGE_CURVE ( 'NONE', #27800, #30662, #35553, .T. ) ;
#9197=CIRCLE ( 'NONE', #14686, 16.00000000000000355 ) ;
#9208=PLANE ( 'NONE',  #8916 ) ;
#9211=AXIS2_PLACEMENT_3D ( 'NONE', #35030, #16673, #42382 ) ;
#9216=VERTEX_POINT ( 'NONE', #47518 ) ;
#9222=COLOUR_RGB ( '', 0.66274510, 0.83137255, 0.94901961) ;
#9224=ADVANCED_FACE ( 'NONE', ( #20866 ), #44091, .F. ) ;
#9228=EDGE_LOOP ( 'NONE', ( #6525, #35582, #8683, #44917 ) ) ;
#9232=CARTESIAN_POINT ( 'NONE',  ( 0.000000000000000000, -20.55727247249726020, -16.78983467731313084 ) ) ;
#9233=CARTESIAN_POINT ( 'NONE',  ( -3.000000000000000000, -22.32062822937469804, -14.36278369418829826 ) ) ;
#9245=DIRECTION ( 'NONE',  ( 1.000000000000000000, 0.000000000000000000, -0.000000000000000000 ) ) ;
#9246=FACE_OUTER_BOUND ( 'NONE', #33683, .T. ) ;
#9250=ORIENTED_EDGE ( 'NONE', *, *, #38063, .F. ) ;
#9261=DIRECTION ( 'NONE',  ( -1.000000000000000000, -0.000000000000000000, -0.000000000000000000 ) ) ;
#9262=VECTOR ( 'NONE', #15961, 1000.000000000000000 ) ;
#9264=ORIENTED_EDGE ( 'NONE', *, *, #37138, .F. ) ;
#9266=DIRECTION ( 'NONE',  ( 0.000000000000000000, -1.000000000000000000, 1.156482317317870936E-15 ) ) ;
#9268=CARTESIAN_POINT ( 'NONE',  ( 10.00000000000000000, 0.000000000000000000, 0.000000000000000000 ) ) ;
#9271=AXIS2_PLACEMENT_3D ( 'NONE', #14157, #10482, #21736 ) ;
#9272=ADVANCED_FACE ( 'NONE', ( #13767 ), #43615, .F. ) ;
#9280=EDGE_CURVE ( 'NONE', #41101, #18029, #10418, .T. ) ;
#9282=ORIENTED_EDGE ( 'NONE', *, *, #2, .F. ) ;
#9290=DIRECTION ( 'NONE',  ( -1.000000000000000000, 0.000000000000000000, -0.000000000000000000 ) ) ;
#9293=CARTESIAN_POINT ( 'NONE',  ( 10.00000000000000000, 12.26510123303308752, -35.53030884539072787 ) ) ;
#9295=CARTESIAN_POINT ( 'NONE',  ( 10.00000000000000000, 0.000000000000000000, 0.000000000000000000 ) ) ;
#9297=CARTESIAN_POINT ( 'NONE',  ( 10.00000000000000000, 0.000000000000000000, 0.000000000000000000 ) ) ;
#9303=ORIENTED_EDGE ( 'NONE', *, *, #22346, .T. ) ;
#9306=DIRECTION ( 'NONE',  ( -0.000000000000000000, -0.9945218953682741780, 0.1045284632676447834 ) ) ;
#9313=AXIS2_PLACEMENT_3D ( 'NONE', #45720, #183, #8271 ) ;
#9316=CARTESIAN_POINT ( 'NONE',  ( 4.999999999999999112, -41.81611651403859042, -3.925862922256606602 ) ) ;
#9326=DIRECTION ( 'NONE',  ( 0.000000000000000000, -0.1564344650402170189, -0.9876883405951399908 ) ) ;
#9332=CARTESIAN_POINT ( 'NONE',  ( 0.000000000000000000, -16.23288003029521320, 33.80338159004277543 ) ) ;
#9336=ORIENTED_EDGE ( 'NONE', *, *, #15758, .F. ) ;
#9339=EDGE_CURVE ( 'NONE', #40104, #8546, #3199, .T. ) ;
#9341=VERTEX_POINT ( 'NONE', #18127 ) ;
#9353=CARTESIAN_POINT ( 'NONE',  ( 0.000000000000000000, 0.000000000000000000, 0.000000000000000000 ) ) ;
#9354=CARTESIAN_POINT ( 'NONE',  ( -3.000000000000000000, 16.83928648764923253, 16.46020748918050458 ) ) ;
#9359=DIRECTION ( 'NONE',  ( -1.000000000000000000, -0.000000000000000000, 0.000000000000000000 ) ) ;
#9361=DIRECTION ( 'NONE',  ( 0.000000000000000000, -0.1564344650402170189, -0.9876883405951399908 ) ) ;
#9381=ORIENTED_EDGE ( 'NONE', *, *, #34237, .F. ) ;
#9385=EDGE_CURVE ( 'NONE', #39461, #25221, #38385, .T. ) ;
#9387=EDGE_CURVE ( 'NONE', #9910, #1345, #36199, .T. ) ;
#9391=CARTESIAN_POINT ( 'NONE',  ( -10.00000000000000000, 0.000000000000000000, 0.000000000000000000 ) ) ;
#9393=ADVANCED_FACE ( 'NONE', ( #36735 ), #33068, .T. ) ;
#9394=VERTEX_POINT ( 'NONE', #18625 ) ;
#9398=DIRECTION ( 'NONE',  ( -1.000000000000000000, -0.000000000000000000, -0.000000000000000000 ) ) ;
#9408=CARTESIAN_POINT ( 'NONE',  ( 5.000000000000000000, 36.13751322684419165, 21.40280677340384585 ) ) ;
#9413=ORIENTED_EDGE ( 'NONE', *, *, #14816, .T. ) ;
#9417=FACE_BOUND ( 'NONE', #32242, .T. ) ;
#9425=CARTESIAN_POINT ( 'NONE',  ( 5.000000000000000000, 31.52238457039637609, -27.75498641678709788 ) ) ;
#9458=ORIENTED_EDGE ( 'NONE', *, *, #32634, .T. ) ;
#9460=DIRECTION ( 'NONE',  ( -1.000000000000000000, 0.000000000000000000, 0.000000000000000000 ) ) ;
#9461=ORIENTED_EDGE ( 'NONE', *, *, #39525, .F. ) ;
#9487=CARTESIAN_POINT ( 'NONE',  ( 0.000000000000000000, -15.48615015657610527, 39.04073710021338428 ) ) ;
#9493=DIRECTION ( 'NONE',  ( -0.000000000000000000, -0.3090169943749573878, 0.9510565162951503115 ) ) ;
#9496=CYLINDRICAL_SURFACE ( 'NONE', #14005, 16.00000000000000000 ) ;
#9497=CARTESIAN_POINT ( 'NONE',  ( 10.00000000000000000, 0.000000000000000000, 0.000000000000000000 ) ) ;
#9500=CARTESIAN_POINT ( 'NONE',  ( 0.000000000000000000, 0.000000000000000000, 0.000000000000000000 ) ) ;
#9508=DIRECTION ( 'NONE',  ( 0.000000000000000000, 0.3090169943749482839, -0.9510565162951533091 ) ) ;
#9514=LINE ( 'NONE', #2186, #10885 ) ;
#9520=DIRECTION ( 'NONE',  ( -0.000000000000000000, -0.9510565162951506446, -0.3090169943749562220 ) ) ;
#9538=CYLINDRICAL_SURFACE ( 'NONE', #43397, 42.00000000000000000 ) ;
#9542=CARTESIAN_POINT ( 'NONE',  ( 10.00000000000000000, -38.55633173626998911, -16.65560815589452304 ) ) ;
#9544=CYLINDRICAL_SURFACE ( 'NONE', #19086, 42.00000000000000000 ) ;
#9546=EDGE_CURVE ( 'NONE', #35770, #33176, #31295, .T. ) ;
#9547=CIRCLE ( 'NONE', #35338, 16.00000000000000000 ) ;
#9557=VERTEX_POINT ( 'NONE', #1919 ) ;
#9558=EDGE_CURVE ( 'NONE', #31834, #34210, #28377, .T. ) ;
#9560=ADVANCED_FACE ( 'NONE', ( #9246 ), #24179, .T. ) ;
#9571=LINE ( 'NONE', #13033, #25298 ) ;
#9574=LINE ( 'NONE', #20854, #3144 ) ;
#9577=AXIS2_PLACEMENT_3D ( 'NONE', #44649, #21885, #40736 ) ;
#9585=CARTESIAN_POINT ( 'NONE',  ( 0.000000000000000000, 22.07842321921492612, -8.187992925817130896 ) ) ;
#9586=DIRECTION ( 'NONE',  ( -1.000000000000000000, 0.000000000000000000, -0.000000000000000000 ) ) ;
#9589=EDGE_LOOP ( 'NONE', ( #30946, #26571, #23977, #47289 ) ) ;
#9591=ORIENTED_EDGE ( 'NONE', *, *, #37247, .T. ) ;
#9597=DIRECTION ( 'NONE',  ( 0.000000000000000000, -0.3090169943749549453, 0.9510565162951511997 ) ) ;
#9608=EDGE_CURVE ( 'NONE', #38886, #12494, #16684, .T. ) ;
#9610=SURFACE_SIDE_STYLE ('',( #43162 ) ) ;
#9614=VECTOR ( 'NONE', #2860, 1000.000000000000000 ) ;
#9616=DIRECTION ( 'NONE',  ( 0.000000000000000000, 0.000000000000000000, 1.000000000000000000 ) ) ;
#9623=VECTOR ( 'NONE', #14033, 1000.000000000000000 ) ;
#9644=VERTEX_POINT ( 'NONE', #40792 ) ;
#9645=AXIS2_PLACEMENT_3D ( 'NONE', #6029, #6496, #28998 ) ;
#9647=FACE_OUTER_BOUND ( 'NONE', #36908, .T. ) ;
#9659=FACE_BOUND ( 'NONE', #37760, .T. ) ;
#9676=CARTESIAN_POINT ( 'NONE',  ( 0.000000000000000000, 0.000000000000000000, 0.000000000000000000 ) ) ;
#9679=AXIS2_PLACEMENT_3D ( 'NONE', #23823, #27751, #16723 ) ;
#9681=DIRECTION ( 'NONE',  ( 0.000000000000000000, 0.000000000000000000, 1.000000000000000000 ) ) ;
#9683=CIRCLE ( 'NONE', #37037, 37.49900000000000944 ) ;
#9692=ORIENTED_EDGE ( 'NONE', *, *, #29666, .F. ) ;
#9706=EDGE_LOOP ( 'NONE', ( #9461, #367, #9336, #34671 ) ) ;
#9707=DIRECTION ( 'NONE',  ( 1.000000000000000000, -0.000000000000000000, -0.000000000000000000 ) ) ;
#9708=PLANE ( 'NONE',  #8660 ) ;
#9712=ORIENTED_EDGE ( 'NONE', *, *, #25846, .F. ) ;
#9717=CARTESIAN_POINT ( 'NONE',  ( 0.000000000000000000, 0.000000000000000000, 0.000000000000000000 ) ) ;
#9723=DIRECTION ( 'NONE',  ( 1.000000000000000000, 0.000000000000000000, 0.000000000000000000 ) ) ;
#9728=AXIS2_PLACEMENT_3D ( 'NONE', #28309, #36130, #28794 ) ;
#9731=VECTOR ( 'NONE', #9493, 1000.000000000000000 ) ;
#9732=CARTESIAN_POINT ( 'NONE',  ( -3.000000000000000000, 23.50000000000000000, -1.500000000000001332 ) ) ;
#9735=VECTOR ( 'NONE', #23072, 1000.000000000000000 ) ;
#9747=CARTESIAN_POINT ( 'NONE',  ( 10.00000000000000000, -36.13751322684434797, 21.40280677340358295 ) ) ;
#9753=VERTEX_POINT ( 'NONE', #399 ) ;
#9762=VECTOR ( 'NONE', #28254, 1000.000000000000114 ) ;
#9764=DIRECTION ( 'NONE',  ( 0.000000000000000000, 0.1564344650402244852, 0.9876883405951387696 ) ) ;
#9789=VERTEX_POINT ( 'NONE', #34389 ) ;
#9796=FACE_OUTER_BOUND ( 'NONE', #37592, .T. ) ;
#9801=AXIS2_PLACEMENT_3D ( 'NONE', #13771, #28698, #10084 ) ;
#9803=DIRECTION ( 'NONE',  ( 1.000000000000000000, 0.000000000000000000, -0.000000000000000000 ) ) ;
#9811=VECTOR ( 'NONE', #16177, 1000.000000000000114 ) ;
#9818=DIRECTION ( 'NONE',  ( 0.000000000000000000, 0.000000000000000000, 1.000000000000000000 ) ) ;
#9823=ORIENTED_EDGE ( 'NONE', *, *, #4868, .T. ) ;
#9843=PLANE ( 'NONE',  #786 ) ;
#9845=EDGE_LOOP ( 'NONE', ( #46506, #35479, #28863, #45596 ) ) ;
#9867=DIRECTION ( 'NONE',  ( -1.000000000000000000, 0.000000000000000000, 0.000000000000000000 ) ) ;
#9876=DIRECTION ( 'NONE',  ( -1.000000000000000000, -0.000000000000000000, -0.000000000000000000 ) ) ;
#9880=LINE ( 'NONE', #46358, #18979 ) ;
#9897=CARTESIAN_POINT ( 'NONE',  ( -3.000000000000000000, -0.9646360437372163421, -23.52805723605591126 ) ) ;
#9909=DIRECTION ( 'NONE',  ( -1.000000000000000000, 0.000000000000000000, 0.000000000000000000 ) ) ;
#9910=VERTEX_POINT ( 'NONE', #16783 ) ;
#9913=VECTOR ( 'NONE', #35982, 1000.000000000000000 ) ;
#9923=LINE ( 'NONE', #47376, #37975 ) ;
#9924=ORIENTED_EDGE ( 'NONE', *, *, #31299, .T. ) ;
#9927=DIRECTION ( 'NONE',  ( -1.000000000000000000, 0.000000000000000000, 0.000000000000000000 ) ) ;
#9936=ORIENTED_EDGE ( 'NONE', *, *, #36284, .T. ) ;
#9948=ORIENTED_EDGE ( 'NONE', *, *, #21905, .T. ) ;
#9965=ORIENTED_EDGE ( 'NONE', *, *, #31884, .T. ) ;
#9967=CARTESIAN_POINT ( 'NONE',  ( 10.00000000000000000, 37.22597642581158084, -5.202137450156524068 ) ) ;
#9970=DIRECTION ( 'NONE',  ( -0.000000000000000000, -0.6691306063588671194, 0.7431448254773862505 ) ) ;
#9974=CARTESIAN_POINT ( 'NONE',  ( 10.00000000000000000, 0.000000000000000000, 0.000000000000000000 ) ) ;
#9979=DIRECTION ( 'NONE',  ( 0.000000000000000000, 0.8090169943749487835, -0.5877852522924713607 ) ) ;
#9981=DIRECTION ( 'NONE',  ( -1.000000000000000000, -0.000000000000000000, -0.000000000000000000 ) ) ;
#9984=CARTESIAN_POINT ( 'NONE',  ( 10.00000000000000000, -0.8828120875898013420, -37.48860685352291711 ) ) ;
#9988=( NAMED_UNIT ( * ) PLANE_ANGLE_UNIT ( ) SI_UNIT ( $, .RADIAN. ) );
#9990=EDGE_LOOP ( 'NONE', ( #35724, #32446, #35226, #18754 ) ) ;
#9993=VECTOR ( 'NONE', #4325, 1000.000000000000000 ) ;
#10002=ADVANCED_FACE ( 'NONE', ( #17010 ), #42734, .T. ) ;
#10007=ORIENTED_EDGE ( 'NONE', *, *, #1827, .T. ) ;
#10017=EDGE_CURVE ( 'NONE', #5548, #38854, #17510, .T. ) ;
#10025=PLANE ( 'NONE',  #45398 ) ;
#10035=FACE_OUTER_BOUND ( 'NONE', #47924, .T. ) ;
#10038=EDGE_CURVE ( 'NONE', #12094, #15804, #47214, .T. ) ;
#10039=CARTESIAN_POINT ( 'NONE',  ( 0.000000000000000000, -22.32062822937469804, -14.36278369418829826 ) ) ;
#10045=CYLINDRICAL_SURFACE ( 'NONE', #17553, 16.00000000000000000 ) ;
#10052=ORIENTED_EDGE ( 'NONE', *, *, #9339, .T. ) ;
#10057=ADVANCED_FACE ( 'NONE', ( #36572 ), #25553, .T. ) ;
#10065=ORIENTED_EDGE ( 'NONE', *, *, #3252, .F. ) ;
#10067=ORIENTED_EDGE ( 'NONE', *, *, #14432, .T. ) ;
#10080=CARTESIAN_POINT ( 'NONE',  ( -3.000000000000000000, 23.59884966291538078, -12.14883922797231541 ) ) ;
#10084=DIRECTION ( 'NONE',  ( 0.000000000000000000, -0.7071067811865536790, 0.7071067811865414665 ) ) ;
#10090=CARTESIAN_POINT ( 'NONE',  ( 10.00000000000000000, 37.58145647212453611, 0.6853352020791767529 ) ) ;
#10094=DIRECTION ( 'NONE',  ( 0.000000000000000000, -0.3090169943749563330, 0.9510565162951507556 ) ) ;
#10095=ORIENTED_EDGE ( 'NONE', *, *, #41708, .F. ) ;
#10103=EDGE_CURVE ( 'NONE', #1846, #40367, #29817, .T. ) ;
#10113=ORIENTED_EDGE ( 'NONE', *, *, #31970, .T. ) ;
#10117=VERTEX_POINT ( 'NONE', #32195 ) ;
#10124=AXIS2_PLACEMENT_3D ( 'NONE', #27606, #42542, #23941 ) ;
#10125=ORIENTED_EDGE ( 'NONE', *, *, #47448, .T. ) ;
#10130=CARTESIAN_POINT ( 'NONE',  ( 10.00000000000000000, -21.32104025579091910, -30.84782396557241313 ) ) ;
#10132=DIRECTION ( 'NONE',  ( -1.000000000000000000, 0.000000000000000000, 0.000000000000000000 ) ) ;
#10134=CARTESIAN_POINT ( 'NONE',  ( 0.000000000000000000, -27.05870788708250885, 26.08949754953014022 ) ) ;
#10137=CARTESIAN_POINT ( 'NONE',  ( -3.000000000000000000, -3.948201729842038432, -23.21447184625298021 ) ) ;
#10138=DIRECTION ( 'NONE',  ( -1.000000000000000000, -0.000000000000000000, 0.000000000000000000 ) ) ;
#10144=VERTEX_POINT ( 'NONE', #7196 ) ;
#10148=CARTESIAN_POINT ( 'NONE',  ( 10.00000000000000000, 0.000000000000000000, 0.000000000000000000 ) ) ;
#10153=CARTESIAN_POINT ( 'NONE',  ( 0.000000000000000000, -30.84782396557201878, -21.32104025579148399 ) ) ;
#10155=DIRECTION ( 'NONE',  ( 1.000000000000000000, -0.000000000000000000, 0.000000000000000000 ) ) ;
#10156=CARTESIAN_POINT ( 'NONE',  ( 10.00000000000000000, 0.000000000000000000, 0.000000000000000000 ) ) ;
#10159=CARTESIAN_POINT ( 'NONE',  ( 10.00000000000000000, 37.48860685352291000, 0.8828120875901893649 ) ) ;
#10165=DIRECTION ( 'NONE',  ( 1.000000000000000000, -0.000000000000000000, -0.000000000000000000 ) ) ;
#10166=ORIENTED_EDGE ( 'NONE', *, *, #24212, .F. ) ;
#10168=DIRECTION ( 'NONE',  ( 0.000000000000000000, 0.000000000000000000, 1.000000000000000000 ) ) ;
#10170=ORIENTED_EDGE ( 'NONE', *, *, #4137, .F. ) ;
#10179=AXIS2_PLACEMENT_3D ( 'NONE', #45520, #37951, #22770 ) ;
#10180=AXIS2_PLACEMENT_3D ( 'NONE', #12480, #43306, #23724 ) ;
#10182=EDGE_LOOP ( 'NONE', ( #48117, #46192, #46504, #43371 ) ) ;
#10184=CIRCLE ( 'NONE', #36074, 37.49900000000000944 ) ;
#10187=CIRCLE ( 'NONE', #32112, 42.00000000000000000 ) ;
#10196=ADVANCED_FACE ( 'NONE', ( #32659 ), #28984, .T. ) ;
#10199=ORIENTED_EDGE ( 'NONE', *, *, #376, .F. ) ;
#10202=LINE ( 'NONE', #32249, #38178 ) ;
#10203=DIRECTION ( 'NONE',  ( 0.000000000000000000, 0.000000000000000000, 1.000000000000000000 ) ) ;
#10212=DIRECTION ( 'NONE',  ( -1.000000000000000000, 0.000000000000000000, 0.000000000000000000 ) ) ;
#10214=VECTOR ( 'NONE', #24769, 999.9999999999998863 ) ;
#10218=CARTESIAN_POINT ( 'NONE',  ( 0.000000000000000000, -38.55633173626998911, -16.65560815589452304 ) ) ;
#10219=EDGE_CURVE ( 'NONE', #7964, #16286, #10184, .T. ) ;
#10222=DIRECTION ( 'NONE',  ( 1.000000000000000000, 0.000000000000000000, 0.000000000000000000 ) ) ;
#10233=DIRECTION ( 'NONE',  ( 0.000000000000000000, -0.9781476007338041345, -0.2079116908177664480 ) ) ;
#10240=VECTOR ( 'NONE', #9520, 1000.000000000000227 ) ;
#10246=CIRCLE ( 'NONE', #44632, 16.00000000000000355 ) ;
#10252=ORIENTED_EDGE ( 'NONE', *, *, #22385, .T. ) ;
#10259=CARTESIAN_POINT ( 'NONE',  ( -3.000000000000000000, 0.000000000000000000, 0.000000000000000000 ) ) ;
#10264=CARTESIAN_POINT ( 'NONE',  ( 10.00000000000000000, -12.42422080174614862, -35.38097989696524337 ) ) ;
#10265=LINE ( 'NONE', #17848, #16032 ) ;
#10267=ORIENTED_EDGE ( 'NONE', *, *, #6264, .T. ) ;
#10268=CARTESIAN_POINT ( 'NONE',  ( 10.00000000000000000, -10.96151621346514382, 35.95386929396252640 ) ) ;
#10270=CARTESIAN_POINT ( 'NONE',  ( -10.00000000000000000, 0.000000000000000000, 0.000000000000000000 ) ) ;
#10277=DIRECTION ( 'NONE',  ( -1.000000000000000000, -0.000000000000000000, 0.000000000000000000 ) ) ;
#10289=CARTESIAN_POINT ( 'NONE',  ( 10.00000000000000000, -35.38097989696520074, 12.42422080174625520 ) ) ;
#10291=CARTESIAN_POINT ( 'NONE',  ( -3.000000000000000000, 9.615535125378775305, 24.73947219025917121 ) ) ;
#10292=ORIENTED_EDGE ( 'NONE', *, *, #32060, .T. ) ;
#10293=DIRECTION ( 'NONE',  ( -1.000000000000000000, 0.000000000000000000, 0.000000000000000000 ) ) ;
#10294=EDGE_LOOP ( 'NONE', ( #8346, #46683, #15996, #38874 ) ) ;
#10295=CARTESIAN_POINT ( 'NONE',  ( 10.00000000000000000, 25.88420570971438650, -27.13269053701069566 ) ) ;
#10297=CARTESIAN_POINT ( 'NONE',  ( 0.000000000000000000, 37.16516213103277266, 4.992566952385114831 ) ) ;
#10305=VECTOR ( 'NONE', #45065, 1000.000000000000000 ) ;
#10310=EDGE_CURVE ( 'NONE', #33538, #12545, #14881, .T. ) ;
#10315=CARTESIAN_POINT ( 'NONE',  ( 10.00000000000000000, -6.736453364083292428, -36.88895765772640800 ) ) ;
#10322=ORIENTED_EDGE ( 'NONE', *, *, #12664, .T. ) ;
#10344=LINE ( 'NONE', #18651, #12821 ) ;
#10345=CARTESIAN_POINT ( 'NONE',  ( 10.00000000000000000, -26.08949754953044220, 27.05870788708222818 ) ) ;
#10346=DIRECTION ( 'NONE',  ( -1.000000000000000000, -0.000000000000000000, 0.000000000000000000 ) ) ;
#10349=VERTEX_POINT ( 'NONE', #87 ) ;
#10350=CIRCLE ( 'NONE', #41618, 37.49900000000001654 ) ;
#10364=EDGE_CURVE ( 'NONE', #14290, #12132, #9136, .T. ) ;
#10376=DIRECTION ( 'NONE',  ( 0.000000000000000000, 0.000000000000000000, 1.000000000000000000 ) ) ;
#10377=CARTESIAN_POINT ( 'NONE',  ( 10.00000000000000000, 33.79645857604513992, -16.45098606841138178 ) ) ;
#10378=LINE ( 'NONE', #32429, #20401 ) ;
#10390=DIRECTION ( 'NONE',  ( 0.000000000000000000, -0.9510565162951500895, -0.3090169943749583314 ) ) ;
#10406=CYLINDRICAL_SURFACE ( 'NONE', #11410, 16.00000000000000000 ) ;
#10409=CARTESIAN_POINT ( 'NONE',  ( 10.00000000000000000, -31.52238457039619490, 27.75498641678731104 ) ) ;
#10415=EDGE_LOOP ( 'NONE', ( #43856, #16283, #41653, #36118 ) ) ;
#10418=CIRCLE ( 'NONE', #30769, 42.00000000000000000 ) ;
#10426=FACE_OUTER_BOUND ( 'NONE', #34734, .T. ) ;
#10437=ORIENTED_EDGE ( 'NONE', *, *, #14266, .F. ) ;
#10438=CIRCLE ( 'NONE', #15132, 16.00000000000000000 ) ;
#10446=DIRECTION ( 'NONE',  ( 0.000000000000000000, -0.9781476007338040235, -0.2079116908177671419 ) ) ;
#10447=DIRECTION ( 'NONE',  ( 0.000000000000000000, 0.000000000000000000, 1.000000000000000000 ) ) ;
#10453=ADVANCED_FACE ( 'NONE', ( #5234 ), #20376, .T. ) ;
#10464=CARTESIAN_POINT ( 'NONE',  ( -3.000000000000000000, -10.45096189432314837, -21.10159698893440350 ) ) ;
#10466=CYLINDRICAL_SURFACE ( 'NONE', #23668, 42.00000000000000000 ) ;
#10473=LINE ( 'NONE', #21489, #19282 ) ;
#10480=ORIENTED_EDGE ( 'NONE', *, *, #19923, .F. ) ;
#10482=DIRECTION ( 'NONE',  ( -1.000000000000000000, -0.000000000000000000, -0.000000000000000000 ) ) ;
#10490=ORIENTED_EDGE ( 'NONE', *, *, #14264, .T. ) ;
#10493=EDGE_CURVE ( 'NONE', #37347, #22843, #7881, .T. ) ;
#10496=CARTESIAN_POINT ( 'NONE',  ( 10.00000000000000000, 0.000000000000000000, 0.000000000000000000 ) ) ;
#10501=EDGE_CURVE ( 'NONE', #23315, #27986, #24790, .T. ) ;
#10505=CIRCLE ( 'NONE', #28478, 15.99999999999999822 ) ;
#10511=DIRECTION ( 'NONE',  ( -1.000000000000000000, -0.000000000000000000, -0.000000000000000000 ) ) ;
#10519=ORIENTED_EDGE ( 'NONE', *, *, #26869, .T. ) ;
#10524=CYLINDRICAL_SURFACE ( 'NONE', #39854, 37.49900000000000233 ) ;
#10527=ORIENTED_EDGE ( 'NONE', *, *, #4510, .F. ) ;
#10531=AXIS2_PLACEMENT_3D ( 'NONE', #21362, #17927, #36771 ) ;
#10532=CYLINDRICAL_SURFACE ( 'NONE', #11219, 16.00000000000000000 ) ;
#10541=VECTOR ( 'NONE', #3788, 1000.000000000000000 ) ;
#10548=VECTOR ( 'NONE', #33672, 1000.000000000000000 ) ;
#10558=EDGE_CURVE ( 'NONE', #17233, #9394, #36516, .T. ) ;
#10564=FACE_OUTER_BOUND ( 'NONE', #40227, .T. ) ;
#10570=CARTESIAN_POINT ( 'NONE',  ( 0.000000000000000000, 10.96151621346540317, -35.95386929396244113 ) ) ;
#10572=CARTESIAN_POINT ( 'NONE',  ( -3.000000000000000000, -10.45096189432314837, -21.10159698893440350 ) ) ;
#10573=CARTESIAN_POINT ( 'NONE',  ( 0.000000000000000000, 31.52238457039599595, 27.75498641678753842 ) ) ;
#10583=CARTESIAN_POINT ( 'NONE',  ( 10.00000000000000000, 27.13269053701096922, 25.88420570971410228 ) ) ;
#10588=CARTESIAN_POINT ( 'NONE',  ( -3.000000000000000000, -25.60904388321925396, 6.976881207771172377 ) ) ;
#10589=FACE_OUTER_BOUND ( 'NONE', #11641, .T. ) ;
#10591=VECTOR ( 'NONE', #37302, 1000.000000000000114 ) ;
#10597=CIRCLE ( 'NONE', #47346, 37.49900000000000233 ) ;
#10600=CARTESIAN_POINT ( 'NONE',  ( 10.00000000000000000, 6.555932627142418312, 37.01155633439060466 ) ) ;
#10606=CYLINDRICAL_SURFACE ( 'NONE', #18655, 16.00000000000000000 ) ;
#10621=AXIS2_PLACEMENT_3D ( 'NONE', #41953, #12097, #8405 ) ;
#10627=CARTESIAN_POINT ( 'NONE',  ( -10.00000000000000000, 0.000000000000000000, 0.000000000000000000 ) ) ;
#10636=LINE ( 'NONE', #36799, #7134 ) ;
#10640=EDGE_LOOP ( 'NONE', ( #19927, #42283, #12724, #5147 ) ) ;
#10653=CARTESIAN_POINT ( 'NONE',  ( 10.00000000000000000, -32.34446384429989507, 26.79245525562703278 ) ) ;
#10666=DIRECTION ( 'NONE',  ( 1.000000000000000000, -0.000000000000000000, -0.000000000000000000 ) ) ;
#10667=ADVANCED_FACE ( 'NONE', ( #22062 ), #33569, .F. ) ;
#10677=ORIENTED_EDGE ( 'NONE', *, *, #47082, .F. ) ;
#10678=EDGE_CURVE ( 'NONE', #20089, #11046, #29897, .T. ) ;
#10682=DIRECTION ( 'NONE',  ( 0.000000000000000000, -0.4067366430757881068, -0.9135454576426063067 ) ) ;
#10689=ORIENTED_EDGE ( 'NONE', *, *, #14886, .T. ) ;
#10699=CARTESIAN_POINT ( 'NONE',  ( 0.000000000000000000, 0.000000000000000000, 0.000000000000000000 ) ) ;
#10700=VERTEX_POINT ( 'NONE', #26476 ) ;
#10715=CARTESIAN_POINT ( 'NONE',  ( 0.000000000000000000, -37.58145647212455032, 0.6853352020789044152 ) ) ;
#10720=DIRECTION ( 'NONE',  ( 1.000000000000000000, -0.000000000000000000, 0.000000000000000000 ) ) ;
#10721=CARTESIAN_POINT ( 'NONE',  ( -3.000000000000000000, 23.50000000000000000, 1.499999999999997780 ) ) ;
#10726=FILL_AREA_STYLE_COLOUR ( '', #9222 ) ;
#10728=DIRECTION ( 'NONE',  ( -1.000000000000000000, 0.000000000000000000, 0.000000000000000000 ) ) ;
#10732=VECTOR ( 'NONE', #42690, 1000.000000000000000 ) ;
#10744=VECTOR ( 'NONE', #10871, 1000.000000000000000 ) ;
#10752=DIRECTION ( 'NONE',  ( 0.000000000000000000, 0.5877852522924742473, -0.8090169943749465631 ) ) ;
#10758=ORIENTED_EDGE ( 'NONE', *, *, #30985, .F. ) ;
#10761=DIRECTION ( 'NONE',  ( 0.000000000000000000, 0.5877852522924685852, 0.8090169943749508930 ) ) ;
#10764=DIRECTION ( 'NONE',  ( -1.000000000000000000, 0.000000000000000000, 0.000000000000000000 ) ) ;
#10767=FACE_OUTER_BOUND ( 'NONE', #27469, .T. ) ;
#10768=CARTESIAN_POINT ( 'NONE',  ( -3.000000000000000000, -14.54903810567645195, -22.19967320028775504 ) ) ;
#10775=DIRECTION ( 'NONE',  ( -1.000000000000000000, 0.000000000000000000, 0.000000000000000000 ) ) ;
#10780=ORIENTED_EDGE ( 'NONE', *, *, #16020, .F. ) ;
#10798=AXIS2_PLACEMENT_3D ( 'NONE', #26099, #11434, #15090 ) ;
#10808=CARTESIAN_POINT ( 'NONE',  ( -10.00000000000000000, 0.000000000000000000, 0.000000000000000000 ) ) ;
#10810=ADVANCED_FACE ( 'NONE', ( #45544 ), #30884, .F. ) ;
#10828=DIRECTION ( 'NONE',  ( 0.000000000000000000, 0.6691306063588672304, -0.7431448254773862505 ) ) ;
#10834=DIRECTION ( 'NONE',  ( -1.000000000000000000, 0.000000000000000000, 0.000000000000000000 ) ) ;
#10837=DIRECTION ( 'NONE',  ( 1.000000000000000000, -0.000000000000000000, 0.000000000000000000 ) ) ;
#10852=CARTESIAN_POINT ( 'NONE',  ( -3.000000000000000000, -22.67460108101774807, -6.353146135318215038 ) ) ;
#10857=EDGE_CURVE ( 'NONE', #46024, #26165, #20411, .T. ) ;
#10871=DIRECTION ( 'NONE',  ( -0.000000000000000000, 0.9781476007338069101, -0.2079116908177532363 ) ) ;
#10880=DIRECTION ( 'NONE',  ( 0.000000000000000000, 0.000000000000000000, 1.000000000000000000 ) ) ;
#10885=VECTOR ( 'NONE', #46974, 1000.000000000000227 ) ;
#10896=CARTESIAN_POINT ( 'NONE',  ( 10.00000000000000000, -27.75498641678764855, 31.52238457039589647 ) ) ;
#10901=ADVANCED_FACE ( 'NONE', ( #9082 ), #4680, .F. ) ;
#10914=CIRCLE ( 'NONE', #47659, 16.00000000000000000 ) ;
#10920=ORIENTED_EDGE ( 'NONE', *, *, #5021, .T. ) ;
#10951=ORIENTED_EDGE ( 'NONE', *, *, #13649, .T. ) ;
#10959=CYLINDRICAL_SURFACE ( 'NONE', #28419, 42.00000000000000000 ) ;
#10964=AXIS2_PLACEMENT_3D ( 'NONE', #33322, #25967, #2969 ) ;
#10972=ORIENTED_EDGE ( 'NONE', *, *, #34800, .F. ) ;
#10974=AXIS2_PLACEMENT_3D ( 'NONE', #41995, #45654, #23373 ) ;
#10977=CIRCLE ( 'NONE', #11752, 42.00000000000000000 ) ;
#10982=VECTOR ( 'NONE', #31734, 999.9999999999998863 ) ;
#10988=VERTEX_POINT ( 'NONE', #6851 ) ;
#10992=LINE ( 'NONE', #14428, #46152 ) ;
#10996=ORIENTED_EDGE ( 'NONE', *, *, #42812, .T. ) ;
#11002=FACE_OUTER_BOUND ( 'NONE', #14788, .T. ) ;
#11005=DIRECTION ( 'NONE',  ( 1.000000000000000000, -0.000000000000000000, 0.000000000000000000 ) ) ;
#11006=EDGE_CURVE ( 'NONE', #41954, #33176, #26649, .T. ) ;
#11015=EDGE_CURVE ( 'NONE', #30305, #19681, #32885, .T. ) ;
#11017=CIRCLE ( 'NONE', #8659, 16.00000000000000000 ) ;
#11020=VECTOR ( 'NONE', #38512, 999.9999999999998863 ) ;
#11025=ORIENTED_EDGE ( 'NONE', *, *, #11459, .F. ) ;
#11034=CARTESIAN_POINT ( 'NONE',  ( 10.00000000000000000, 0.000000000000000000, 0.000000000000000000 ) ) ;
#11038=ORIENTED_EDGE ( 'NONE', *, *, #24257, .T. ) ;
#11045=DIRECTION ( 'NONE',  ( 0.000000000000000000, 0.000000000000000000, 1.000000000000000000 ) ) ;
#11046=VERTEX_POINT ( 'NONE', #3398 ) ;
#11055=CARTESIAN_POINT ( 'NONE',  ( 10.00000000000000000, 26.08949754953024325, 27.05870788708241648 ) ) ;
#11057=VECTOR ( 'NONE', #37361, 1000.000000000000000 ) ;
#11058=CIRCLE ( 'NONE', #45436, 16.00000000000000000 ) ;
#11060=DIRECTION ( 'NONE',  ( 0.000000000000000000, -0.3090169943749449533, -0.9510565162951543083 ) ) ;
#11063=AXIS2_PLACEMENT_3D ( 'NONE', #40080, #21218, #32255 ) ;
#11064=EDGE_CURVE ( 'NONE', #14109, #12152, #3181, .T. ) ;
#11069=DIRECTION ( 'NONE',  ( 1.000000000000000000, 0.000000000000000000, 0.000000000000000000 ) ) ;
#11071=PLANE ( 'NONE',  #13628 ) ;
#11073=CARTESIAN_POINT ( 'NONE',  ( 5.000000000000000000, -31.52238457039619490, 27.75498641678731104 ) ) ;
#11078=DIRECTION ( 'NONE',  ( 0.000000000000000000, -0.1564344650402380854, 0.9876883405951365491 ) ) ;
#11087=ORIENTED_EDGE ( 'NONE', *, *, #40052, .F. ) ;
#11092=( GEOMETRIC_REPRESENTATION_CONTEXT ( 3 ) GLOBAL_UNCERTAINTY_ASSIGNED_CONTEXT ( ( #15425 ) ) GLOBAL_UNIT_ASSIGNED_CONTEXT ( ( #4990, #17195, #35813 ) ) REPRESENTATION_CONTEXT ( 'NONE', 'WORKASPACE' ) );
#11094=CARTESIAN_POINT ( 'NONE',  ( 0.000000000000000000, 0.000000000000000000, 0.000000000000000000 ) ) ;
#11096=DIRECTION ( 'NONE',  ( -1.000000000000000000, -0.000000000000000000, 0.000000000000000000 ) ) ;
#11099=VECTOR ( 'NONE', #42292, 1000.000000000000000 ) ;
#11121=ORIENTED_EDGE ( 'NONE', *, *, #37282, .T. ) ;
#11127=DIRECTION ( 'NONE',  ( 1.000000000000000000, 0.000000000000000000, -0.000000000000000000 ) ) ;
#11128=FACE_OUTER_BOUND ( 'NONE', #19913, .T. ) ;
#11136=CARTESIAN_POINT ( 'NONE',  ( 10.00000000000000000, 21.53537804866081373, 30.80686688397018358 ) ) ;
#11137=ADVANCED_FACE ( 'NONE', ( #11002 ), #44528, .T. ) ;
#11150=CARTESIAN_POINT ( 'NONE',  ( 10.00000000000000000, -33.17418723428319538, 17.67226234102814431 ) ) ;
#11151=VECTOR ( 'NONE', #1338, 1000.000000000000000 ) ;
#11159=ORIENTED_EDGE ( 'NONE', *, *, #22634, .F. ) ;
#11162=ORIENTED_EDGE ( 'NONE', *, *, #19702, .T. ) ;
#11164=AXIS2_PLACEMENT_3D ( 'NONE', #28107, #35921, #9979 ) ;
#11170=ORIENTED_EDGE ( 'NONE', *, *, #23984, .T. ) ;
#11174=EDGE_CURVE ( 'NONE', #33176, #18905, #33325, .T. ) ;
#11175=CARTESIAN_POINT ( 'NONE',  ( 10.00000000000000000, 0.000000000000000000, 0.000000000000000000 ) ) ;
#11199=VECTOR ( 'NONE', #14622, 1000.000000000000000 ) ;
#11211=LINE ( 'NONE', #34198, #43323 ) ;
#11212=ORIENTED_EDGE ( 'NONE', *, *, #3304, .F. ) ;
#11213=ORIENTED_EDGE ( 'NONE', *, *, #43142, .T. ) ;
#11219=AXIS2_PLACEMENT_3D ( 'NONE', #11985, #20281, #34238 ) ;
#11228=EDGE_CURVE ( 'NONE', #18553, #17403, #23960, .T. ) ;
#11235=CARTESIAN_POINT ( 'NONE',  ( 0.000000000000000000, 0.000000000000000000, 0.000000000000000000 ) ) ;
#11238=CARTESIAN_POINT ( 'NONE',  ( 10.00000000000000000, 6.555932627142952995, -37.01155633439051940 ) ) ;
#11249=FACE_OUTER_BOUND ( 'NONE', #32888, .T. ) ;
#11257=DIRECTION ( 'NONE',  ( -1.000000000000000000, -0.000000000000000000, -0.000000000000000000 ) ) ;
#11272=DIRECTION ( 'NONE',  ( 0.000000000000000000, -0.5877852522924801315, 0.8090169943749421222 ) ) ;
#11288=ADVANCED_FACE ( 'NONE', ( #30567 ), #11974, .F. ) ;
#11298=ORIENTED_EDGE ( 'NONE', *, *, #30711, .F. ) ;
#11300=CARTESIAN_POINT ( 'NONE',  ( 0.000000000000000000, 5.835314593368772229, -22.81335362449846826 ) ) ;
#11311=DIRECTION ( 'NONE',  ( 0.000000000000000000, 0.6691306063588675634, -0.7431448254773856954 ) ) ;
#11312=AXIS2_PLACEMENT_3D ( 'NONE', #43956, #10682, #40307 ) ;
#11331=DIRECTION ( 'NONE',  ( 0.000000000000000000, 0.9945218953682731788, 0.1045284632676559550 ) ) ;
#11354=AXIS2_PLACEMENT_3D ( 'NONE', #11882, #45651, #34372 ) ;
#11356=DIRECTION ( 'NONE',  ( -1.000000000000000000, -0.000000000000000000, 0.000000000000000000 ) ) ;
#11357=EDGE_CURVE ( 'NONE', #37523, #20853, #14805, .T. ) ;
#11358=DIRECTION ( 'NONE',  ( 0.000000000000000000, 0.000000000000000000, 1.000000000000000000 ) ) ;
#11359=CARTESIAN_POINT ( 'NONE',  ( -3.000000000000000000, 26.50000000000000355, 1.500000000000000000 ) ) ;
#11361=ORIENTED_EDGE ( 'NONE', *, *, #37085, .F. ) ;
#11367=ADVANCED_FACE ( 'NONE', ( #28105 ), #43277, .F. ) ;
#11368=DIRECTION ( 'NONE',  ( 1.000000000000000000, 0.000000000000000000, 0.000000000000000000 ) ) ;
#11372=ORIENTED_EDGE ( 'NONE', *, *, #19702, .F. ) ;
#11381=CARTESIAN_POINT ( 'NONE',  ( 10.00000000000000000, 10.41901085202078114, 40.68715046381932865 ) ) ;
#11382=FACE_OUTER_BOUND ( 'NONE', #33663, .T. ) ;
#11386=CARTESIAN_POINT ( 'NONE',  ( 10.00000000000000000, 29.81001611431041098, -22.74946021919100403 ) ) ;
#11399=VECTOR ( 'NONE', #9143, 1000.000000000000000 ) ;
#11410=AXIS2_PLACEMENT_3D ( 'NONE', #40281, #47836, #43698 ) ;
#11427=ORIENTED_EDGE ( 'NONE', *, *, #28962, .T. ) ;
#11430=CYLINDRICAL_SURFACE ( 'NONE', #44283, 42.00000000000000000 ) ;
#11434=DIRECTION ( 'NONE',  ( -1.000000000000000000, 0.000000000000000000, 0.000000000000000000 ) ) ;
#11446=ORIENTED_EDGE ( 'NONE', *, *, #15428, .F. ) ;
#11448=CARTESIAN_POINT ( 'NONE',  ( 10.00000000000000000, -21.53537804866103045, 30.80686688397002371 ) ) ;
#11455=CIRCLE ( 'NONE', #16133, 16.00000000000000355 ) ;
#11459=EDGE_CURVE ( 'NONE', #38425, #48416, #23346, .T. ) ;
#11460=EDGE_CURVE ( 'NONE', #9341, #23667, #20858, .T. ) ;
#11463=ADVANCED_FACE ( 'NONE', ( #30457 ), #12112, .T. ) ;
#11471=VECTOR ( 'NONE', #15525, 1000.000000000000114 ) ;
#11474=VERTEX_POINT ( 'NONE', #33632 ) ;
#11485=DIRECTION ( 'NONE',  ( 0.000000000000000000, 0.000000000000000000, 1.000000000000000000 ) ) ;
#11489=CARTESIAN_POINT ( 'NONE',  ( 10.00000000000000000, -29.81001611430991360, -22.74946021919165418 ) ) ;
#11496=CARTESIAN_POINT ( 'NONE',  ( 10.00000000000000000, 26.08949754953024325, 27.05870788708241648 ) ) ;
#11497=VECTOR ( 'NONE', #5852, 999.9999999999998863 ) ;
#11498=DIRECTION ( 'NONE',  ( -1.000000000000000000, 0.000000000000000000, -0.000000000000000000 ) ) ;
#11499=DIRECTION ( 'NONE',  ( 1.000000000000000000, 0.000000000000000000, 0.000000000000000000 ) ) ;
#11517=ADVANCED_FACE ( 'NONE', ( #7694 ), #22861, .T. ) ;
#11519=CARTESIAN_POINT ( 'NONE',  ( 0.000000000000000000, 0.000000000000000000, 0.000000000000000000 ) ) ;
#11521=LINE ( 'NONE', #8322, #30481 ) ;
#11522=VERTEX_POINT ( 'NONE', #34119 ) ;
#11529=CARTESIAN_POINT ( 'NONE',  ( -3.000000000000000000, -18.13022148937263012, 15.02647892043544608 ) ) ;
#11537=ORIENTED_EDGE ( 'NONE', *, *, #36902, .F. ) ;
#11542=CARTESIAN_POINT ( 'NONE',  ( 10.00000000000000000, 2.663952781846733675, -41.91543099594814947 ) ) ;
#11545=EDGE_LOOP ( 'NONE', ( #19754, #8506, #31032, #2528 ) ) ;
#11546=CARTESIAN_POINT ( 'NONE',  ( 0.000000000000000000, 0.000000000000000000, 0.000000000000000000 ) ) ;
#11558=CARTESIAN_POINT ( 'NONE',  ( 0.000000000000000000, 27.13269053701132094, -25.88420570971372570 ) ) ;
#11559=CARTESIAN_POINT ( 'NONE',  ( -3.000000000000000000, 16.61724383029390140, -20.69703378468903665 ) ) ;
#11567=CARTESIAN_POINT ( 'NONE',  ( -3.000000000000000000, -25.60904388321916159, -6.976881207771517879 ) ) ;
#11570=EDGE_CURVE ( 'NONE', #42331, #23892, #39639, .T. ) ;
#11573=EDGE_CURVE ( 'NONE', #46514, #22743, #11616, .T. ) ;
#11582=VERTEX_POINT ( 'NONE', #30956 ) ;
#11584=CARTESIAN_POINT ( 'NONE',  ( 0.000000000000000000, 41.81611651403868990, -3.925862922255709542 ) ) ;
#11597=ORIENTED_EDGE ( 'NONE', *, *, #11602, .T. ) ;
#11598=DIRECTION ( 'NONE',  ( -1.000000000000000000, -0.000000000000000000, 0.000000000000000000 ) ) ;
#11601=LINE ( 'NONE', #21878, #10591 ) ;
#11602=EDGE_CURVE ( 'NONE', #5896, #32654, #16971, .T. ) ;
#11605=CARTESIAN_POINT ( 'NONE',  ( 10.00000000000000000, 26.79245525562714647, 32.34446384429980981 ) ) ;
#11611=VECTOR ( 'NONE', #30271, 1000.000000000000000 ) ;
#11612=DIRECTION ( 'NONE',  ( -1.000000000000000000, 0.000000000000000000, 0.000000000000000000 ) ) ;
#11616=LINE ( 'NONE', #16014, #23232 ) ;
#11623=LINE ( 'NONE', #41005, #25601 ) ;
#11630=CARTESIAN_POINT ( 'NONE',  ( 5.000000000000000000, 26.79245525562762253, -32.34446384429941901 ) ) ;
#11635=ORIENTED_EDGE ( 'NONE', *, *, #23599, .F. ) ;
#11636=AXIS2_PLACEMENT_3D ( 'NONE', #13959, #6619, #3667 ) ;
#11641=EDGE_LOOP ( 'NONE', ( #47262, #238, #24713, #8236 ) ) ;
#11648=ORIENTED_EDGE ( 'NONE', *, *, #22346, .F. ) ;
#11651=AXIS2_PLACEMENT_3D ( 'NONE', #7774, #4116, #27121 ) ;
#11663=AXIS2_PLACEMENT_3D ( 'NONE', #10137, #36562, #13828 ) ;
#11668=ORIENTED_EDGE ( 'NONE', *, *, #31214, .T. ) ;
#11672=EDGE_CURVE ( 'NONE', #41802, #45751, #8646, .T. ) ;
#11673=DIRECTION ( 'NONE',  ( 0.000000000000000000, 0.8910065241883656784, 0.4539904997395510788 ) ) ;
#11679=STYLED_ITEM ( 'NONE', ( #21237 ), #21055 ) ;
#11689=AXIS2_PLACEMENT_3D ( 'NONE', #26796, #45392, #44438 ) ;
#11690=ORIENTED_EDGE ( 'NONE', *, *, #11672, .T. ) ;
#11693=VERTEX_POINT ( 'NONE', #42435 ) ;
#11701=CARTESIAN_POINT ( 'NONE',  ( 10.00000000000000000, -30.84782396557233142, 21.32104025579104345 ) ) ;
#11704=ORIENTED_EDGE ( 'NONE', *, *, #1558, .F. ) ;
#11712=FACE_OUTER_BOUND ( 'NONE', #15153, .T. ) ;
#11715=EDGE_CURVE ( 'NONE', #6597, #19561, #38526, .T. ) ;
#11723=ORIENTED_EDGE ( 'NONE', *, *, #10219, .F. ) ;
#11729=CYLINDRICAL_SURFACE ( 'NONE', #39433, 42.00000000000000000 ) ;
#11750=AXIS2_PLACEMENT_3D ( 'NONE', #5748, #24339, #43188 ) ;
#11751=EDGE_CURVE ( 'NONE', #32221, #37634, #47321, .T. ) ;
#11752=AXIS2_PLACEMENT_3D ( 'NONE', #7432, #18673, #11358 ) ;
#11753=DIRECTION ( 'NONE',  ( 0.000000000000000000, 0.8660254037844432595, -0.4999999999999919509 ) ) ;
#11760=ORIENTED_EDGE ( 'NONE', *, *, #6246, .T. ) ;
#11762=DIRECTION ( 'NONE',  ( 0.000000000000000000, 0.8910065241883688980, -0.4539904997395446951 ) ) ;
#11781=DIRECTION ( 'NONE',  ( -1.000000000000000000, 0.000000000000000000, 0.000000000000000000 ) ) ;
#11791=AXIS2_PLACEMENT_3D ( 'NONE', #24077, #19904, #20382 ) ;
#11795=DIRECTION ( 'NONE',  ( 1.000000000000000000, -0.000000000000000000, -0.000000000000000000 ) ) ;
#11801=DIRECTION ( 'NONE',  ( 0.000000000000000000, -0.9510565162951543083, 0.3090169943749449533 ) ) ;
#11802=CYLINDRICAL_SURFACE ( 'NONE', #4583, 42.00000000000000000 ) ;
#11812=ORIENTED_EDGE ( 'NONE', *, *, #44773, .F. ) ;
#11813=EDGE_CURVE ( 'NONE', #22090, #18915, #47771, .T. ) ;
#11821=DIRECTION ( 'NONE',  ( 0.000000000000000000, 0.000000000000000000, 1.000000000000000000 ) ) ;
#11831=CARTESIAN_POINT ( 'NONE',  ( 10.00000000000000000, 10.41901085202135668, -40.68715046381917944 ) ) ;
#11836=DIRECTION ( 'NONE',  ( 0.000000000000000000, 0.000000000000000000, 1.000000000000000000 ) ) ;
#11839=EDGE_CURVE ( 'NONE', #42002, #10117, #5280, .T. ) ;
#11840=CARTESIAN_POINT ( 'NONE',  ( -3.000000000000000000, 14.60985201121704513, 18.46759930825707841 ) ) ;
#11845=ORIENTED_EDGE ( 'NONE', *, *, #3025, .F. ) ;
#11850=VECTOR ( 'NONE', #28600, 1000.000000000000000 ) ;
#11854=CARTESIAN_POINT ( 'NONE',  ( 0.000000000000000000, -3.948201729842038432, -23.21447184625298021 ) ) ;
#11857=DIRECTION ( 'NONE',  ( 0.000000000000000000, -0.1564344650402170744, -0.9876883405951398798 ) ) ;
#11865=VECTOR ( 'NONE', #46323, 1000.000000000000000 ) ;
#11867=AXIS2_PLACEMENT_3D ( 'NONE', #31927, #16493, #42434 ) ;
#11870=ORIENTED_EDGE ( 'NONE', *, *, #15708, .T. ) ;
#11871=EDGE_CURVE ( 'NONE', #962, #12545, #44838, .T. ) ;
#11877=VERTEX_POINT ( 'NONE', #26726 ) ;
#11878=EDGE_CURVE ( 'NONE', #9789, #25227, #1364, .T. ) ;
#11882=CARTESIAN_POINT ( 'NONE',  ( 0.000000000000000000, 0.000000000000000000, 0.000000000000000000 ) ) ;
#11889=CARTESIAN_POINT ( 'NONE',  ( 10.00000000000000000, -4.992566952385247170, 37.16516213103275845 ) ) ;
#11892=ORIENTED_EDGE ( 'NONE', *, *, #562, .F. ) ;
#11916=CARTESIAN_POINT ( 'NONE',  ( 0.000000000000000000, -40.98264845739743123, -9.188173127307734944 ) ) ;
#11923=CARTESIAN_POINT ( 'NONE',  ( 0.000000000000000000, -36.13751322684404244, -21.40280677340410165 ) ) ;
#11931=VECTOR ( 'NONE', #11311, 1000.000000000000114 ) ;
#11936=DIRECTION ( 'NONE',  ( -1.000000000000000000, -0.000000000000000000, 0.000000000000000000 ) ) ;
#11941=VECTOR ( 'NONE', #17014, 1000.000000000000000 ) ;
#11944=ORIENTED_EDGE ( 'NONE', *, *, #47314, .T. ) ;
#11948=DIRECTION ( 'NONE',  ( -1.000000000000000000, -0.000000000000000000, -0.000000000000000000 ) ) ;
#11949=LINE ( 'NONE', #4599, #28174 ) ;
#11961=VERTEX_POINT ( 'NONE', #30169 ) ;
#11972=DIRECTION ( 'NONE',  ( 0.000000000000000000, 0.000000000000000000, 1.000000000000000000 ) ) ;
#11974=PLANE ( 'NONE',  #21630 ) ;
#11985=CARTESIAN_POINT ( 'NONE',  ( 10.00000000000000000, -30.00120703465189465, -22.64427369931201639 ) ) ;
#11987=CARTESIAN_POINT ( 'NONE',  ( 5.000000000000000000, 15.48615015657637706, -39.04073710021327770 ) ) ;
#11990=DIRECTION ( 'NONE',  ( 0.000000000000000000, 0.9135454576426063067, -0.4067366430757881068 ) ) ;
#12005=CIRCLE ( 'NONE', #40938, 16.00000000000000355 ) ;
#12018=AXIS2_PLACEMENT_3D ( 'NONE', #39904, #32319, #28160 ) ;
#12025=EDGE_LOOP ( 'NONE', ( #5930, #35363, #45987, #1111 ) ) ;
#12042=CARTESIAN_POINT ( 'NONE',  ( 10.00000000000000000, 35.38097989696512968, 12.42422080174651100 ) ) ;
#12045=AXIS2_PLACEMENT_3D ( 'NONE', #13289, #1552, #9597 ) ;
#12058=EDGE_CURVE ( 'NONE', #19561, #19028, #34782, .T. ) ;
#12062=CIRCLE ( 'NONE', #5014, 42.00000000000000000 ) ;
#12067=VECTOR ( 'NONE', #33528, 1000.000000000000000 ) ;
#12070=CARTESIAN_POINT ( 'NONE',  ( -3.000000000000000000, 26.50000000000000000, -1.500000000000001332 ) ) ;
#12077=VECTOR ( 'NONE', #21765, 1000.000000000000000 ) ;
#12088=CARTESIAN_POINT ( 'NONE',  ( 4.999999999999999112, -40.98264845739743123, -9.188173127307734944 ) ) ;
#12091=AXIS2_PLACEMENT_3D ( 'NONE', #4692, #15710, #45095 ) ;
#12093=CARTESIAN_POINT ( 'NONE',  ( 0.000000000000000000, 0.000000000000000000, 0.000000000000000000 ) ) ;
#12094=VERTEX_POINT ( 'NONE', #31378 ) ;
#12097=DIRECTION ( 'NONE',  ( -1.000000000000000000, 0.000000000000000000, 0.000000000000000000 ) ) ;
#12102=ORIENTED_EDGE ( 'NONE', *, *, #11357, .F. ) ;
#12107=FACE_OUTER_BOUND ( 'NONE', #23588, .T. ) ;
#12112=CYLINDRICAL_SURFACE ( 'NONE', #20824, 16.00000000000000000 ) ;
#12114=DIRECTION ( 'NONE',  ( 1.000000000000000000, -0.000000000000000000, -0.000000000000000000 ) ) ;
#12118=EDGE_CURVE ( 'NONE', #38854, #5281, #38723, .T. ) ;
#12127=EDGE_CURVE ( 'NONE', #32836, #43777, #4687, .T. ) ;
#12129=ORIENTED_EDGE ( 'NONE', *, *, #20536, .T. ) ;
#12132=VERTEX_POINT ( 'NONE', #37625 ) ;
#12141=DIRECTION ( 'NONE',  ( -1.000000000000000000, 0.000000000000000000, -0.000000000000000000 ) ) ;
#12148=ORIENTED_EDGE ( 'NONE', *, *, #43818, .F. ) ;
#12152=VERTEX_POINT ( 'NONE', #11923 ) ;
#12177=LINE ( 'NONE', #1387, #15916 ) ;
#12184=EDGE_CURVE ( 'NONE', #15589, #994, #34913, .T. ) ;
#12195=CARTESIAN_POINT ( 'NONE',  ( 0.000000000000000000, 18.84667830672605859, -18.68964196561243796 ) ) ;
#12196=ORIENTED_EDGE ( 'NONE', *, *, #4775, .T. ) ;
#12197=CIRCLE ( 'NONE', #41899, 42.00000000000000000 ) ;
#12200=DIRECTION ( 'NONE',  ( 1.000000000000000000, 0.000000000000000000, -0.000000000000000000 ) ) ;
#12203=VERTEX_POINT ( 'NONE', #15834 ) ;
#12218=CIRCLE ( 'NONE', #23953, 21.00000000000000000 ) ;
#12224=ORIENTED_EDGE ( 'NONE', *, *, #31921, .F. ) ;
#12231=EDGE_CURVE ( 'NONE', #23219, #30321, #31102, .T. ) ;
#12236=CIRCLE ( 'NONE', #30191, 37.49900000000000944 ) ;
#12241=ORIENTED_EDGE ( 'NONE', *, *, #38770, .F. ) ;
#12245=VERTEX_POINT ( 'NONE', #33941 ) ;
#12251=CARTESIAN_POINT ( 'NONE',  ( 0.000000000000000000, 16.45098606841173705, -33.79645857604496229 ) ) ;
#12259=ORIENTED_EDGE ( 'NONE', *, *, #34403, .T. ) ;
#12261=VERTEX_POINT ( 'NONE', #15592 ) ;
#12266=DIRECTION ( 'NONE',  ( -0.000000000000000000, 0.2079116908177543743, 0.9781476007338066880 ) ) ;
#12270=CARTESIAN_POINT ( 'NONE',  ( 0.000000000000000000, 0.000000000000000000, 0.000000000000000000 ) ) ;
#12277=CARTESIAN_POINT ( 'NONE',  ( 0.000000000000000000, 0.000000000000000000, 0.000000000000000000 ) ) ;
#12285=DIRECTION ( 'NONE',  ( 1.000000000000000000, -0.000000000000000000, -0.000000000000000000 ) ) ;
#12291=EDGE_CURVE ( 'NONE', #16979, #41890, #6034, .T. ) ;
#12298=DIRECTION ( 'NONE',  ( 0.000000000000000000, 0.000000000000000000, 1.000000000000000000 ) ) ;
#12300=ADVANCED_FACE ( 'NONE', ( #46670 ), #9208, .F. ) ;
#12306=LINE ( 'NONE', #46554, #37767 ) ;
#12315=EDGE_CURVE ( 'NONE', #24628, #6878, #12842, .T. ) ;
#12332=DIRECTION ( 'NONE',  ( 0.000000000000000000, 0.6691306063588563502, 0.7431448254773960205 ) ) ;
#12339=DIRECTION ( 'NONE',  ( -1.000000000000000000, 0.000000000000000000, 0.000000000000000000 ) ) ;
#12347=PRESENTATION_STYLE_ASSIGNMENT (( #4747 ) ) ;
#12357=ORIENTED_EDGE ( 'NONE', *, *, #13825, .T. ) ;
#12358=DIRECTION ( 'NONE',  ( 0.000000000000000000, -0.8910065241883722287, 0.4539904997395382558 ) ) ;
#12359=CARTESIAN_POINT ( 'NONE',  ( 10.00000000000000000, 0.000000000000000000, 0.000000000000000000 ) ) ;
#12360=ORIENTED_EDGE ( 'NONE', *, *, #20386, .F. ) ;
#12365=ORIENTED_EDGE ( 'NONE', *, *, #17529, .T. ) ;
#12368=ORIENTED_EDGE ( 'NONE', *, *, #15473, .F. ) ;
#12376=ORIENTED_EDGE ( 'NONE', *, *, #31970, .F. ) ;
#12378=CARTESIAN_POINT ( 'NONE',  ( 10.00000000000000000, 27.05870788708267582, -26.08949754952995903 ) ) ;
#12381=VERTEX_POINT ( 'NONE', #35641 ) ;
#12389=CARTESIAN_POINT ( 'NONE',  ( 0.000000000000000000, 0.000000000000000000, 0.000000000000000000 ) ) ;
#12394=ORIENTED_EDGE ( 'NONE', *, *, #48389, .F. ) ;
#12408=DIRECTION ( 'NONE',  ( 1.000000000000000000, 0.000000000000000000, 0.000000000000000000 ) ) ;
#12411=EDGE_LOOP ( 'NONE', ( #13626, #32475, #18789, #13425 ) ) ;
#12415=CARTESIAN_POINT ( 'NONE',  ( 10.00000000000000000, -37.16516213103280108, 4.992566952384862589 ) ) ;
#12431=LINE ( 'NONE', #8739, #18606 ) ;
#12435=ORIENTED_EDGE ( 'NONE', *, *, #46852, .T. ) ;
#12447=EDGE_CURVE ( 'NONE', #23509, #1910, #22144, .T. ) ;
#12463=CARTESIAN_POINT ( 'NONE',  ( 10.00000000000000000, 37.58145647212453611, 16.68533520207917675 ) ) ;
#12465=CARTESIAN_POINT ( 'NONE',  ( 10.00000000000000000, 0.000000000000000000, 0.000000000000000000 ) ) ;
#12469=CARTESIAN_POINT ( 'NONE',  ( 10.00000000000000000, -12.26510123303284594, 35.53030884539080603 ) ) ;
#12471=VERTEX_POINT ( 'NONE', #10896 ) ;
#12479=EDGE_CURVE ( 'NONE', #911, #9557, #36358, .T. ) ;
#12480=CARTESIAN_POINT ( 'NONE',  ( 0.000000000000000000, -5.202137450156655518, 37.22597642581156663 ) ) ;
#12494=VERTEX_POINT ( 'NONE', #21897 ) ;
#12498=DIRECTION ( 'NONE',  ( -1.000000000000000000, 0.000000000000000000, 0.000000000000000000 ) ) ;
#12506=CARTESIAN_POINT ( 'NONE',  ( 10.00000000000000000, 0.000000000000000000, 0.000000000000000000 ) ) ;
#12507=ORIENTED_EDGE ( 'NONE', *, *, #26075, .F. ) ;
#12521=CARTESIAN_POINT ( 'NONE',  ( 10.00000000000000000, -26.79245525562691199, -32.34446384430000876 ) ) ;
#12522=DIRECTION ( 'NONE',  ( -1.000000000000000000, 0.000000000000000000, -0.000000000000000000 ) ) ;
#12525=SHAPE_REPRESENTATION ( 'fast gear_ISO - Spur gear 2M 40T 20PA 10FW ---S40A75H50L38.0N', ( #11636 ), #21829 ) ;
#12526=FACE_OUTER_BOUND ( 'NONE', #2852, .T. ) ;
#12527=PLANE ( 'NONE',  #12091 ) ;
#12533=CIRCLE ( 'NONE', #39879, 37.49900000000000233 ) ;
#12535=CARTESIAN_POINT ( 'NONE',  ( 10.00000000000000000, 4.992566952385523393, -37.16516213103272293 ) ) ;
#12545=VERTEX_POINT ( 'NONE', #10409 ) ;
#12558=FACE_OUTER_BOUND ( 'NONE', #24927, .T. ) ;
#12563=ORIENTED_EDGE ( 'NONE', *, *, #30627, .T. ) ;
#12566=AXIS2_PLACEMENT_3D ( 'NONE', #46828, #27754, #39236 ) ;
#12567=VECTOR ( 'NONE', #6882, 1000.000000000000000 ) ;
#12574=VECTOR ( 'NONE', #18859, 1000.000000000000000 ) ;
#12605=CIRCLE ( 'NONE', #3901, 16.00000000000000000 ) ;
#12631=CIRCLE ( 'NONE', #3245, 15.99999999999999822 ) ;
#12641=CARTESIAN_POINT ( 'NONE',  ( 5.000000000000000000, -35.47612816024539484, 22.48208911017487921 ) ) ;
#12647=FACE_OUTER_BOUND ( 'NONE', #20659, .T. ) ;
#12661=VERTEX_POINT ( 'NONE', #22868 ) ;
#12664=EDGE_CURVE ( 'NONE', #16286, #4226, #3464, .T. ) ;
#12666=AXIS2_PLACEMENT_3D ( 'NONE', #40432, #2484, #17659 ) ;
#12672=DIRECTION ( 'NONE',  ( 0.000000000000000000, 0.000000000000000000, 1.000000000000000000 ) ) ;
#12679=ORIENTED_EDGE ( 'NONE', *, *, #28082, .F. ) ;
#12685=DIRECTION ( 'NONE',  ( -1.000000000000000000, 0.000000000000000000, 0.000000000000000000 ) ) ;
#12708=AXIS2_PLACEMENT_3D ( 'NONE', #48436, #25672, #7808 ) ;
#12709=VERTEX_POINT ( 'NONE', #34850 ) ;
#12710=CARTESIAN_POINT ( 'NONE',  ( -3.000000000000000000, -0.9646360437375307573, 23.52805723605590060 ) ) ;
#12711=EDGE_CURVE ( 'NONE', #16717, #5383, #7700, .T. ) ;
#12712=ORIENTED_EDGE ( 'NONE', *, *, #11871, .F. ) ;
#12724=ORIENTED_EDGE ( 'NONE', *, *, #39541, .F. ) ;
#12732=ORIENTED_EDGE ( 'NONE', *, *, #38131, .F. ) ;
#12734=CIRCLE ( 'NONE', #8802, 42.00000000000000000 ) ;
#12736=CARTESIAN_POINT ( 'NONE',  ( -3.000000000000000000, -4.261787119644969479, -26.19803753235780519 ) ) ;
#12737=CARTESIAN_POINT ( 'NONE',  ( 10.00000000000000000, 0.000000000000000000, 0.000000000000000000 ) ) ;
#12750=VECTOR ( 'NONE', #27288, 1000.000000000000000 ) ;
#12751=CARTESIAN_POINT ( 'NONE',  ( 10.00000000000000000, -9.188173127307592836, 40.98264845739746676 ) ) ;
#12754=CARTESIAN_POINT ( 'NONE',  ( 10.00000000000000000, -6.736453364083292428, -36.88895765772640800 ) ) ;
#12761=EDGE_CURVE ( 'NONE', #5067, #42424, #44914, .T. ) ;
#12778=EDGE_LOOP ( 'NONE', ( #18955, #21842, #14482, #33443 ) ) ;
#12780=EDGE_CURVE ( 'NONE', #14949, #37649, #27518, .T. ) ;
#12784=FACE_OUTER_BOUND ( 'NONE', #2354, .T. ) ;
#12794=ORIENTED_EDGE ( 'NONE', *, *, #21056, .T. ) ;
#12797=DIRECTION ( 'NONE',  ( 1.000000000000000000, 0.000000000000000000, -0.000000000000000000 ) ) ;
#12798=CARTESIAN_POINT ( 'NONE',  ( 10.00000000000000000, -37.22597642581161637, 5.202137450156258502 ) ) ;
#12800=AXIS2_PLACEMENT_3D ( 'NONE', #13908, #28830, #43294 ) ;
#12802=ORIENTED_EDGE ( 'NONE', *, *, #12118, .T. ) ;
#12819=EDGE_CURVE ( 'NONE', #22743, #23433, #358, .T. ) ;
#12820=AXIS2_PLACEMENT_3D ( 'NONE', #6397, #36249, #17647 ) ;
#12821=VECTOR ( 'NONE', #3486, 1000.000000000000000 ) ;
#12842=CIRCLE ( 'NONE', #27698, 42.00000000000000000 ) ;
#12854=DIRECTION ( 'NONE',  ( -0.000000000000000000, -0.2079116908177653378, 0.9781476007338044676 ) ) ;
#12865=EDGE_LOOP ( 'NONE', ( #360, #20280, #42560, #25164 ) ) ;
#12874=CARTESIAN_POINT ( 'NONE',  ( 5.000000000000000000, -39.04073710021356192, 15.48615015657568073 ) ) ;
#12888=EDGE_CURVE ( 'NONE', #7136, #6878, #32410, .T. ) ;
#12893=AXIS2_PLACEMENT_3D ( 'NONE', #25094, #35876, #10168 ) ;
#12899=CARTESIAN_POINT ( 'NONE',  ( 10.00000000000000000, 0.000000000000000000, 0.000000000000000000 ) ) ;
#12901=CIRCLE ( 'NONE', #35565, 16.00000000000000000 ) ;
#12902=ORIENTED_EDGE ( 'NONE', *, *, #35405, .F. ) ;
#12903=CARTESIAN_POINT ( 'NONE',  ( 0.000000000000000000, 0.000000000000000000, 0.000000000000000000 ) ) ;
#12915=AXIS2_PLACEMENT_3D ( 'NONE', #21880, #18457, #86 ) ;
#12923=DIRECTION ( 'NONE',  ( -1.000000000000000000, 0.000000000000000000, 0.000000000000000000 ) ) ;
#12927=DIRECTION ( 'NONE',  ( -1.000000000000000000, 0.000000000000000000, -0.000000000000000000 ) ) ;
#12928=VERTEX_POINT ( 'NONE', #40470 ) ;
#12939=AXIS2_PLACEMENT_3D ( 'NONE', #37171, #3141, #18323 ) ;
#12959=DIRECTION ( 'NONE',  ( 0.000000000000000000, 0.000000000000000000, 1.000000000000000000 ) ) ;
#12972=CIRCLE ( 'NONE', #30161, 16.00000000000000355 ) ;
#12976=EDGE_LOOP ( 'NONE', ( #717, #13098, #30977, #42853 ) ) ;
#12977=CIRCLE ( 'NONE', #46591, 37.49900000000001654 ) ;
#12978=ORIENTED_EDGE ( 'NONE', *, *, #36932, .T. ) ;
#12990=ORIENTED_EDGE ( 'NONE', *, *, #11015, .F. ) ;
#12999=EDGE_CURVE ( 'NONE', #956, #17342, #7162, .T. ) ;
#13002=ORIENTED_EDGE ( 'NONE', *, *, #39937, .F. ) ;
#13007=ORIENTED_EDGE ( 'NONE', *, *, #38456, .F. ) ;
#13011=CARTESIAN_POINT ( 'NONE',  ( 10.00000000000000000, -6.555932627142143865, -37.01155633439065440 ) ) ;
#13031=CIRCLE ( 'NONE', #46636, 16.00000000000000000 ) ;
#13033=CARTESIAN_POINT ( 'NONE',  ( 10.00000000000000000, -35.92658777277517856, 10.74501242461269257 ) ) ;
#13036=EDGE_CURVE ( 'NONE', #28215, #26631, #4471, .T. ) ;
#13039=DIRECTION ( 'NONE',  ( 0.000000000000000000, 0.000000000000000000, 1.000000000000000000 ) ) ;
#13049=DIRECTION ( 'NONE',  ( 0.000000000000000000, -0.3090169943749548342, 0.9510565162951511997 ) ) ;
#13073=FACE_OUTER_BOUND ( 'NONE', #6281, .T. ) ;
#13080=DIRECTION ( 'NONE',  ( 0.000000000000000000, 0.000000000000000000, 1.000000000000000000 ) ) ;
#13095=CARTESIAN_POINT ( 'NONE',  ( -3.000000000000000000, 14.60985201121729737, -18.46759930825687945 ) ) ;
#13096=EDGE_LOOP ( 'NONE', ( #18894, #28701, #24154, #9692 ) ) ;
#13098=ORIENTED_EDGE ( 'NONE', *, *, #11228, .F. ) ;
#13101=CARTESIAN_POINT ( 'NONE',  ( 10.00000000000000000, 22.74946021919133088, 29.81001611431016229 ) ) ;
#13107=FACE_OUTER_BOUND ( 'NONE', #42765, .T. ) ;
#13108=LINE ( 'NONE', #16781, #45681 ) ;
#13113=DIRECTION ( 'NONE',  ( 1.000000000000000000, 0.000000000000000000, 0.000000000000000000 ) ) ;
#13117=CARTESIAN_POINT ( 'NONE',  ( -3.000000000000000000, 14.60985201121704513, 18.46759930825707841 ) ) ;
#13128=EDGE_CURVE ( 'NONE', #844, #17342, #12005, .T. ) ;
#13130=CARTESIAN_POINT ( 'NONE',  ( 0.000000000000000000, 0.000000000000000000, 0.000000000000000000 ) ) ;
#13138=ORIENTED_EDGE ( 'NONE', *, *, #770, .F. ) ;
#13139=EDGE_LOOP ( 'NONE', ( #7482, #21531, #26753, #19634 ) ) ;
#13149=VERTEX_POINT ( 'NONE', #23781 ) ;
#13151=LINE ( 'NONE', #27357, #39735 ) ;
#13154=CYLINDRICAL_SURFACE ( 'NONE', #39190, 21.00000000000000000 ) ;
#13156=ORIENTED_EDGE ( 'NONE', *, *, #33765, .F. ) ;
#13161=FACE_OUTER_BOUND ( 'NONE', #20605, .T. ) ;
#13171=FACE_OUTER_BOUND ( 'NONE', #38080, .T. ) ;
#13181=VERTEX_POINT ( 'NONE', #27958 ) ;
#13187=CARTESIAN_POINT ( 'NONE',  ( -3.000000000000000000, -1.278221433540145391, -26.51162292216073979 ) ) ;
#13199=CARTESIAN_POINT ( 'NONE',  ( 0.000000000000000000, 2.571758278209441661E-15, -21.00000000000000000 ) ) ;
#13202=ADVANCED_FACE ( 'NONE', ( #2228 ), #35525, .T. ) ;
#13209=ORIENTED_EDGE ( 'NONE', *, *, #44991, .T. ) ;
#13210=PRODUCT ( 'fast gear_ISO - Spur gear 2M 40T 20PA 10FW ---S40A75H50L38.0N', 'fast gear_ISO - Spur gear 2M 40T 20PA 10FW ---S40A75H50L38.0N', '', ( #23787 ) ) ;
#13215=EDGE_LOOP ( 'NONE', ( #22049, #4956, #14430, #47154 ) ) ;
#13228=CARTESIAN_POINT ( 'NONE',  ( 0.000000000000000000, -21.32104025579091910, -30.84782396557241313 ) ) ;
#13241=ADVANCED_FACE ( 'NONE', ( #1279 ), #46300, .T. ) ;
#13243=LINE ( 'NONE', #39188, #31790 ) ;
#13247=ADVANCED_FACE ( 'NONE', ( #25876 ), #426, .T. ) ;
#13250=VERTEX_POINT ( 'NONE', #3113 ) ;
#13254=DIRECTION ( 'NONE',  ( -1.000000000000000000, -0.000000000000000000, -0.000000000000000000 ) ) ;
#13268=ADVANCED_FACE ( 'NONE', ( #44252 ), #21731, .F. ) ;
#13276=ORIENTED_EDGE ( 'NONE', *, *, #1446, .F. ) ;
#13285=VERTEX_POINT ( 'NONE', #15123 ) ;
#13286=ORIENTED_EDGE ( 'NONE', *, *, #7045, .F. ) ;
#13288=ORIENTED_EDGE ( 'NONE', *, *, #15138, .F. ) ;
#13289=CARTESIAN_POINT ( 'NONE',  ( 10.00000000000000000, 0.000000000000000000, 0.000000000000000000 ) ) ;
#13296=CARTESIAN_POINT ( 'NONE',  ( -3.000000000000000000, 0.000000000000000000, 0.000000000000000000 ) ) ;
#13298=CYLINDRICAL_SURFACE ( 'NONE', #31777, 16.00000000000000000 ) ;
#13301=VECTOR ( 'NONE', #8672, 1000.000000000000000 ) ;
#13306=CIRCLE ( 'NONE', #29708, 15.99999999999999467 ) ;
#13316=ORIENTED_EDGE ( 'NONE', *, *, #23833, .F. ) ;
#13318=ORIENTED_EDGE ( 'NONE', *, *, #6102, .T. ) ;
#13324=ORIENTED_EDGE ( 'NONE', *, *, #28393, .T. ) ;
#13325=LINE ( 'NONE', #24102, #23716 ) ;
#13331=ORIENTED_EDGE ( 'NONE', *, *, #32293, .T. ) ;
#13338=AXIS2_PLACEMENT_3D ( 'NONE', #1315, #39235, #46100 ) ;
#13360=LINE ( 'NONE', #46414, #33459 ) ;
#13366=ORIENTED_EDGE ( 'NONE', *, *, #27370, .T. ) ;
#13380=ADVANCED_FACE ( 'NONE', ( #29560 ), #10959, .T. ) ;
#13382=ORIENTED_EDGE ( 'NONE', *, *, #5024, .T. ) ;
#13385=ORIENTED_EDGE ( 'NONE', *, *, #46869, .F. ) ;
#13393=DIRECTION ( 'NONE',  ( 0.000000000000000000, -0.8090169943749531134, 0.5877852522924653655 ) ) ;
#13394=CIRCLE ( 'NONE', #26676, 16.00000000000000000 ) ;
#13417=CARTESIAN_POINT ( 'NONE',  ( -10.00000000000000000, 0.000000000000000000, 0.000000000000000000 ) ) ;
#13425=ORIENTED_EDGE ( 'NONE', *, *, #47465, .T. ) ;
#13433=VECTOR ( 'NONE', #27013, 1000.000000000000000 ) ;
#13439=AXIS2_PLACEMENT_3D ( 'NONE', #47644, #13893, #2157 ) ;
#13453=DIRECTION ( 'NONE',  ( 0.000000000000000000, 0.000000000000000000, -1.000000000000000000 ) ) ;
#13454=ORIENTED_EDGE ( 'NONE', *, *, #12819, .F. ) ;
#13457=DIRECTION ( 'NONE',  ( 0.000000000000000000, -0.5877852522924624790, -0.8090169943749552228 ) ) ;
#13463=VERTEX_POINT ( 'NONE', #26856 ) ;
#13468=DIRECTION ( 'NONE',  ( -1.000000000000000000, -0.000000000000000000, -0.000000000000000000 ) ) ;
#13471=CARTESIAN_POINT ( 'NONE',  ( 10.00000000000000000, 0.000000000000000000, 0.000000000000000000 ) ) ;
#13480=EDGE_CURVE ( 'NONE', #17719, #26953, #41794, .T. ) ;
#13488=DIRECTION ( 'NONE',  ( 0.000000000000000000, -0.1045284632676429099, -0.9945218953682744001 ) ) ;
#13489=VECTOR ( 'NONE', #38154, 1000.000000000000000 ) ;
#13493=AXIS2_PLACEMENT_3D ( 'NONE', #5475, #42691, #4750 ) ;
#13495=CIRCLE ( 'NONE', #40851, 37.49900000000000944 ) ;
#13503=AXIS2_PLACEMENT_3D ( 'NONE', #42922, #20384, #8893 ) ;
#13504=EDGE_CURVE ( 'NONE', #20013, #45931, #43177, .T. ) ;
#13505=CARTESIAN_POINT ( 'NONE',  ( 10.00000000000000000, 0.000000000000000000, 0.000000000000000000 ) ) ;
#13509=DIRECTION ( 'NONE',  ( -1.000000000000000000, -0.000000000000000000, -0.000000000000000000 ) ) ;
#13518=ORIENTED_EDGE ( 'NONE', *, *, #3518, .F. ) ;
#13526=ORIENTED_EDGE ( 'NONE', *, *, #13878, .F. ) ;
#13530=DIRECTION ( 'NONE',  ( -1.000000000000000000, -0.000000000000000000, -0.000000000000000000 ) ) ;
#13539=CIRCLE ( 'NONE', #22929, 42.00000000000000000 ) ;
#13542=DIRECTION ( 'NONE',  ( -1.000000000000000000, -0.000000000000000000, -0.000000000000000000 ) ) ;
#13551=DIRECTION ( 'NONE',  ( -1.000000000000000000, -0.000000000000000000, 0.000000000000000000 ) ) ;
#13561=DIRECTION ( 'NONE',  ( 0.000000000000000000, 0.000000000000000000, -1.000000000000000000 ) ) ;
#13570=ORIENTED_EDGE ( 'NONE', *, *, #37346, .F. ) ;
#13576=ORIENTED_EDGE ( 'NONE', *, *, #44478, .T. ) ;
#13580=DIRECTION ( 'NONE',  ( 0.000000000000000000, 0.000000000000000000, -1.000000000000000000 ) ) ;
#13587=DIRECTION ( 'NONE',  ( -1.000000000000000000, -0.000000000000000000, -0.000000000000000000 ) ) ;
#13588=CARTESIAN_POINT ( 'NONE',  ( 10.00000000000000000, 33.00180498840046539, 17.80606268964551120 ) ) ;
#13613=ORIENTED_EDGE ( 'NONE', *, *, #19332, .T. ) ;
#13614=AXIS2_PLACEMENT_3D ( 'NONE', #32397, #5721, #25030 ) ;
#13619=CARTESIAN_POINT ( 'NONE',  ( -3.000000000000000000, -18.13022148937263012, 15.02647892043544608 ) ) ;
#13626=ORIENTED_EDGE ( 'NONE', *, *, #46637, .F. ) ;
#13628=AXIS2_PLACEMENT_3D ( 'NONE', #18647, #27392, #37496 ) ;
#13640=DIRECTION ( 'NONE',  ( 0.000000000000000000, 0.000000000000000000, 1.000000000000000000 ) ) ;
#13649=EDGE_CURVE ( 'NONE', #45643, #994, #23639, .T. ) ;
#13655=CIRCLE ( 'NONE', #3483, 16.00000000000000000 ) ;
#13657=ORIENTED_EDGE ( 'NONE', *, *, #23488, .F. ) ;
#13673=DIRECTION ( 'NONE',  ( -1.000000000000000000, -0.000000000000000000, 0.000000000000000000 ) ) ;
#13676=ORIENTED_EDGE ( 'NONE', *, *, #41461, .T. ) ;
#13708=EDGE_LOOP ( 'NONE', ( #46471, #5347, #12196, #6526 ) ) ;
#13711=CARTESIAN_POINT ( 'NONE',  ( 0.000000000000000000, 0.000000000000000000, 0.000000000000000000 ) ) ;
#13725=ORIENTED_EDGE ( 'NONE', *, *, #3025, .T. ) ;
#13734=VECTOR ( 'NONE', #41759, 999.9999999999998863 ) ;
#13739=ORIENTED_EDGE ( 'NONE', *, *, #31180, .F. ) ;
#13741=DIRECTION ( 'NONE',  ( -1.000000000000000000, 0.000000000000000000, 0.000000000000000000 ) ) ;
#13751=VERTEX_POINT ( 'NONE', #48340 ) ;
#13756=ORIENTED_EDGE ( 'NONE', *, *, #47465, .F. ) ;
#13761=EDGE_CURVE ( 'NONE', #33430, #41296, #41641, .T. ) ;
#13767=FACE_OUTER_BOUND ( 'NONE', #33389, .T. ) ;
#13768=DIRECTION ( 'NONE',  ( -1.000000000000000000, 0.000000000000000000, -0.000000000000000000 ) ) ;
#13771=CARTESIAN_POINT ( 'NONE',  ( 10.00000000000000000, -12.26510123303234501, -35.53030884539098366 ) ) ;
#13773=LINE ( 'NONE', #28700, #48267 ) ;
#13775=ORIENTED_EDGE ( 'NONE', *, *, #5451, .F. ) ;
#13777=DIRECTION ( 'NONE',  ( -1.000000000000000000, -0.000000000000000000, 0.000000000000000000 ) ) ;
#13778=VERTEX_POINT ( 'NONE', #29981 ) ;
#13786=DIRECTION ( 'NONE',  ( 0.000000000000000000, 0.000000000000000000, 1.000000000000000000 ) ) ;
#13787=CARTESIAN_POINT ( 'NONE',  ( 0.000000000000000000, -16.23288003029473359, -33.80338159004301701 ) ) ;
#13791=CARTESIAN_POINT ( 'NONE',  ( 0.000000000000000000, -12.42422080174663712, 35.38097989696507994 ) ) ;
#13793=DIRECTION ( 'NONE',  ( -1.000000000000000000, 0.000000000000000000, 0.000000000000000000 ) ) ;
#13810=DIRECTION ( 'NONE',  ( -1.000000000000000000, -0.000000000000000000, -0.000000000000000000 ) ) ;
#13817=EDGE_LOOP ( 'NONE', ( #4967, #12360, #35609, #20466 ) ) ;
#13823=DIRECTION ( 'NONE',  ( 1.000000000000000000, 0.000000000000000000, 0.000000000000000000 ) ) ;
#13825=EDGE_CURVE ( 'NONE', #25099, #37634, #19430, .T. ) ;
#13828=DIRECTION ( 'NONE',  ( 0.000000000000000000, 0.9945218953682742891, -0.1045284632676436315 ) ) ;
#13837=FACE_BOUND ( 'NONE', #46428, .T. ) ;
#13838=AXIS2_PLACEMENT_3D ( 'NONE', #939, #34233, #26910 ) ;
#13839=DIRECTION ( 'NONE',  ( 0.000000000000000000, -0.5877852522924689183, -0.8090169943749504489 ) ) ;
#13848=EDGE_LOOP ( 'NONE', ( #30267, #37173, #17096, #4700 ) ) ;
#13849=AXIS2_PLACEMENT_3D ( 'NONE', #27035, #8420, #38280 ) ;
#13853=ORIENTED_EDGE ( 'NONE', *, *, #45342, .F. ) ;
#13859=VERTEX_POINT ( 'NONE', #34857 ) ;
#13861=EDGE_CURVE ( 'NONE', #28645, #40027, #6494, .T. ) ;
#13869=CYLINDRICAL_SURFACE ( 'NONE', #7804, 16.00000000000000000 ) ;
#13873=ADVANCED_FACE ( 'NONE', ( #22874 ), #8910, .T. ) ;
#13874=DIRECTION ( 'NONE',  ( 0.000000000000000000, 7.228014483236689653E-16, -1.000000000000000000 ) ) ;
#13878=EDGE_CURVE ( 'NONE', #15085, #28664, #833, .T. ) ;
#13881=CARTESIAN_POINT ( 'NONE',  ( 0.000000000000000000, -22.67460108101774807, -6.353146135318215038 ) ) ;
#13882=ORIENTED_EDGE ( 'NONE', *, *, #35868, .T. ) ;
#13889=DIRECTION ( 'NONE',  ( 0.000000000000000000, 0.6691306063588563502, 0.7431448254773960205 ) ) ;
#13893=DIRECTION ( 'NONE',  ( 0.000000000000000000, 0.8660254037844432595, -0.4999999999999920064 ) ) ;
#13895=ORIENTED_EDGE ( 'NONE', *, *, #38182, .T. ) ;
#13896=DIRECTION ( 'NONE',  ( 0.000000000000000000, -0.8660254037844363761, -0.5000000000000039968 ) ) ;
#13907=CARTESIAN_POINT ( 'NONE',  ( 10.00000000000000000, 0.000000000000000000, 0.000000000000000000 ) ) ;
#13908=CARTESIAN_POINT ( 'NONE',  ( 10.00000000000000000, 0.000000000000000000, 0.000000000000000000 ) ) ;
#13911=AXIS2_PLACEMENT_3D ( 'NONE', #26824, #41760, #34632 ) ;
#13923=EDGE_CURVE ( 'NONE', #9910, #30912, #41981, .T. ) ;
#13924=AXIS2_PLACEMENT_3D ( 'NONE', #42281, #16576, #28315 ) ;
#13929=DIRECTION ( 'NONE',  ( 0.000000000000000000, 0.000000000000000000, 1.000000000000000000 ) ) ;
#13931=DIRECTION ( 'NONE',  ( -1.000000000000000000, -0.000000000000000000, -0.000000000000000000 ) ) ;
#13941=LINE ( 'NONE', #28150, #14168 ) ;
#13945=DIRECTION ( 'NONE',  ( -1.000000000000000000, 0.000000000000000000, 0.000000000000000000 ) ) ;
#13952=DIRECTION ( 'NONE',  ( -0.000000000000000000, 0.9781476007338066880, -0.2079116908177543743 ) ) ;
#13954=CARTESIAN_POINT ( 'NONE',  ( 10.00000000000000000, -0.6853352020787742971, -37.58145647212455032 ) ) ;
#13958=CARTESIAN_POINT ( 'NONE',  ( 10.00000000000000000, 37.22597642581158084, 10.79786254984347593 ) ) ;
#13959=CARTESIAN_POINT ( 'NONE',  ( 0.000000000000000000, 0.000000000000000000, 0.000000000000000000 ) ) ;
#13963=EDGE_CURVE ( 'NONE', #15289, #20089, #20561, .T. ) ;
#13970=EDGE_CURVE ( 'NONE', #37389, #31548, #9880, .T. ) ;
#13980=FACE_OUTER_BOUND ( 'NONE', #32630, .T. ) ;
#13984=ORIENTED_EDGE ( 'NONE', *, *, #28959, .F. ) ;
#13989=FACE_OUTER_BOUND ( 'NONE', #19553, .T. ) ;
#13990=VERTEX_POINT ( 'NONE', #39756 ) ;
#14005=AXIS2_PLACEMENT_3D ( 'NONE', #17086, #46725, #5851 ) ;
#14009=ORIENTED_EDGE ( 'NONE', *, *, #30120, .T. ) ;
#14011=CARTESIAN_POINT ( 'NONE',  ( 0.000000000000000000, 33.79645857604513992, 16.45098606841138178 ) ) ;
#14031=AXIS2_PLACEMENT_3D ( 'NONE', #28787, #36839, #31996 ) ;
#14033=DIRECTION ( 'NONE',  ( -1.000000000000000000, 0.000000000000000000, -0.000000000000000000 ) ) ;
#14037=EDGE_LOOP ( 'NONE', ( #11704, #5366, #25167, #15778 ) ) ;
#14043=ORIENTED_EDGE ( 'NONE', *, *, #9055, .T. ) ;
#14056=CIRCLE ( 'NONE', #2346, 37.49900000000001654 ) ;
#14065=ORIENTED_EDGE ( 'NONE', *, *, #36734, .T. ) ;
#14080=CARTESIAN_POINT ( 'NONE',  ( 10.00000000000000000, -16.45098606841149902, 33.79645857604508308 ) ) ;
#14088=ORIENTED_EDGE ( 'NONE', *, *, #16762, .T. ) ;
#14095=ORIENTED_EDGE ( 'NONE', *, *, #16700, .F. ) ;
#14103=CIRCLE ( 'NONE', #39895, 21.00000000000000000 ) ;
#14109=VERTEX_POINT ( 'NONE', #25760 ) ;
#14110=ORIENTED_EDGE ( 'NONE', *, *, #38053, .F. ) ;
#14115=CARTESIAN_POINT ( 'NONE',  ( 50.00005079999999680, 0.000000000000000000, 0.000000000000000000 ) ) ;
#14119=CARTESIAN_POINT ( 'NONE',  ( -10.00000000000000000, 0.000000000000000000, 0.000000000000000000 ) ) ;
#14131=CARTESIAN_POINT ( 'NONE',  ( 10.00000000000000000, 26.08949754953062694, -27.05870788708203989 ) ) ;
#14132=ORIENTED_EDGE ( 'NONE', *, *, #11064, .F. ) ;
#14135=CIRCLE ( 'NONE', #16475, 37.49900000000000944 ) ;
#14136=AXIS2_PLACEMENT_3D ( 'NONE', #682, #37893, #3374 ) ;
#14137=LINE ( 'NONE', #10464, #30849 ) ;
#14140=AXIS2_PLACEMENT_3D ( 'NONE', #19110, #30149, #45071 ) ;
#14149=EDGE_CURVE ( 'NONE', #12471, #29523, #29684, .T. ) ;
#14152=( LENGTH_UNIT ( ) NAMED_UNIT ( * ) SI_UNIT ( .MILLI., .METRE. ) );
#14157=CARTESIAN_POINT ( 'NONE',  ( -10.00000000000000000, 0.000000000000000000, 0.000000000000000000 ) ) ;
#14168=VECTOR ( 'NONE', #24725, 1000.000000000000000 ) ;
#14185=DIRECTION ( 'NONE',  ( -1.000000000000000000, -0.000000000000000000, 0.000000000000000000 ) ) ;
#14190=DIRECTION ( 'NONE',  ( -1.000000000000000000, -0.000000000000000000, -0.000000000000000000 ) ) ;
#14193=CIRCLE ( 'NONE', #20440, 37.49900000000000944 ) ;
#14203=EDGE_CURVE ( 'NONE', #38112, #894, #3738, .T. ) ;
#14207=ORIENTED_EDGE ( 'NONE', *, *, #35521, .F. ) ;
#14214=CARTESIAN_POINT ( 'NONE',  ( 0.000000000000000000, -35.53030884539094103, 12.26510123303246935 ) ) ;
#14216=ORIENTED_EDGE ( 'NONE', *, *, #32634, .F. ) ;
#14218=ORIENTED_EDGE ( 'NONE', *, *, #10017, .T. ) ;
#14220=ORIENTED_EDGE ( 'NONE', *, *, #11006, .T. ) ;
#14228=DIRECTION ( 'NONE',  ( 0.000000000000000000, -0.8910065241883626808, -0.4539904997395570740 ) ) ;
#14230=CYLINDRICAL_SURFACE ( 'NONE', #12666, 42.00000000000000000 ) ;
#14232=ORIENTED_EDGE ( 'NONE', *, *, #42891, .F. ) ;
#14235=ADVANCED_FACE ( 'NONE', ( #21367 ), #44134, .F. ) ;
#14249=DIRECTION ( 'NONE',  ( 1.000000000000000000, 0.000000000000000000, -0.000000000000000000 ) ) ;
#14257=DIRECTION ( 'NONE',  ( 0.000000000000000000, 0.000000000000000000, -1.000000000000000000 ) ) ;
#14260=CARTESIAN_POINT ( 'NONE',  ( 0.000000000000000000, -35.38097989696503021, -12.42422080174676147 ) ) ;
#14261=DIRECTION ( 'NONE',  ( -0.000000000000000000, 0.5000000000000039968, -0.8660254037844363761 ) ) ;
#14264=EDGE_CURVE ( 'NONE', #7751, #1711, #19785, .T. ) ;
#14266=EDGE_CURVE ( 'NONE', #26114, #44403, #40146, .T. ) ;
#14272=ORIENTED_EDGE ( 'NONE', *, *, #34875, .F. ) ;
#14281=DIRECTION ( 'NONE',  ( 0.000000000000000000, -0.8090169943749508930, 0.5877852522924683631 ) ) ;
#14290=VERTEX_POINT ( 'NONE', #12070 ) ;
#14319=CARTESIAN_POINT ( 'NONE',  ( 0.000000000000000000, 10.41901085202078292, 40.68715046381932865 ) ) ;
#14335=VECTOR ( 'NONE', #7513, 1000.000000000000000 ) ;
#14336=VECTOR ( 'NONE', #7126, 1000.000000000000000 ) ;
#14338=CIRCLE ( 'NONE', #17438, 15.99999999999999822 ) ;
#14373=DIRECTION ( 'NONE',  ( 0.000000000000000000, 0.7431448254773862505, 0.6691306063588671194 ) ) ;
#14375=CIRCLE ( 'NONE', #12045, 37.49900000000000233 ) ;
#14386=DIRECTION ( 'NONE',  ( -1.000000000000000000, 0.000000000000000000, 0.000000000000000000 ) ) ;
#14401=DIRECTION ( 'NONE',  ( -1.000000000000000000, 0.000000000000000000, 0.000000000000000000 ) ) ;
#14403=ORIENTED_EDGE ( 'NONE', *, *, #39262, .F. ) ;
#14421=EDGE_CURVE ( 'NONE', #38747, #22486, #4947, .T. ) ;
#14425=VERTEX_POINT ( 'NONE', #23788 ) ;
#14428=CARTESIAN_POINT ( 'NONE',  ( 0.000000000000000000, 14.60985201121729737, -18.46759930825687945 ) ) ;
#14430=ORIENTED_EDGE ( 'NONE', *, *, #33524, .F. ) ;
#14432=EDGE_CURVE ( 'NONE', #20645, #18777, #29199, .T. ) ;
#14462=AXIS2_PLACEMENT_3D ( 'NONE', #34896, #16305, #8952 ) ;
#14470=ORIENTED_EDGE ( 'NONE', *, *, #7529, .F. ) ;
#14476=CIRCLE ( 'NONE', #12915, 37.49900000000000944 ) ;
#14481=CARTESIAN_POINT ( 'NONE',  ( 0.000000000000000000, -18.13022148937243472, -15.02647892043568767 ) ) ;
#14482=ORIENTED_EDGE ( 'NONE', *, *, #43818, .T. ) ;
#14483=DIRECTION ( 'NONE',  ( -1.000000000000000000, -0.000000000000000000, -0.000000000000000000 ) ) ;
#14485=CARTESIAN_POINT ( 'NONE',  ( 10.00000000000000000, -17.80606268964563554, 33.00180498840040855 ) ) ;
#14489=CIRCLE ( 'NONE', #41858, 16.00000000000000000 ) ;
#14490=VERTEX_POINT ( 'NONE', #27961 ) ;
#14506=FACE_OUTER_BOUND ( 'NONE', #32158, .T. ) ;
#14512=DIRECTION ( 'NONE',  ( -1.000000000000000000, 0.000000000000000000, -0.000000000000000000 ) ) ;
#14516=PLANE ( 'NONE',  #43627 ) ;
#14523=ORIENTED_EDGE ( 'NONE', *, *, #3242, .F. ) ;
#14534=EDGE_LOOP ( 'NONE', ( #41659, #28841, #12368, #4058 ) ) ;
#14535=EDGE_CURVE ( 'NONE', #26532, #31490, #42391, .T. ) ;
#14548=ORIENTED_EDGE ( 'NONE', *, *, #1708, .F. ) ;
#14549=EDGE_CURVE ( 'NONE', #8400, #12094, #3676, .T. ) ;
#14566=CYLINDRICAL_SURFACE ( 'NONE', #22899, 37.49900000000000233 ) ;
#14567=CARTESIAN_POINT ( 'NONE',  ( -3.000000000000000000, 22.07842321921492612, -8.187992925817130896 ) ) ;
#14569=CARTESIAN_POINT ( 'NONE',  ( 0.000000000000000000, 0.000000000000000000, 0.000000000000000000 ) ) ;
#14571=ORIENTED_EDGE ( 'NONE', *, *, #36714, .F. ) ;
#14584=VECTOR ( 'NONE', #10834, 1000.000000000000000 ) ;
#14586=DIRECTION ( 'NONE',  ( 0.000000000000000000, 0.000000000000000000, 1.000000000000000000 ) ) ;
#14592=EDGE_CURVE ( 'NONE', #37265, #962, #22169, .T. ) ;
#14619=FACE_OUTER_BOUND ( 'NONE', #31455, .T. ) ;
#14620=CARTESIAN_POINT ( 'NONE',  ( 0.000000000000000000, 14.60985201121704513, 18.46759930825707841 ) ) ;
#14622=DIRECTION ( 'NONE',  ( 1.000000000000000000, 0.000000000000000000, -0.000000000000000000 ) ) ;
#14624=DIRECTION ( 'NONE',  ( -1.000000000000000000, -0.000000000000000000, 0.000000000000000000 ) ) ;
#14627=AXIS2_PLACEMENT_3D ( 'NONE', #9500, #21958, #25147 ) ;
#14630=PLANE ( 'NONE',  #21777 ) ;
#14637=DIRECTION ( 'NONE',  ( 0.000000000000000000, -0.8090169943749403458, -0.5877852522924830181 ) ) ;
#14641=CIRCLE ( 'NONE', #6808, 37.49900000000000233 ) ;
#14642=CARTESIAN_POINT ( 'NONE',  ( 10.00000000000000000, -37.16516213103273714, -4.992566952385376844 ) ) ;
#14644=EDGE_LOOP ( 'NONE', ( #37480, #15840, #3889, #17039 ) ) ;
#14645=ORIENTED_EDGE ( 'NONE', *, *, #1047, .F. ) ;
#14649=FACE_OUTER_BOUND ( 'NONE', #4069, .T. ) ;
#14654=DIRECTION ( 'NONE',  ( -1.000000000000000000, -0.000000000000000000, 0.000000000000000000 ) ) ;
#14663=ORIENTED_EDGE ( 'NONE', *, *, #32715, .F. ) ;
#14664=VERTEX_POINT ( 'NONE', #18831 ) ;
#14671=CARTESIAN_POINT ( 'NONE',  ( 0.000000000000000000, 0.000000000000000000, 0.000000000000000000 ) ) ;
#14673=FACE_OUTER_BOUND ( 'NONE', #34461, .T. ) ;
#14677=DIRECTION ( 'NONE',  ( 1.000000000000000000, -0.000000000000000000, 0.000000000000000000 ) ) ;
#14678=DIRECTION ( 'NONE',  ( 0.000000000000000000, -0.8910065241883627918, -0.4539904997395568520 ) ) ;
#14686=AXIS2_PLACEMENT_3D ( 'NONE', #15774, #42875, #9326 ) ;
#14699=VECTOR ( 'NONE', #15246, 1000.000000000000000 ) ;
#14706=EDGE_CURVE ( 'NONE', #8228, #15615, #34485, .T. ) ;
#14708=ORIENTED_EDGE ( 'NONE', *, *, #162, .T. ) ;
#14717=DIRECTION ( 'NONE',  ( -1.000000000000000000, -0.000000000000000000, -0.000000000000000000 ) ) ;
#14718=ORIENTED_EDGE ( 'NONE', *, *, #46032, .F. ) ;
#14731=EDGE_LOOP ( 'NONE', ( #44370, #14132, #11298, #29679 ) ) ;
#14732=DIRECTION ( 'NONE',  ( -1.000000000000000000, 0.000000000000000000, 0.000000000000000000 ) ) ;
#14735=DIRECTION ( 'NONE',  ( -1.000000000000000000, -0.000000000000000000, 0.000000000000000000 ) ) ;
#14737=VECTOR ( 'NONE', #1425, 1000.000000000000114 ) ;
#14746=EDGE_CURVE ( 'NONE', #37265, #32654, #19815, .T. ) ;
#14758=EDGE_CURVE ( 'NONE', #36706, #33430, #723, .T. ) ;
#14761=ORIENTED_EDGE ( 'NONE', *, *, #27834, .F. ) ;
#14762=EDGE_CURVE ( 'NONE', #45279, #34171, #15655, .T. ) ;
#14775=LINE ( 'NONE', #30198, #7798 ) ;
#14782=FACE_OUTER_BOUND ( 'NONE', #13817, .T. ) ;
#14788=EDGE_LOOP ( 'NONE', ( #43529, #19141, #21327, #2975 ) ) ;
#14798=CARTESIAN_POINT ( 'NONE',  ( 5.000000000000000000, 39.04073710021344112, 15.48615015657596850 ) ) ;
#14805=LINE ( 'NONE', #5593, #19270 ) ;
#14810=DIRECTION ( 'NONE',  ( 0.000000000000000000, 0.9876883405951382144, -0.1564344650402276493 ) ) ;
#14811=DIRECTION ( 'NONE',  ( 0.000000000000000000, 0.3090169943749480619, -0.9510565162951533091 ) ) ;
#14816=EDGE_CURVE ( 'NONE', #44741, #22704, #45619, .T. ) ;
#14820=ORIENTED_EDGE ( 'NONE', *, *, #16239, .T. ) ;
#14823=VERTEX_POINT ( 'NONE', #13199 ) ;
#14826=CARTESIAN_POINT ( 'NONE',  ( 4.999999999999999112, 3.925862922256769583, -41.81611651403857621 ) ) ;
#14828=AXIS2_PLACEMENT_3D ( 'NONE', #2441, #46535, #17367 ) ;
#14835=VECTOR ( 'NONE', #7945, 1000.000000000000000 ) ;
#14849=FACE_OUTER_BOUND ( 'NONE', #32244, .T. ) ;
#14858=FACE_OUTER_BOUND ( 'NONE', #46984, .T. ) ;
#14861=FACE_OUTER_BOUND ( 'NONE', #13215, .T. ) ;
#14863=EDGE_CURVE ( 'NONE', #22486, #44741, #6591, .T. ) ;
#14873=AXIS2_PLACEMENT_3D ( 'NONE', #24104, #5269, #46371 ) ;
#14874=AXIS2_PLACEMENT_3D ( 'NONE', #37694, #41613, #23011 ) ;
#14878=EDGE_CURVE ( 'NONE', #19822, #15289, #10505, .T. ) ;
#14880=VERTEX_POINT ( 'NONE', #46968 ) ;
#14881=CIRCLE ( 'NONE', #34489, 42.00000000000000000 ) ;
#14886=EDGE_CURVE ( 'NONE', #29480, #19341, #1463, .T. ) ;
#14891=ORIENTED_EDGE ( 'NONE', *, *, #315, .T. ) ;
#14893=FACE_OUTER_BOUND ( 'NONE', #14534, .T. ) ;
#14899=CIRCLE ( 'NONE', #10179, 15.99999999999999822 ) ;
#14900=DIRECTION ( 'NONE',  ( -1.000000000000000000, 0.000000000000000000, -0.000000000000000000 ) ) ;
#14907=DIRECTION ( 'NONE',  ( -1.000000000000000000, 0.000000000000000000, 0.000000000000000000 ) ) ;
#14911=ORIENTED_EDGE ( 'NONE', *, *, #42683, .T. ) ;
#14914=DIRECTION ( 'NONE',  ( 0.000000000000000000, 0.000000000000000000, 1.000000000000000000 ) ) ;
#14916=DIRECTION ( 'NONE',  ( -1.000000000000000000, -0.000000000000000000, -0.000000000000000000 ) ) ;
#14920=CARTESIAN_POINT ( 'NONE',  ( 4.999999999999999112, 40.68715046381927891, 10.41901085202092858 ) ) ;
#14937=AXIS2_PLACEMENT_3D ( 'NONE', #17184, #10094, #6905 ) ;
#14938=AXIS2_PLACEMENT_3D ( 'NONE', #3632, #36904, #26152 ) ;
#14944=ADVANCED_FACE ( 'NONE', ( #47914 ), #47207, .T. ) ;
#14949=VERTEX_POINT ( 'NONE', #3367 ) ;
#14955=ORIENTED_EDGE ( 'NONE', *, *, #19100, .T. ) ;
#14969=AXIS2_PLACEMENT_3D ( 'NONE', #24599, #20926, #1842 ) ;
#14973=DIRECTION ( 'NONE',  ( -1.000000000000000000, 0.000000000000000000, 0.000000000000000000 ) ) ;
#14974=CARTESIAN_POINT ( 'NONE',  ( -3.000000000000000000, 8.688484142253939169, 21.88630264137371029 ) ) ;
#14985=AXIS2_PLACEMENT_3D ( 'NONE', #14131, #33214, #36872 ) ;
#14987=DIRECTION ( 'NONE',  ( -1.000000000000000000, 0.000000000000000000, -0.000000000000000000 ) ) ;
#14988=VERTEX_POINT ( 'NONE', #36180 ) ;
#14996=DIRECTION ( 'NONE',  ( -0.000000000000000000, 0.1045284632676559550, -0.9945218953682731788 ) ) ;
#15027=ORIENTED_EDGE ( 'NONE', *, *, #24210, .F. ) ;
#15032=CARTESIAN_POINT ( 'NONE',  ( 10.00000000000000000, 37.01155633439068282, -6.555932627142014191 ) ) ;
#15033=CARTESIAN_POINT ( 'NONE',  ( 0.000000000000000000, 4.992566952384984269, 37.16516213103279398 ) ) ;
#15044=DIRECTION ( 'NONE',  ( 0.000000000000000000, 0.000000000000000000, 1.000000000000000000 ) ) ;
#15050=CARTESIAN_POINT ( 'NONE',  ( 10.00000000000000000, 33.80338159004307386, -16.23288003029461279 ) ) ;
#15051=AXIS2_PLACEMENT_3D ( 'NONE', #2272, #18087, #46835 ) ;
#15055=CARTESIAN_POINT ( 'NONE',  ( 10.00000000000000000, 0.000000000000000000, 0.000000000000000000 ) ) ;
#15070=AXIS2_PLACEMENT_3D ( 'NONE', #11235, #4130, #46215 ) ;
#15080=DIRECTION ( 'NONE',  ( -1.000000000000000000, 0.000000000000000000, 0.000000000000000000 ) ) ;
#15083=CIRCLE ( 'NONE', #19782, 16.00000000000000000 ) ;
#15085=VERTEX_POINT ( 'NONE', #25158 ) ;
#15087=ORIENTED_EDGE ( 'NONE', *, *, #8622, .F. ) ;
#15090=DIRECTION ( 'NONE',  ( 0.000000000000000000, 0.000000000000000000, 1.000000000000000000 ) ) ;
#15104=EDGE_LOOP ( 'NONE', ( #28413, #9823, #27498, #35107 ) ) ;
#15122=VECTOR ( 'NONE', #7756, 1000.000000000000000 ) ;
#15123=CARTESIAN_POINT ( 'NONE',  ( 10.00000000000000000, 35.47612816024556537, -22.48208911017461631 ) ) ;
#15132=AXIS2_PLACEMENT_3D ( 'NONE', #16761, #27787, #13561 ) ;
#15137=ORIENTED_EDGE ( 'NONE', *, *, #22093, .F. ) ;
#15138=EDGE_CURVE ( 'NONE', #46278, #36861, #11211, .T. ) ;
#15153=EDGE_LOOP ( 'NONE', ( #34103, #2195, #668, #32708 ) ) ;
#15163=VECTOR ( 'NONE', #23285, 1000.000000000000000 ) ;
#15167=CARTESIAN_POINT ( 'NONE',  ( 10.00000000000000000, 0.000000000000000000, 0.000000000000000000 ) ) ;
#15171=PLANE ( 'NONE',  #12708 ) ;
#15189=ORIENTED_EDGE ( 'NONE', *, *, #22707, .F. ) ;
#15192=CIRCLE ( 'NONE', #23780, 42.00000000000000000 ) ;
#15199=ORIENTED_EDGE ( 'NONE', *, *, #9033, .F. ) ;
#15205=EDGE_LOOP ( 'NONE', ( #24835, #8700, #5461, #206 ) ) ;
#15209=CIRCLE ( 'NONE', #21450, 16.00000000000000000 ) ;
#15212=VERTEX_POINT ( 'NONE', #7286 ) ;
#15220=AXIS2_PLACEMENT_3D ( 'NONE', #43574, #6132, #21537 ) ;
#15221=PLANE ( 'NONE',  #14140 ) ;
#15225=CARTESIAN_POINT ( 'NONE',  ( 10.00000000000000000, -30.84782396557201878, -21.32104025579148399 ) ) ;
#15229=CARTESIAN_POINT ( 'NONE',  ( 10.00000000000000000, 26.08949754953062694, -27.05870788708203989 ) ) ;
#15231=CARTESIAN_POINT ( 'NONE',  ( 10.00000000000000000, 29.81001611431009479, 22.74946021919143391 ) ) ;
#15235=CARTESIAN_POINT ( 'NONE',  ( 0.000000000000000000, -23.29833615347109443, 3.418703333116492438 ) ) ;
#15238=DIRECTION ( 'NONE',  ( 0.000000000000000000, -0.9876883405951358830, -0.1564344650402420822 ) ) ;
#15246=DIRECTION ( 'NONE',  ( -1.000000000000000000, 0.000000000000000000, -0.000000000000000000 ) ) ;
#15247=LINE ( 'NONE', #41421, #24912 ) ;
#15262=ADVANCED_FACE ( 'NONE', ( #36313 ), #17457, .T. ) ;
#15264=VECTOR ( 'NONE', #40520, 1000.000000000000000 ) ;
#15267=CARTESIAN_POINT ( 'NONE',  ( 0.000000000000000000, 18.84667830672579925, 18.68964196561269020 ) ) ;
#15279=VERTEX_POINT ( 'NONE', #35342 ) ;
#15289=VERTEX_POINT ( 'NONE', #43658 ) ;
#15291=DIRECTION ( 'NONE',  ( 0.000000000000000000, 0.4539904997395479702, -0.8910065241883673437 ) ) ;
#15300=DIRECTION ( 'NONE',  ( 0.000000000000000000, 0.000000000000000000, 1.000000000000000000 ) ) ;
#15319=AXIS2_PLACEMENT_3D ( 'NONE', #12798, #42166, #13049 ) ;
#15328=ORIENTED_EDGE ( 'NONE', *, *, #28534, .T. ) ;
#15329=CARTESIAN_POINT ( 'NONE',  ( 10.00000000000000000, -33.80338159004296017, 16.23288003029484727 ) ) ;
#15332=AXIS2_PLACEMENT_3D ( 'NONE', #1128, #26362, #11673 ) ;
#15338=VERTEX_POINT ( 'NONE', #35829 ) ;
#15341=ORIENTED_EDGE ( 'NONE', *, *, #35882, .F. ) ;
#15344=CARTESIAN_POINT ( 'NONE',  ( 10.00000000000000000, -27.13269053701114331, 25.88420570971391754 ) ) ;
#15357=ORIENTED_EDGE ( 'NONE', *, *, #31214, .F. ) ;
#15364=AXIS2_PLACEMENT_3D ( 'NONE', #41628, #40912, #11045 ) ;
#15365=DIRECTION ( 'NONE',  ( -0.000000000000000000, 0.8090169943749498938, -0.5877852522924696954 ) ) ;
#15368=DIRECTION ( 'NONE',  ( -1.000000000000000000, -0.000000000000000000, -0.000000000000000000 ) ) ;
#15370=FACE_OUTER_BOUND ( 'NONE', #13708, .T. ) ;
#15377=AXIS2_PLACEMENT_3D ( 'NONE', #31129, #41906, #27449 ) ;
#15378=FACE_OUTER_BOUND ( 'NONE', #15205, .T. ) ;
#15388=AXIS2_PLACEMENT_3D ( 'NONE', #38341, #15365, #27333 ) ;
#15390=FACE_OUTER_BOUND ( 'NONE', #7104, .T. ) ;
#15403=CIRCLE ( 'NONE', #26330, 37.49900000000000233 ) ;
#15406=CARTESIAN_POINT ( 'NONE',  ( 0.000000000000000000, 16.83928648764923253, 16.46020748918050458 ) ) ;
#15409=CYLINDRICAL_SURFACE ( 'NONE', #4315, 16.00000000000000000 ) ;
#15420=DIRECTION ( 'NONE',  ( -1.000000000000000000, 0.000000000000000000, -0.000000000000000000 ) ) ;
#15423=ORIENTED_EDGE ( 'NONE', *, *, #37402, .T. ) ;
#15425=UNCERTAINTY_MEASURE_WITH_UNIT (LENGTH_MEASURE( 1.000000000000000082E-05 ), #4990, 'distance_accuracy_value', 'NONE');
#15428=EDGE_CURVE ( 'NONE', #15687, #14664, #21631, .T. ) ;
#15429=DIRECTION ( 'NONE',  ( -1.000000000000000000, -0.000000000000000000, 0.000000000000000000 ) ) ;
#15430=ORIENTED_EDGE ( 'NONE', *, *, #34087, .T. ) ;
#15438=ORIENTED_EDGE ( 'NONE', *, *, #29339, .F. ) ;
#15463=DIRECTION ( 'NONE',  ( 1.000000000000000000, -0.000000000000000000, -0.000000000000000000 ) ) ;
#15473=EDGE_CURVE ( 'NONE', #3134, #35244, #41207, .T. ) ;
#15491=CARTESIAN_POINT ( 'NONE',  ( 10.00000000000000000, 17.80606268964540462, 33.00180498840053644 ) ) ;
#15496=VERTEX_POINT ( 'NONE', #31154 ) ;
#15502=CIRCLE ( 'NONE', #13924, 16.00000000000000000 ) ;
#15513=DIRECTION ( 'NONE',  ( 0.000000000000000000, 0.000000000000000000, 1.000000000000000000 ) ) ;
#15521=CARTESIAN_POINT ( 'NONE',  ( 0.000000000000000000, -39.04073710021332744, -15.48615015657624028 ) ) ;
#15522=EDGE_CURVE ( 'NONE', #11693, #33751, #42152, .T. ) ;
#15523=LINE ( 'NONE', #31192, #43420 ) ;
#15525=DIRECTION ( 'NONE',  ( -0.000000000000000000, 0.1045284632676436315, 0.9945218953682742891 ) ) ;
#15534=ORIENTED_EDGE ( 'NONE', *, *, #48389, .T. ) ;
#15537=DIRECTION ( 'NONE',  ( 0.000000000000000000, 0.000000000000000000, 1.000000000000000000 ) ) ;
#15550=ORIENTED_EDGE ( 'NONE', *, *, #5451, .T. ) ;
#15551=VERTEX_POINT ( 'NONE', #15491 ) ;
#15564=CIRCLE ( 'NONE', #38246, 37.49900000000000944 ) ;
#15569=DIRECTION ( 'NONE',  ( 0.000000000000000000, 0.9945218953682742891, -0.1045284632676436315 ) ) ;
#15571=LINE ( 'NONE', #19243, #36933 ) ;
#15589=VERTEX_POINT ( 'NONE', #34311 ) ;
#15592=CARTESIAN_POINT ( 'NONE',  ( 10.00000000000000000, -3.925862922255855647, -41.81611651403866858 ) ) ;
#15596=AXIS2_PLACEMENT_3D ( 'NONE', #14011, #6676, #21603 ) ;
#15600=VERTEX_POINT ( 'NONE', #45576 ) ;
#15601=VERTEX_POINT ( 'NONE', #23309 ) ;
#15602=CARTESIAN_POINT ( 'NONE',  ( 10.00000000000000000, -6.736453364083817341, 36.88895765772630142 ) ) ;
#15609=CARTESIAN_POINT ( 'NONE',  ( 0.000000000000000000, 0.000000000000000000, 0.000000000000000000 ) ) ;
#15615=VERTEX_POINT ( 'NONE', #43372 ) ;
#15621=DIRECTION ( 'NONE',  ( -1.000000000000000000, -0.000000000000000000, -0.000000000000000000 ) ) ;
#15624=DIRECTION ( 'NONE',  ( -1.000000000000000000, 0.000000000000000000, -0.000000000000000000 ) ) ;
#15625=ADVANCED_FACE ( 'NONE', ( #12784 ), #1763, .F. ) ;
#15632=ORIENTED_EDGE ( 'NONE', *, *, #10103, .F. ) ;
#15633=DIRECTION ( 'NONE',  ( -1.000000000000000000, -0.000000000000000000, 0.000000000000000000 ) ) ;
#15637=LINE ( 'NONE', #42312, #42557 ) ;
#15641=ADVANCED_FACE ( 'NONE', ( #2236 ), #43601, .T. ) ;
#15647=EDGE_CURVE ( 'NONE', #43176, #38863, #43287, .T. ) ;
#15649=CARTESIAN_POINT ( 'NONE',  ( 10.00000000000000000, 0.000000000000000000, 0.000000000000000000 ) ) ;
#15655=LINE ( 'NONE', #41141, #45649 ) ;
#15656=ORIENTED_EDGE ( 'NONE', *, *, #39007, .T. ) ;
#15664=ORIENTED_EDGE ( 'NONE', *, *, #46717, .F. ) ;
#15666=VECTOR ( 'NONE', #17491, 1000.000000000000000 ) ;
#15667=AXIS2_PLACEMENT_3D ( 'NONE', #35073, #46827, #20147 ) ;
#15668=PLANE ( 'NONE',  #41459 ) ;
#15669=ORIENTED_EDGE ( 'NONE', *, *, #46940, .T. ) ;
#15672=DIRECTION ( 'NONE',  ( 0.000000000000000000, 0.000000000000000000, 1.000000000000000000 ) ) ;
#15678=ORIENTED_EDGE ( 'NONE', *, *, #11015, .T. ) ;
#15687=VERTEX_POINT ( 'NONE', #46801 ) ;
#15708=EDGE_CURVE ( 'NONE', #41148, #26085, #9571, .T. ) ;
#15709=DIRECTION ( 'NONE',  ( -1.000000000000000000, -0.000000000000000000, 0.000000000000000000 ) ) ;
#15710=DIRECTION ( 'NONE',  ( 1.000000000000000000, 0.000000000000000000, -0.000000000000000000 ) ) ;
#15718=ORIENTED_EDGE ( 'NONE', *, *, #41867, .F. ) ;
#15720=DIRECTION ( 'NONE',  ( 1.000000000000000000, -0.000000000000000000, 0.000000000000000000 ) ) ;
#15737=EDGE_CURVE ( 'NONE', #30648, #47828, #21793, .T. ) ;
#15758=EDGE_CURVE ( 'NONE', #5993, #34646, #43834, .T. ) ;
#15774=CARTESIAN_POINT ( 'NONE',  ( 10.00000000000000000, 30.80686688397041451, -21.53537804866048688 ) ) ;
#15778=ORIENTED_EDGE ( 'NONE', *, *, #31232, .T. ) ;
#15797=VERTEX_POINT ( 'NONE', #10295 ) ;
#15800=CARTESIAN_POINT ( 'NONE',  ( 0.000000000000000000, -10.45096189432314837, -21.10159698893440350 ) ) ;
#15801=FACE_OUTER_BOUND ( 'NONE', #1108, .T. ) ;
#15804=VERTEX_POINT ( 'NONE', #25212 ) ;
#15812=DIRECTION ( 'NONE',  ( 0.000000000000000000, -0.7071067811865535679, 0.7071067811865413555 ) ) ;
#15814=CIRCLE ( 'NONE', #24396, 16.00000000000000000 ) ;
#15815=LINE ( 'NONE', #30750, #4908 ) ;
#15816=ADVANCED_FACE ( 'NONE', ( #47503 ), #22293, .T. ) ;
#15834=CARTESIAN_POINT ( 'NONE',  ( 0.000000000000000000, 10.41901085202135491, -40.68715046381917944 ) ) ;
#15839=VECTOR ( 'NONE', #10837, 1000.000000000000000 ) ;
#15840=ORIENTED_EDGE ( 'NONE', *, *, #36135, .F. ) ;
#15845=ORIENTED_EDGE ( 'NONE', *, *, #16114, .T. ) ;
#15846=VECTOR ( 'NONE', #46600, 1000.000000000000000 ) ;
#15855=ADVANCED_FACE ( 'NONE', ( #6879 ), #42816, .F. ) ;
#15871=ORIENTED_EDGE ( 'NONE', *, *, #17977, .F. ) ;
#15872=ORIENTED_EDGE ( 'NONE', *, *, #33803, .T. ) ;
#15881=DIRECTION ( 'NONE',  ( 0.000000000000000000, 0.000000000000000000, 1.000000000000000000 ) ) ;
#15888=LINE ( 'NONE', #12463, #26335 ) ;
#15892=DIRECTION ( 'NONE',  ( 0.000000000000000000, 0.000000000000000000, 1.000000000000000000 ) ) ;
#15900=DIRECTION ( 'NONE',  ( -1.000000000000000000, 0.000000000000000000, 0.000000000000000000 ) ) ;
#15901=AXIS2_PLACEMENT_3D ( 'NONE', #21559, #6389, #2460 ) ;
#15905=EDGE_CURVE ( 'NONE', #15601, #13149, #36167, .T. ) ;
#15916=VECTOR ( 'NONE', #16550, 1000.000000000000000 ) ;
#15924=ORIENTED_EDGE ( 'NONE', *, *, #42934, .T. ) ;
#15952=DIRECTION ( 'NONE',  ( -1.000000000000000000, 0.000000000000000000, 0.000000000000000000 ) ) ;
#15961=DIRECTION ( 'NONE',  ( 0.000000000000000000, 0.4067366430757887730, 0.9135454576426059736 ) ) ;
#15976=ADVANCED_FACE ( 'NONE', ( #1690 ), #32041, .T. ) ;
#15978=LINE ( 'NONE', #30922, #4238 ) ;
#15980=DIRECTION ( 'NONE',  ( -1.000000000000000000, 0.000000000000000000, -0.000000000000000000 ) ) ;
#15985=EDGE_CURVE ( 'NONE', #44254, #28319, #24197, .T. ) ;
#15995=DIRECTION ( 'NONE',  ( -1.000000000000000000, -0.000000000000000000, 0.000000000000000000 ) ) ;
#15996=ORIENTED_EDGE ( 'NONE', *, *, #16680, .T. ) ;
#15997=ORIENTED_EDGE ( 'NONE', *, *, #22637, .F. ) ;
#16003=LINE ( 'NONE', #42915, #11020 ) ;
#16011=CARTESIAN_POINT ( 'NONE',  ( 0.000000000000000000, 0.000000000000000000, 0.000000000000000000 ) ) ;
#16014=CARTESIAN_POINT ( 'NONE',  ( 4.999999999999999112, -36.13751322684434797, 21.40280677340357940 ) ) ;
#16015=CARTESIAN_POINT ( 'NONE',  ( 10.00000000000000000, 6.736453364084091788, -36.88895765772625879 ) ) ;
#16016=CYLINDRICAL_SURFACE ( 'NONE', #245, 16.00000000000000355 ) ;
#16020=EDGE_CURVE ( 'NONE', #31490, #32836, #3353, .T. ) ;
#16026=EDGE_CURVE ( 'NONE', #4179, #17031, #21728, .T. ) ;
#16027=EDGE_CURVE ( 'NONE', #36913, #5880, #15192, .T. ) ;
#16028=DIRECTION ( 'NONE',  ( 0.000000000000000000, 0.3090169943749480619, -0.9510565162951533091 ) ) ;
#16032=VECTOR ( 'NONE', #18081, 1000.000000000000000 ) ;
#16036=CIRCLE ( 'NONE', #14462, 37.49900000000000233 ) ;
#16044=DIRECTION ( 'NONE',  ( -1.000000000000000000, -0.000000000000000000, 0.000000000000000000 ) ) ;
#16049=CARTESIAN_POINT ( 'NONE',  ( 0.000000000000000000, 8.688484142254221609, -21.88630264137359660 ) ) ;
#16061=CARTESIAN_POINT ( 'NONE',  ( -3.000000000000000000, -14.54903810567645195, -22.19967320028775504 ) ) ;
#16073=ORIENTED_EDGE ( 'NONE', *, *, #29336, .T. ) ;
#16074=ORIENTED_EDGE ( 'NONE', *, *, #47616, .F. ) ;
#16077=DIRECTION ( 'NONE',  ( 0.000000000000000000, -0.8910065241883722287, 0.4539904997395382003 ) ) ;
#16085=EDGE_LOOP ( 'NONE', ( #42102, #43715, #13331, #1946 ) ) ;
#16100=ADVANCED_FACE ( 'NONE', ( #41074 ), #44721, .T. ) ;
#16101=ORIENTED_EDGE ( 'NONE', *, *, #14758, .F. ) ;
#16105=CIRCLE ( 'NONE', #41889, 16.00000000000000355 ) ;
#16111=ORIENTED_EDGE ( 'NONE', *, *, #16588, .F. ) ;
#16114=EDGE_CURVE ( 'NONE', #29882, #35670, #7761, .T. ) ;
#16117=CARTESIAN_POINT ( 'NONE',  ( 10.00000000000000000, 37.58145647212453611, 16.68533520207917675 ) ) ;
#16133=AXIS2_PLACEMENT_3D ( 'NONE', #24963, #39909, #17622 ) ;
#16144=VECTOR ( 'NONE', #6068, 1000.000000000000000 ) ;
#16172=ORIENTED_EDGE ( 'NONE', *, *, #43605, .T. ) ;
#16175=DIRECTION ( 'NONE',  ( 0.000000000000000000, -0.7071067811865389130, -0.7071067811865563435 ) ) ;
#16177=DIRECTION ( 'NONE',  ( -0.000000000000000000, -0.3090169943749448977, -0.9510565162951543083 ) ) ;
#16181=EDGE_LOOP ( 'NONE', ( #16779, #42840, #37202, #17105 ) ) ;
#16189=LINE ( 'NONE', #31119, #45562 ) ;
#16197=AXIS2_PLACEMENT_3D ( 'NONE', #13130, #1138, #38595 ) ;
#16204=DIRECTION ( 'NONE',  ( 0.000000000000000000, 0.000000000000000000, 1.000000000000000000 ) ) ;
#16208=FACE_OUTER_BOUND ( 'NONE', #48120, .T. ) ;
#16212=AXIS2_PLACEMENT_3D ( 'NONE', #12093, #4726, #27018 ) ;
#16219=AXIS2_PLACEMENT_3D ( 'NONE', #9497, #9981, #2619 ) ;
#16222=AXIS2_PLACEMENT_3D ( 'NONE', #48271, #41650, #37257 ) ;
#16229=CARTESIAN_POINT ( 'NONE',  ( 10.00000000000000000, -30.80686688397025108, 21.53537804866070715 ) ) ;
#16232=ORIENTED_EDGE ( 'NONE', *, *, #37311, .F. ) ;
#16236=CYLINDRICAL_SURFACE ( 'NONE', #40210, 16.00000000000000000 ) ;
#16239=EDGE_CURVE ( 'NONE', #29827, #15289, #41150, .T. ) ;
#16243=CARTESIAN_POINT ( 'NONE',  ( 10.00000000000000000, -27.13269053701078448, -25.88420570971428702 ) ) ;
#16247=CIRCLE ( 'NONE', #18569, 15.99999999999999822 ) ;
#16249=DIRECTION ( 'NONE',  ( -0.000000000000000000, -1.000000000000000000, -0.000000000000000000 ) ) ;
#16250=CARTESIAN_POINT ( 'NONE',  ( 10.00000000000000000, 21.32104025579114648, 30.84782396557224970 ) ) ;
#16253=CARTESIAN_POINT ( 'NONE',  ( 10.00000000000000000, 31.52238457039638320, -27.75498641678709788 ) ) ;
#16255=CARTESIAN_POINT ( 'NONE',  ( 10.00000000000000000, 0.000000000000000000, 0.000000000000000000 ) ) ;
#16272=EDGE_CURVE ( 'NONE', #1412, #19636, #2591, .T. ) ;
#16278=CIRCLE ( 'NONE', #40489, 42.00000000000000000 ) ;
#16281=DIRECTION ( 'NONE',  ( 0.000000000000000000, -1.000000000000000000, -1.040834085586084257E-14 ) ) ;
#16283=ORIENTED_EDGE ( 'NONE', *, *, #32293, .F. ) ;
#16286=VERTEX_POINT ( 'NONE', #31775 ) ;
#16291=VERTEX_POINT ( 'NONE', #47153 ) ;
#16293=ORIENTED_EDGE ( 'NONE', *, *, #19603, .T. ) ;
#16297=LINE ( 'NONE', #27079, #43647 ) ;
#16298=CARTESIAN_POINT ( 'NONE',  ( -3.000000000000000000, -1.278221433540502217, 26.51162292216071847 ) ) ;
#16301=DIRECTION ( 'NONE',  ( -1.000000000000000000, -0.000000000000000000, -0.000000000000000000 ) ) ;
#16303=ORIENTED_EDGE ( 'NONE', *, *, #1619, .F. ) ;
#16305=DIRECTION ( 'NONE',  ( -1.000000000000000000, 0.000000000000000000, 0.000000000000000000 ) ) ;
#16309=PLANE ( 'NONE',  #43489 ) ;
#16316=DIRECTION ( 'NONE',  ( -1.000000000000000000, 0.000000000000000000, 0.000000000000000000 ) ) ;
#16322=ADVANCED_FACE ( 'NONE', ( #17049 ), #35408, .T. ) ;
#16323=ORIENTED_EDGE ( 'NONE', *, *, #12291, .T. ) ;
#16332=AXIS2_PLACEMENT_3D ( 'NONE', #25406, #14654, #40365 ) ;
#16339=CIRCLE ( 'NONE', #31982, 16.00000000000000000 ) ;
#16347=DIRECTION ( 'NONE',  ( 1.000000000000000000, 0.000000000000000000, 0.000000000000000000 ) ) ;
#16348=ORIENTED_EDGE ( 'NONE', *, *, #47943, .T. ) ;
#16353=ORIENTED_EDGE ( 'NONE', *, *, #34868, .F. ) ;
#16368=CARTESIAN_POINT ( 'NONE',  ( 10.00000000000000000, 0.000000000000000000, 0.000000000000000000 ) ) ;
#16374=LINE ( 'NONE', #39629, #20838 ) ;
#16375=VECTOR ( 'NONE', #44932, 1000.000000000000000 ) ;
#16378=VECTOR ( 'NONE', #22475, 1000.000000000000000 ) ;
#16382=AXIS2_PLACEMENT_3D ( 'NONE', #35903, #11368, #20980 ) ;
#16393=ORIENTED_EDGE ( 'NONE', *, *, #40682, .T. ) ;
#16399=CARTESIAN_POINT ( 'NONE',  ( 10.00000000000000000, -36.88895765772628010, -6.736453364083947015 ) ) ;
#16401=DIRECTION ( 'NONE',  ( 1.000000000000000000, -0.000000000000000000, -0.000000000000000000 ) ) ;
#16403=EDGE_CURVE ( 'NONE', #11961, #45643, #28076, .T. ) ;
#16405=CYLINDRICAL_SURFACE ( 'NONE', #2517, 37.49900000000000233 ) ;
#16416=ORIENTED_EDGE ( 'NONE', *, *, #2964, .T. ) ;
#16424=CARTESIAN_POINT ( 'NONE',  ( 10.00000000000000000, 26.79245525562761188, -32.34446384429941901 ) ) ;
#16434=CARTESIAN_POINT ( 'NONE',  ( 10.00000000000000000, 5.202137450156907761, -37.22597642581151689 ) ) ;
#16450=ORIENTED_EDGE ( 'NONE', *, *, #21163, .T. ) ;
#16455=EDGE_LOOP ( 'NONE', ( #26688, #23606, #18120, #6398 ) ) ;
#16456=CARTESIAN_POINT ( 'NONE',  ( 4.999999999999999112, 10.41901085202135491, -40.68715046381917944 ) ) ;
#16475=AXIS2_PLACEMENT_3D ( 'NONE', #25015, #47534, #43399 ) ;
#16482=CARTESIAN_POINT ( 'NONE',  ( 10.00000000000000000, 36.88895765772633695, 6.736453364083687667 ) ) ;
#16488=CARTESIAN_POINT ( 'NONE',  ( 10.00000000000000000, -37.48860685352291711, 0.8828120875899322373 ) ) ;
#16493=DIRECTION ( 'NONE',  ( -1.000000000000000000, 0.000000000000000000, 0.000000000000000000 ) ) ;
#16498=EDGE_CURVE ( 'NONE', #27191, #26165, #8195, .T. ) ;
#16507=AXIS2_PLACEMENT_3D ( 'NONE', #30748, #4075, #33676 ) ;
#16535=DIRECTION ( 'NONE',  ( 0.000000000000000000, 0.000000000000000000, 1.000000000000000000 ) ) ;
#16537=DIRECTION ( 'NONE',  ( 0.000000000000000000, 0.000000000000000000, 1.000000000000000000 ) ) ;
#16540=CYLINDRICAL_SURFACE ( 'NONE', #25387, 16.00000000000000000 ) ;
#16542=CARTESIAN_POINT ( 'NONE',  ( 0.000000000000000000, 0.6853352020790449695, 37.58145647212454321 ) ) ;
#16550=DIRECTION ( 'NONE',  ( 1.000000000000000000, -0.000000000000000000, -0.000000000000000000 ) ) ;
#16553=CARTESIAN_POINT ( 'NONE',  ( -3.000000000000000000, -4.261787119645322974, 26.19803753235774835 ) ) ;
#16554=DIRECTION ( 'NONE',  ( 0.000000000000000000, 0.000000000000000000, 1.000000000000000000 ) ) ;
#16555=DIRECTION ( 'NONE',  ( -1.000000000000000000, -0.000000000000000000, -0.000000000000000000 ) ) ;
#16557=CARTESIAN_POINT ( 'NONE',  ( 0.000000000000000000, -3.948201729842348850, 23.21447184625293048 ) ) ;
#16565=VERTEX_POINT ( 'NONE', #27299 ) ;
#16566=CIRCLE ( 'NONE', #36127, 16.00000000000000000 ) ;
#16571=VERTEX_POINT ( 'NONE', #8925 ) ;
#16576=DIRECTION ( 'NONE',  ( -1.000000000000000000, 0.000000000000000000, 0.000000000000000000 ) ) ;
#16581=ORIENTED_EDGE ( 'NONE', *, *, #27928, .T. ) ;
#16586=VECTOR ( 'NONE', #19507, 1000.000000000000000 ) ;
#16588=EDGE_CURVE ( 'NONE', #18777, #44892, #37086, .T. ) ;
#16598=ORIENTED_EDGE ( 'NONE', *, *, #27712, .T. ) ;
#16600=CARTESIAN_POINT ( 'NONE',  ( 10.00000000000000000, 0.000000000000000000, 0.000000000000000000 ) ) ;
#16603=CARTESIAN_POINT ( 'NONE',  ( 10.00000000000000000, 15.48615015657582283, 39.04073710021349797 ) ) ;
#16607=VECTOR ( 'NONE', #14261, 999.9999999999998863 ) ;
#16610=CARTESIAN_POINT ( 'NONE',  ( 10.00000000000000000, 37.22597642581158084, -5.202137450156524068 ) ) ;
#16625=EDGE_CURVE ( 'NONE', #18915, #30366, #26807, .T. ) ;
#16628=CARTESIAN_POINT ( 'NONE',  ( 0.000000000000000000, 5.835314593368477354, 22.81335362449854642 ) ) ;
#16654=DIRECTION ( 'NONE',  ( 1.000000000000000000, 0.000000000000000000, 0.000000000000000000 ) ) ;
#16667=VERTEX_POINT ( 'NONE', #620 ) ;
#16673=DIRECTION ( 'NONE',  ( -1.000000000000000000, 0.000000000000000000, 0.000000000000000000 ) ) ;
#16674=AXIS2_PLACEMENT_3D ( 'NONE', #36709, #13254, #43114 ) ;
#16676=ORIENTED_EDGE ( 'NONE', *, *, #16498, .T. ) ;
#16680=EDGE_CURVE ( 'NONE', #14823, #32747, #37934, .T. ) ;
#16683=AXIS2_PLACEMENT_3D ( 'NONE', #17299, #9723, #17547 ) ;
#16684=CIRCLE ( 'NONE', #22202, 42.00000000000000000 ) ;
#16685=AXIS2_PLACEMENT_3D ( 'NONE', #7763, #10728, #18768 ) ;
#16696=CARTESIAN_POINT ( 'NONE',  ( 10.00000000000000000, 0.000000000000000000, 0.000000000000000000 ) ) ;
#16699=EDGE_CURVE ( 'NONE', #35244, #20241, #42713, .T. ) ;
#16700=EDGE_CURVE ( 'NONE', #41993, #46585, #2302, .T. ) ;
#16704=LINE ( 'NONE', #16456, #1211 ) ;
#16705=ORIENTED_EDGE ( 'NONE', *, *, #14762, .T. ) ;
#16712=CIRCLE ( 'NONE', #39389, 15.99999999999999822 ) ;
#16717=VERTEX_POINT ( 'NONE', #47096 ) ;
#16723=DIRECTION ( 'NONE',  ( 0.000000000000000000, 0.000000000000000000, -1.000000000000000000 ) ) ;
#16731=CARTESIAN_POINT ( 'NONE',  ( 10.00000000000000000, -33.17418723428319538, 17.67226234102814431 ) ) ;
#16736=FILL_AREA_STYLE_COLOUR ( '', #4836 ) ;
#16761=CARTESIAN_POINT ( 'NONE',  ( 0.000000000000000000, -17.67226234102801286, -33.17418723428327354 ) ) ;
#16762=EDGE_CURVE ( 'NONE', #42524, #19183, #407, .T. ) ;
#16764=DIRECTION ( 'NONE',  ( -1.000000000000000000, 0.000000000000000000, -0.000000000000000000 ) ) ;
#16766=ORIENTED_EDGE ( 'NONE', *, *, #46032, .T. ) ;
#16770=AXIS2_PLACEMENT_3D ( 'NONE', #48141, #37605, #45198 ) ;
#16774=EDGE_CURVE ( 'NONE', #23667, #12709, #30112, .T. ) ;
#16777=ORIENTED_EDGE ( 'NONE', *, *, #395, .T. ) ;
#16779=ORIENTED_EDGE ( 'NONE', *, *, #1708, .T. ) ;
#16781=CARTESIAN_POINT ( 'NONE',  ( -3.000000000000000000, -14.54903810567676636, 22.19967320028755964 ) ) ;
#16783=CARTESIAN_POINT ( 'NONE',  ( 10.00000000000000000, -10.74501242461258244, -35.92658777277521409 ) ) ;
#16792=VECTOR ( 'NONE', #10764, 1000.000000000000000 ) ;
#16793=DIRECTION ( 'NONE',  ( -1.000000000000000000, -0.000000000000000000, 0.000000000000000000 ) ) ;
#16802=AXIS2_PLACEMENT_3D ( 'NONE', #8207, #5019, #34872 ) ;
#16814=ORIENTED_EDGE ( 'NONE', *, *, #9387, .F. ) ;
#16819=ORIENTED_EDGE ( 'NONE', *, *, #42067, .T. ) ;
#16820=ORIENTED_EDGE ( 'NONE', *, *, #34810, .F. ) ;
#16825=ORIENTED_EDGE ( 'NONE', *, *, #39417, .F. ) ;
#16839=DIRECTION ( 'NONE',  ( 0.000000000000000000, 0.1045284632676436315, 0.9945218953682742891 ) ) ;
#16853=CARTESIAN_POINT ( 'NONE',  ( 0.000000000000000000, 22.07842321921481243, 8.187992925817422218 ) ) ;
#16860=LINE ( 'NONE', #23964, #6189 ) ;
#16862=AXIS2_PLACEMENT_3D ( 'NONE', #38278, #45878, #8896 ) ;
#16867=ADVANCED_FACE ( 'NONE', ( #32876 ), #7433, .T. ) ;
#16871=ORIENTED_EDGE ( 'NONE', *, *, #33546, .T. ) ;
#16885=ORIENTED_EDGE ( 'NONE', *, *, #32644, .F. ) ;
#16887=ORIENTED_EDGE ( 'NONE', *, *, #13504, .F. ) ;
#16889=DIRECTION ( 'NONE',  ( 0.000000000000000000, -0.9945218953682741780, 0.1045284632676447972 ) ) ;
#16890=DIRECTION ( 'NONE',  ( -1.000000000000000000, 0.000000000000000000, 0.000000000000000000 ) ) ;
#16894=ORIENTED_EDGE ( 'NONE', *, *, #4744, .T. ) ;
#16909=DIRECTION ( 'NONE',  ( -1.000000000000000000, -0.000000000000000000, 0.000000000000000000 ) ) ;
#16920=CARTESIAN_POINT ( 'NONE',  ( 10.00000000000000000, -36.88895765772637247, 6.736453364083436313 ) ) ;
#16926=DIRECTION ( 'NONE',  ( -1.000000000000000000, 0.000000000000000000, -0.000000000000000000 ) ) ;
#16936=AXIS2_PLACEMENT_3D ( 'NONE', #20568, #13952, #35508 ) ;
#16949=CARTESIAN_POINT ( 'NONE',  ( -3.000000000000000000, 18.84667830672579925, 18.68964196561269020 ) ) ;
#16952=ORIENTED_EDGE ( 'NONE', *, *, #25908, .T. ) ;
#16957=EDGE_CURVE ( 'NONE', #36861, #36640, #36322, .T. ) ;
#16959=CARTESIAN_POINT ( 'NONE',  ( -3.000000000000000000, 23.50000000000000000, -1.500000000000001332 ) ) ;
#16969=CARTESIAN_POINT ( 'NONE',  ( 0.000000000000000000, 26.50000000000000711, 1.500000000000000000 ) ) ;
#16971=LINE ( 'NONE', #9148, #31850 ) ;
#16979=VERTEX_POINT ( 'NONE', #41681 ) ;
#16997=ORIENTED_EDGE ( 'NONE', *, *, #43345, .F. ) ;
#17007=FACE_BOUND ( 'NONE', #30756, .T. ) ;
#17010=FACE_OUTER_BOUND ( 'NONE', #38058, .T. ) ;
#17013=ADVANCED_FACE ( 'NONE', ( #19871 ), #38491, .T. ) ;
#17014=DIRECTION ( 'NONE',  ( -1.000000000000000000, 0.000000000000000000, 0.000000000000000000 ) ) ;
#17018=CARTESIAN_POINT ( 'NONE',  ( 0.000000000000000000, 0.000000000000000000, 0.000000000000000000 ) ) ;
#17023=DIRECTION ( 'NONE',  ( 0.000000000000000000, 0.000000000000000000, 1.000000000000000000 ) ) ;
#17031=VERTEX_POINT ( 'NONE', #11359 ) ;
#17039=ORIENTED_EDGE ( 'NONE', *, *, #31071, .T. ) ;
#17042=ORIENTED_EDGE ( 'NONE', *, *, #27768, .F. ) ;
#17049=FACE_OUTER_BOUND ( 'NONE', #21792, .T. ) ;
#17057=ORIENTED_EDGE ( 'NONE', *, *, #14549, .T. ) ;
#17058=ORIENTED_EDGE ( 'NONE', *, *, #6599, .F. ) ;
#17061=LINE ( 'NONE', #46207, #11099 ) ;
#17074=DIRECTION ( 'NONE',  ( -1.000000000000000000, 0.000000000000000000, 0.000000000000000000 ) ) ;
#17086=CARTESIAN_POINT ( 'NONE',  ( 10.00000000000000000, -37.01155633439063308, 6.555932627142289526 ) ) ;
#17096=ORIENTED_EDGE ( 'NONE', *, *, #34137, .F. ) ;
#17105=ORIENTED_EDGE ( 'NONE', *, *, #45881, .T. ) ;
#17114=ORIENTED_EDGE ( 'NONE', *, *, #10678, .T. ) ;
#17115=CARTESIAN_POINT ( 'NONE',  ( 0.000000000000000000, 37.01155633439068282, -6.555932627142014191 ) ) ;
#17119=PLANE ( 'NONE',  #41095 ) ;
#17120=DIRECTION ( 'NONE',  ( 0.000000000000000000, -0.8090169943749531134, 0.5877852522924653655 ) ) ;
#17122=EDGE_CURVE ( 'NONE', #36907, #17574, #17620, .T. ) ;
#17124=ORIENTED_EDGE ( 'NONE', *, *, #8119, .T. ) ;
#17126=DIRECTION ( 'NONE',  ( 0.000000000000000000, 0.000000000000000000, 1.000000000000000000 ) ) ;
#17128=PLANE ( 'NONE',  #37369 ) ;
#17130=VERTEX_POINT ( 'NONE', #2243 ) ;
#17131=EDGE_CURVE ( 'NONE', #7846, #12203, #16704, .T. ) ;
#17136=CYLINDRICAL_SURFACE ( 'NONE', #40236, 42.00000000000000000 ) ;
#17142=AXIS2_PLACEMENT_3D ( 'NONE', #30208, #7909, #22842 ) ;
#17143=CARTESIAN_POINT ( 'NONE',  ( 10.00000000000000000, -37.58145647212455032, 0.6853352020789044152 ) ) ;
#17150=DIRECTION ( 'NONE',  ( 0.000000000000000000, 0.9876883405951382144, -0.1564344650402276493 ) ) ;
#17153=ORIENTED_EDGE ( 'NONE', *, *, #24692, .F. ) ;
#17165=EDGE_LOOP ( 'NONE', ( #38644, #546, #43154, #27375 ) ) ;
#17166=EDGE_CURVE ( 'NONE', #30366, #16979, #5942, .T. ) ;
#17168=ORIENTED_EDGE ( 'NONE', *, *, #35791, .F. ) ;
#17172=DIRECTION ( 'NONE',  ( 0.000000000000000000, -0.1564344650402170744, -0.9876883405951398798 ) ) ;
#17184=CARTESIAN_POINT ( 'NONE',  ( -3.000000000000000000, 6.762365576493643893, -25.66652317338391853 ) ) ;
#17185=EDGE_LOOP ( 'NONE', ( #971, #18847, #39714, #2089 ) ) ;
#17187=DIRECTION ( 'NONE',  ( 0.000000000000000000, -0.7431448254773954654, 0.6691306063588569053 ) ) ;
#17195=( NAMED_UNIT ( * ) PLANE_ANGLE_UNIT ( ) SI_UNIT ( $, .RADIAN. ) );
#17198=DIRECTION ( 'NONE',  ( 1.000000000000000000, -0.000000000000000000, 0.000000000000000000 ) ) ;
#17221=AXIS2_PLACEMENT_3D ( 'NONE', #28684, #2719, #44081 ) ;
#17229=DIRECTION ( 'NONE',  ( 0.000000000000000000, -0.8090169943749508930, 0.5877852522924682521 ) ) ;
#17230=FACE_OUTER_BOUND ( 'NONE', #4878, .T. ) ;
#17233=VERTEX_POINT ( 'NONE', #35053 ) ;
#17235=CARTESIAN_POINT ( 'NONE',  ( 10.00000000000000000, 0.000000000000000000, 0.000000000000000000 ) ) ;
#17240=CARTESIAN_POINT ( 'NONE',  ( 0.000000000000000000, 0.000000000000000000, 0.000000000000000000 ) ) ;
#17268=ADVANCED_FACE ( 'NONE', ( #5445 ), #24281, .T. ) ;
#17279=VERTEX_POINT ( 'NONE', #29145 ) ;
#17287=DIRECTION ( 'NONE',  ( -1.000000000000000000, 0.000000000000000000, 0.000000000000000000 ) ) ;
#17291=CARTESIAN_POINT ( 'NONE',  ( 0.000000000000000000, -6.736453364083290651, -36.88895765772640090 ) ) ;
#17296=DIRECTION ( 'NONE',  ( -1.000000000000000000, -0.000000000000000000, -0.000000000000000000 ) ) ;
#17299=CARTESIAN_POINT ( 'NONE',  ( 0.000000000000000000, 30.80686688397010542, 21.53537804866092387 ) ) ;
#17310=CARTESIAN_POINT ( 'NONE',  ( -3.000000000000000000, 5.835314593368477354, 22.81335362449854642 ) ) ;
#17315=ORIENTED_EDGE ( 'NONE', *, *, #44478, .F. ) ;
#17316=CARTESIAN_POINT ( 'NONE',  ( -3.000000000000000000, 14.60985201121729737, -18.46759930825687945 ) ) ;
#17323=ORIENTED_EDGE ( 'NONE', *, *, #26246, .T. ) ;
#17332=EDGE_CURVE ( 'NONE', #7964, #5993, #36837, .T. ) ;
#17334=ADVANCED_FACE ( 'NONE', ( #40904 ), #3693, .T. ) ;
#17341=CARTESIAN_POINT ( 'NONE',  ( 10.00000000000000000, -35.92658777277517856, 10.74501242461269257 ) ) ;
#17342=VERTEX_POINT ( 'NONE', #44330 ) ;
#17356=DIRECTION ( 'NONE',  ( 0.000000000000000000, 0.7071067811865487940, -0.7071067811865462405 ) ) ;
#17360=DIRECTION ( 'NONE',  ( 0.000000000000000000, -0.3090169943749548342, 0.9510565162951511997 ) ) ;
#17367=DIRECTION ( 'NONE',  ( 0.000000000000000000, 0.000000000000000000, 1.000000000000000000 ) ) ;
#17368=VECTOR ( 'NONE', #46342, 1000.000000000000000 ) ;
#17388=EDGE_CURVE ( 'NONE', #27870, #46797, #38197, .T. ) ;
#17398=ORIENTED_EDGE ( 'NONE', *, *, #4039, .T. ) ;
#17403=VERTEX_POINT ( 'NONE', #248 ) ;
#17407=ORIENTED_EDGE ( 'NONE', *, *, #46634, .T. ) ;
#17432=ORIENTED_EDGE ( 'NONE', *, *, #21547, .F. ) ;
#17434=CARTESIAN_POINT ( 'NONE',  ( -3.000000000000000000, -22.67460108101783334, 6.353146135317912169 ) ) ;
#17435=CARTESIAN_POINT ( 'NONE',  ( -3.000000000000000000, -18.13022148937263012, 15.02647892043544608 ) ) ;
#17438=AXIS2_PLACEMENT_3D ( 'NONE', #28810, #40791, #29298 ) ;
#17450=CARTESIAN_POINT ( 'NONE',  ( 10.00000000000000000, -16.65560815589383381, -38.55633173627028754 ) ) ;
#17457=CYLINDRICAL_SURFACE ( 'NONE', #27748, 42.00000000000000000 ) ;
#17478=ORIENTED_EDGE ( 'NONE', *, *, #42634, .T. ) ;
#17491=DIRECTION ( 'NONE',  ( -1.000000000000000000, 0.000000000000000000, 0.000000000000000000 ) ) ;
#17502=DIRECTION ( 'NONE',  ( -1.000000000000000000, 0.000000000000000000, -0.000000000000000000 ) ) ;
#17505=CARTESIAN_POINT ( 'NONE',  ( 10.00000000000000000, 22.74946021919175720, -29.81001611430984255 ) ) ;
#17508=AXIS2_PLACEMENT_3D ( 'NONE', #33739, #15633, #7574 ) ;
#17510=CIRCLE ( 'NONE', #23771, 16.00000000000000000 ) ;
#17522=CARTESIAN_POINT ( 'NONE',  ( 5.000000000000000000, -36.13751322684404244, -21.40280677340410165 ) ) ;
#17526=DIRECTION ( 'NONE',  ( 0.000000000000000000, -0.4539904997395540764, 0.8910065241883642351 ) ) ;
#17527=DIRECTION ( 'NONE',  ( -1.000000000000000000, -0.000000000000000000, 0.000000000000000000 ) ) ;
#17529=EDGE_CURVE ( 'NONE', #15797, #38112, #7944, .T. ) ;
#17530=ORIENTED_EDGE ( 'NONE', *, *, #4499, .T. ) ;
#17537=FACE_OUTER_BOUND ( 'NONE', #10294, .T. ) ;
#17541=CARTESIAN_POINT ( 'NONE',  ( 10.00000000000000000, 16.23288003029543347, -33.80338159004267595 ) ) ;
#17543=CARTESIAN_POINT ( 'NONE',  ( 0.000000000000000000, 0.000000000000000000, 0.000000000000000000 ) ) ;
#17547=DIRECTION ( 'NONE',  ( 0.000000000000000000, 0.000000000000000000, -1.000000000000000000 ) ) ;
#17552=VECTOR ( 'NONE', #17527, 1000.000000000000000 ) ;
#17553=AXIS2_PLACEMENT_3D ( 'NONE', #36472, #37198, #7334 ) ;
#17559=CYLINDRICAL_SURFACE ( 'NONE', #43375, 42.00000000000000000 ) ;
#17572=EDGE_CURVE ( 'NONE', #17403, #31111, #32181, .T. ) ;
#17573=ADVANCED_FACE ( 'NONE', ( #35486 ), #1972, .T. ) ;
#17574=VERTEX_POINT ( 'NONE', #35000 ) ;
#17575=ORIENTED_EDGE ( 'NONE', *, *, #31573, .F. ) ;
#17576=VECTOR ( 'NONE', #28335, 1000.000000000000114 ) ;
#17590=AXIS2_PLACEMENT_3D ( 'NONE', #46880, #2316, #13580 ) ;
#17608=ORIENTED_EDGE ( 'NONE', *, *, #11570, .T. ) ;
#17610=CARTESIAN_POINT ( 'NONE',  ( -3.000000000000000000, -10.45096189432344147, 21.10159698893426494 ) ) ;
#17618=EDGE_CURVE ( 'NONE', #13751, #34159, #20299, .T. ) ;
#17619=CYLINDRICAL_SURFACE ( 'NONE', #26307, 16.00000000000000000 ) ;
#17620=CIRCLE ( 'NONE', #34040, 42.00000000000000000 ) ;
#17621=VECTOR ( 'NONE', #44152, 1000.000000000000000 ) ;
#17622=DIRECTION ( 'NONE',  ( 0.000000000000000000, 0.3090169943749482839, -0.9510565162951533091 ) ) ;
#17624=VECTOR ( 'NONE', #11127, 1000.000000000000000 ) ;
#17636=LINE ( 'NONE', #10289, #28406 ) ;
#17647=DIRECTION ( 'NONE',  ( 0.000000000000000000, 0.000000000000000000, 1.000000000000000000 ) ) ;
#17654=DIRECTION ( 'NONE',  ( -1.000000000000000000, 0.000000000000000000, 0.000000000000000000 ) ) ;
#17659=DIRECTION ( 'NONE',  ( 0.000000000000000000, 0.000000000000000000, 1.000000000000000000 ) ) ;
#17667=CIRCLE ( 'NONE', #490, 16.00000000000000000 ) ;
#17669=ORIENTED_EDGE ( 'NONE', *, *, #3035, .T. ) ;
#17672=CYLINDRICAL_SURFACE ( 'NONE', #26274, 16.00000000000000000 ) ;
#17673=ORIENTED_EDGE ( 'NONE', *, *, #23446, .T. ) ;
#17674=EDGE_CURVE ( 'NONE', #24885, #40287, #20491, .T. ) ;
#17677=CARTESIAN_POINT ( 'NONE',  ( 10.00000000000000000, -35.47612816024539484, 22.48208911017487921 ) ) ;
#17690=CARTESIAN_POINT ( 'NONE',  ( 0.000000000000000000, -10.96151621346514382, 35.95386929396252640 ) ) ;
#17695=LINE ( 'NONE', #28229, #1757 ) ;
#17697=ORIENTED_EDGE ( 'NONE', *, *, #26310, .T. ) ;
#17698=AXIS2_PLACEMENT_3D ( 'NONE', #1655, #23204, #8999 ) ;
#17703=VECTOR ( 'NONE', #28162, 1000.000000000000000 ) ;
#17704=DIRECTION ( 'NONE',  ( 0.000000000000000000, -0.3090169943749460635, -0.9510565162951539753 ) ) ;
#17713=DIRECTION ( 'NONE',  ( -1.000000000000000000, 0.000000000000000000, 0.000000000000000000 ) ) ;
#17715=CARTESIAN_POINT ( 'NONE',  ( 10.00000000000000000, 37.48860685352291000, 0.8828120875901893649 ) ) ;
#17716=CARTESIAN_POINT ( 'NONE',  ( 0.000000000000000000, 23.59884966291538078, -12.14883922797231541 ) ) ;
#17719=VERTEX_POINT ( 'NONE', #21748 ) ;
#17722=DIRECTION ( 'NONE',  ( 0.000000000000000000, -0.1564344650402172410, -0.9876883405951399908 ) ) ;
#17724=AXIS2_PLACEMENT_3D ( 'NONE', #48129, #29531, #30014 ) ;
#17735=ORIENTED_EDGE ( 'NONE', *, *, #22285, .T. ) ;
#17736=EDGE_CURVE ( 'NONE', #11877, #14823, #40595, .T. ) ;
#17758=VERTEX_POINT ( 'NONE', #29582 ) ;
#17760=ORIENTED_EDGE ( 'NONE', *, *, #25070, .F. ) ;
#17772=ORIENTED_EDGE ( 'NONE', *, *, #38867, .F. ) ;
#17780=EDGE_LOOP ( 'NONE', ( #29348, #8957, #35898, #44177 ) ) ;
#17782=ORIENTED_EDGE ( 'NONE', *, *, #9387, .T. ) ;
#17792=ADVANCED_FACE ( 'NONE', ( #33491 ), #7301, .F. ) ;
#17801=CARTESIAN_POINT ( 'NONE',  ( 10.00000000000000000, 0.000000000000000000, 0.000000000000000000 ) ) ;
#17809=DIRECTION ( 'NONE',  ( -1.000000000000000000, -0.000000000000000000, -0.000000000000000000 ) ) ;
#17813=ORIENTED_EDGE ( 'NONE', *, *, #20064, .F. ) ;
#17815=FACE_OUTER_BOUND ( 'NONE', #9706, .T. ) ;
#17818=AXIS2_PLACEMENT_3D ( 'NONE', #47642, #16654, #38445 ) ;
#17830=CARTESIAN_POINT ( 'NONE',  ( -3.000000000000000000, -13.04903810567647682, -19.60159698893442481 ) ) ;
#17838=EDGE_CURVE ( 'NONE', #20905, #8546, #4606, .T. ) ;
#17842=VECTOR ( 'NONE', #37011, 1000.000000000000000 ) ;
#17847=DIRECTION ( 'NONE',  ( 0.000000000000000000, 0.000000000000000000, 1.000000000000000000 ) ) ;
#17848=CARTESIAN_POINT ( 'NONE',  ( -3.000000000000000000, -11.95096189432345390, 23.69967320028757385 ) ) ;
#17849=ORIENTED_EDGE ( 'NONE', *, *, #15905, .F. ) ;
#17853=DIRECTION ( 'NONE',  ( -1.000000000000000000, -0.000000000000000000, -0.000000000000000000 ) ) ;
#17854=CARTESIAN_POINT ( 'NONE',  ( 10.00000000000000000, 0.000000000000000000, 0.000000000000000000 ) ) ;
#17856=CARTESIAN_POINT ( 'NONE',  ( -3.000000000000000000, 23.50000000000000000, -1.500000000000001332 ) ) ;
#17874=ADVANCED_FACE ( 'NONE', ( #22248 ), #22489, .F. ) ;
#17877=EDGE_CURVE ( 'NONE', #38831, #27191, #30078, .T. ) ;
#17878=ORIENTED_EDGE ( 'NONE', *, *, #39758, .T. ) ;
#17890=DIRECTION ( 'NONE',  ( -1.000000000000000000, -0.000000000000000000, 0.000000000000000000 ) ) ;
#17913=EDGE_CURVE ( 'NONE', #28068, #26813, #28291, .T. ) ;
#17915=LINE ( 'NONE', #3479, #44247 ) ;
#17924=ORIENTED_EDGE ( 'NONE', *, *, #29336, .F. ) ;
#17927=DIRECTION ( 'NONE',  ( 1.000000000000000000, 0.000000000000000000, 0.000000000000000000 ) ) ;
#17928=CIRCLE ( 'NONE', #36685, 15.99999999999999822 ) ;
#17929=ORIENTED_EDGE ( 'NONE', *, *, #40629, .T. ) ;
#17947=DIRECTION ( 'NONE',  ( -1.000000000000000000, 0.000000000000000000, 0.000000000000000000 ) ) ;
#17958=DIRECTION ( 'NONE',  ( 0.000000000000000000, 0.000000000000000000, 1.000000000000000000 ) ) ;
#17974=DIRECTION ( 'NONE',  ( -0.000000000000000000, -1.000000000000000000, -0.000000000000000000 ) ) ;
#17977=EDGE_CURVE ( 'NONE', #40081, #18029, #17061, .T. ) ;
#17978=DIRECTION ( 'NONE',  ( 0.000000000000000000, 0.4067366430758017626, -0.9135454576426003115 ) ) ;
#17984=ORIENTED_EDGE ( 'NONE', *, *, #6759, .T. ) ;
#17989=AXIS2_PLACEMENT_3D ( 'NONE', #23881, #39552, #1609 ) ;
#17999=EDGE_CURVE ( 'NONE', #17342, #22498, #43737, .T. ) ;
#18008=DIRECTION ( 'NONE',  ( -1.000000000000000000, -0.000000000000000000, -0.000000000000000000 ) ) ;
#18021=CARTESIAN_POINT ( 'NONE',  ( 10.00000000000000000, 0.000000000000000000, 0.000000000000000000 ) ) ;
#18022=CARTESIAN_POINT ( 'NONE',  ( -3.000000000000000000, 5.835314593368477354, 22.81335362449854642 ) ) ;
#18023=DIRECTION ( 'NONE',  ( 1.000000000000000000, 0.000000000000000000, 0.000000000000000000 ) ) ;
#18029=VERTEX_POINT ( 'NONE', #39608 ) ;
#18044=ORIENTED_EDGE ( 'NONE', *, *, #25461, .T. ) ;
#18045=ORIENTED_EDGE ( 'NONE', *, *, #14149, .F. ) ;
#18048=ORIENTED_EDGE ( 'NONE', *, *, #34137, .T. ) ;
#18053=AXIS2_PLACEMENT_3D ( 'NONE', #13296, #42920, #47065 ) ;
#18067=EDGE_LOOP ( 'NONE', ( #37669, #12732, #24902, #13676 ) ) ;
#18081=DIRECTION ( 'NONE',  ( 1.000000000000000000, 0.000000000000000000, -0.000000000000000000 ) ) ;
#18087=DIRECTION ( 'NONE',  ( 1.000000000000000000, 0.000000000000000000, 0.000000000000000000 ) ) ;
#18089=FACE_OUTER_BOUND ( 'NONE', #7498, .T. ) ;
#18099=CIRCLE ( 'NONE', #11867, 16.00000000000000000 ) ;
#18100=ADVANCED_FACE ( 'NONE', ( #44879 ), #22372, .F. ) ;
#18104=VERTEX_POINT ( 'NONE', #46933 ) ;
#18110=ADVANCED_FACE ( 'NONE', ( #47168 ), #40722, .T. ) ;
#18117=ORIENTED_EDGE ( 'NONE', *, *, #30904, .T. ) ;
#18119=CYLINDRICAL_SURFACE ( 'NONE', #20644, 37.49900000000000233 ) ;
#18120=ORIENTED_EDGE ( 'NONE', *, *, #1446, .T. ) ;
#18127=CARTESIAN_POINT ( 'NONE',  ( 0.000000000000000000, -12.42422080174614862, -35.38097989696524337 ) ) ;
#18134=ORIENTED_EDGE ( 'NONE', *, *, #41444, .T. ) ;
#18140=CARTESIAN_POINT ( 'NONE',  ( -3.000000000000000000, -10.45096189432344147, 21.10159698893426494 ) ) ;
#18142=DIRECTION ( 'NONE',  ( -0.000000000000000000, 0.8090169943749426773, 0.5877852522924797984 ) ) ;
#18149=DIRECTION ( 'NONE',  ( 0.000000000000000000, -0.8660254037844363761, -0.5000000000000039968 ) ) ;
#18155=CARTESIAN_POINT ( 'NONE',  ( 0.000000000000000000, -3.948201729842348850, 23.21447184625293048 ) ) ;
#18163=DIRECTION ( 'NONE',  ( 0.000000000000000000, -0.9876883405951393247, 0.1564344650402207104 ) ) ;
#18166=VECTOR ( 'NONE', #14900, 1000.000000000000000 ) ;
#18170=EDGE_CURVE ( 'NONE', #26953, #14880, #39833, .T. ) ;
#18171=AXIS2_PLACEMENT_3D ( 'NONE', #28526, #13587, #39786 ) ;
#18178=ADVANCED_FACE ( 'NONE', ( #38260 ), #34324, .T. ) ;
#18184=CARTESIAN_POINT ( 'NONE',  ( 10.00000000000000000, 17.80606268964585226, -33.00180498840028775 ) ) ;
#18187=FACE_OUTER_BOUND ( 'NONE', #23273, .T. ) ;
#18193=CIRCLE ( 'NONE', #34607, 16.00000000000000000 ) ;
#18194=ORIENTED_EDGE ( 'NONE', *, *, #43667, .F. ) ;
#18195=LINE ( 'NONE', #33387, #10744 ) ;
#18196=ORIENTED_EDGE ( 'NONE', *, *, #26791, .T. ) ;
#18202=CARTESIAN_POINT ( 'NONE',  ( 0.000000000000000000, -0.9646360437372163421, -23.52805723605591126 ) ) ;
#18204=DIRECTION ( 'NONE',  ( 1.000000000000000000, 0.000000000000000000, 0.000000000000000000 ) ) ;
#18232=AXIS2_PLACEMENT_3D ( 'NONE', #44411, #37060, #45139 ) ;
#18236=DIRECTION ( 'NONE',  ( -1.000000000000000000, 0.000000000000000000, -0.000000000000000000 ) ) ;
#18242=VECTOR ( 'NONE', #2816, 1000.000000000000000 ) ;
#18243=DIRECTION ( 'NONE',  ( -1.000000000000000000, 0.000000000000000000, 0.000000000000000000 ) ) ;
#18251=ORIENTED_EDGE ( 'NONE', *, *, #25417, .T. ) ;
#18253=VECTOR ( 'NONE', #41340, 999.9999999999998863 ) ;
#18265=CARTESIAN_POINT ( 'NONE',  ( 4.999999999999999112, -10.41901085202050581, -40.68715046381939970 ) ) ;
#18273=DIRECTION ( 'NONE',  ( 0.000000000000000000, 0.000000000000000000, 1.000000000000000000 ) ) ;
#18280=EDGE_LOOP ( 'NONE', ( #14820, #23865, #23913, #35128 ) ) ;
#18290=EDGE_CURVE ( 'NONE', #47513, #46797, #6222, .T. ) ;
#18293=AXIS2_PLACEMENT_3D ( 'NONE', #1119, #41523, #31241 ) ;
#18295=( NAMED_UNIT ( * ) PLANE_ANGLE_UNIT ( ) SI_UNIT ( $, .RADIAN. ) );
#18300=CARTESIAN_POINT ( 'NONE',  ( 10.00000000000000000, 27.05870788708231700, 26.08949754953034272 ) ) ;
#18302=ORIENTED_EDGE ( 'NONE', *, *, #47616, .T. ) ;
#18307=VECTOR ( 'NONE', #21157, 1000.000000000000000 ) ;
#18308=EDGE_LOOP ( 'NONE', ( #34431, #36689, #43659, #37651 ) ) ;
#18316=ORIENTED_EDGE ( 'NONE', *, *, #1011, .T. ) ;
#18318=EDGE_LOOP ( 'NONE', ( #26221, #45793, #11025, #40642 ) ) ;
#18323=DIRECTION ( 'NONE',  ( 1.000000000000000000, 0.000000000000000000, -0.000000000000000000 ) ) ;
#18329=EDGE_CURVE ( 'NONE', #23892, #15601, #38288, .T. ) ;
#18338=CARTESIAN_POINT ( 'NONE',  ( 0.000000000000000000, 0.000000000000000000, 0.000000000000000000 ) ) ;
#18340=EDGE_LOOP ( 'NONE', ( #34656, #24659, #26267, #35334 ) ) ;
#18367=ORIENTED_EDGE ( 'NONE', *, *, #2636, .T. ) ;
#18370=ORIENTED_EDGE ( 'NONE', *, *, #13761, .T. ) ;
#18379=AXIS2_PLACEMENT_3D ( 'NONE', #26765, #8634, #34831 ) ;
#18385=EDGE_LOOP ( 'NONE', ( #6824, #46185, #40472, #44104 ) ) ;
#18390=CARTESIAN_POINT ( 'NONE',  ( 10.00000000000000000, 33.00180498840072829, -17.80606268964504935 ) ) ;
#18397=CARTESIAN_POINT ( 'NONE',  ( 0.000000000000000000, 9.188173127307898369, -40.98264845739739570 ) ) ;
#18402=CARTESIAN_POINT ( 'NONE',  ( -3.000000000000000000, 8.688484142253939169, 21.88630264137371029 ) ) ;
#18408=ADVANCED_FACE ( 'NONE', ( #39225 ), #9843, .F. ) ;
#18445=CIRCLE ( 'NONE', #15319, 16.00000000000000000 ) ;
#18457=DIRECTION ( 'NONE',  ( -1.000000000000000000, -0.000000000000000000, 0.000000000000000000 ) ) ;
#18461=FACE_OUTER_BOUND ( 'NONE', #24857, .T. ) ;
#18466=CARTESIAN_POINT ( 'NONE',  ( 4.999999999999999112, -38.55633173627022359, 16.65560815589396526 ) ) ;
#18468=CIRCLE ( 'NONE', #2838, 37.49900000000001654 ) ;
#18481=AXIS2_PLACEMENT_3D ( 'NONE', #45022, #11498, #4147 ) ;
#18487=ORIENTED_EDGE ( 'NONE', *, *, #5321, .F. ) ;
#18522=EDGE_CURVE ( 'NONE', #44892, #3614, #8575, .T. ) ;
#18533=DIRECTION ( 'NONE',  ( 0.000000000000000000, -0.8910065241883722287, 0.4539904997395382558 ) ) ;
#18538=AXIS2_PLACEMENT_3D ( 'NONE', #30937, #45862, #11836 ) ;
#18553=VERTEX_POINT ( 'NONE', #14485 ) ;
#18569=AXIS2_PLACEMENT_3D ( 'NONE', #5359, #29552, #14637 ) ;
#18584=CYLINDRICAL_SURFACE ( 'NONE', #45635, 16.00000000000000000 ) ;
#18585=FACE_OUTER_BOUND ( 'NONE', #22518, .T. ) ;
#18596=CARTESIAN_POINT ( 'NONE',  ( 0.000000000000000000, 29.81001611431041098, -22.74946021919100403 ) ) ;
#18597=FACE_OUTER_BOUND ( 'NONE', #13848, .T. ) ;
#18600=ORIENTED_EDGE ( 'NONE', *, *, #41127, .F. ) ;
#18604=CARTESIAN_POINT ( 'NONE',  ( -3.000000000000000000, -19.89357724624987256, -12.59942793731086041 ) ) ;
#18606=VECTOR ( 'NONE', #38623, 1000.000000000000000 ) ;
#18609=CARTESIAN_POINT ( 'NONE',  ( -3.000000000000000000, 5.835314593368477354, 22.81335362449854642 ) ) ;
#18625=CARTESIAN_POINT ( 'NONE',  ( -3.000000000000000000, -14.54903810567676636, 22.19967320028755964 ) ) ;
#18627=EDGE_LOOP ( 'NONE', ( #47946, #27956, #8200, #28816 ) ) ;
#18643=DIRECTION ( 'NONE',  ( -0.000000000000000000, -0.9510565162951506446, -0.3090169943749562220 ) ) ;
#18647=CARTESIAN_POINT ( 'NONE',  ( -3.000000000000000000, 0.000000000000000000, 0.000000000000000000 ) ) ;
#18650=CARTESIAN_POINT ( 'NONE',  ( -3.000000000000000000, -1.278221433540502217, 26.51162292216071847 ) ) ;
#18651=CARTESIAN_POINT ( 'NONE',  ( 10.00000000000000000, 10.74501242461333028, -35.92658777277499382 ) ) ;
#18655=AXIS2_PLACEMENT_3D ( 'NONE', #33103, #10346, #25994 ) ;
#18656=ORIENTED_EDGE ( 'NONE', *, *, #7745, .T. ) ;
#18662=CARTESIAN_POINT ( 'NONE',  ( 5.000000000000000000, 27.75498641678786527, -31.52238457039571173 ) ) ;
#18663=EDGE_LOOP ( 'NONE', ( #5386, #14218, #12802, #17929 ) ) ;
#18667=AXIS2_PLACEMENT_3D ( 'NONE', #29565, #10233, #47443 ) ;
#18671=CARTESIAN_POINT ( 'NONE',  ( 0.000000000000000000, 37.58145647212453611, 0.6853352020791767529 ) ) ;
#18673=DIRECTION ( 'NONE',  ( -1.000000000000000000, -0.000000000000000000, -0.000000000000000000 ) ) ;
#18675=ORIENTED_EDGE ( 'NONE', *, *, #3360, .T. ) ;
#18684=ORIENTED_EDGE ( 'NONE', *, *, #27877, .F. ) ;
#18687=EDGE_CURVE ( 'NONE', #293, #47513, #6285, .T. ) ;
#18688=DIRECTION ( 'NONE',  ( 0.000000000000000000, 0.000000000000000000, 1.000000000000000000 ) ) ;
#18697=VECTOR ( 'NONE', #18142, 999.9999999999998863 ) ;
#18700=CARTESIAN_POINT ( 'NONE',  ( 0.000000000000000000, 25.88420570971438650, -27.13269053701069566 ) ) ;
#18703=CARTESIAN_POINT ( 'NONE',  ( -10.00000000000000000, 0.000000000000000000, 0.000000000000000000 ) ) ;
#18718=EDGE_CURVE ( 'NONE', #32747, #14823, #14103, .T. ) ;
#18738=DIRECTION ( 'NONE',  ( -1.000000000000000000, 0.000000000000000000, -0.000000000000000000 ) ) ;
#18746=DIRECTION ( 'NONE',  ( 1.000000000000000000, -0.000000000000000000, -0.000000000000000000 ) ) ;
#18747=ORIENTED_EDGE ( 'NONE', *, *, #3518, .T. ) ;
#18754=ORIENTED_EDGE ( 'NONE', *, *, #19765, .T. ) ;
#18758=DIRECTION ( 'NONE',  ( -1.000000000000000000, -0.000000000000000000, 0.000000000000000000 ) ) ;
#18768=DIRECTION ( 'NONE',  ( 0.000000000000000000, 0.000000000000000000, 1.000000000000000000 ) ) ;
#18774=ORIENTED_EDGE ( 'NONE', *, *, #25222, .T. ) ;
#18777=VERTEX_POINT ( 'NONE', #11542 ) ;
#18789=ORIENTED_EDGE ( 'NONE', *, *, #29022, .T. ) ;
#18792=ORIENTED_EDGE ( 'NONE', *, *, #22325, .T. ) ;
#18796=DIRECTION ( 'NONE',  ( -1.000000000000000000, 0.000000000000000000, 0.000000000000000000 ) ) ;
#18800=ORIENTED_EDGE ( 'NONE', *, *, #30500, .F. ) ;
#18825=AXIS2_PLACEMENT_3D ( 'NONE', #34207, #30538, #45466 ) ;
#18831=CARTESIAN_POINT ( 'NONE',  ( -3.000000000000000000, -22.32062822937489344, 14.36278369418800160 ) ) ;
#18832=ORIENTED_EDGE ( 'NONE', *, *, #29666, .T. ) ;
#18836=ADVANCED_FACE ( 'NONE', ( #46994 ), #8810, .T. ) ;
#18847=ORIENTED_EDGE ( 'NONE', *, *, #11715, .F. ) ;
#18853=DIRECTION ( 'NONE',  ( 0.000000000000000000, -0.9510565162951565288, 0.3090169943749382364 ) ) ;
#18858=VERTEX_POINT ( 'NONE', #35495 ) ;
#18859=DIRECTION ( 'NONE',  ( -1.000000000000000000, 0.000000000000000000, -0.000000000000000000 ) ) ;
#18861=CARTESIAN_POINT ( 'NONE',  ( -3.000000000000000000, -23.29833615347109443, 3.418703333116492438 ) ) ;
#18862=ORIENTED_EDGE ( 'NONE', *, *, #4499, .F. ) ;
#18877=CARTESIAN_POINT ( 'NONE',  ( -3.000000000000000000, -4.261787119644969479, -26.19803753235780519 ) ) ;
#18889=ORIENTED_EDGE ( 'NONE', *, *, #30908, .F. ) ;
#18894=ORIENTED_EDGE ( 'NONE', *, *, #26746, .T. ) ;
#18905=VERTEX_POINT ( 'NONE', #39166 ) ;
#18915=VERTEX_POINT ( 'NONE', #7069 ) ;
#18917=ORIENTED_EDGE ( 'NONE', *, *, #4868, .F. ) ;
#18922=DIRECTION ( 'NONE',  ( -1.000000000000000000, 0.000000000000000000, -0.000000000000000000 ) ) ;
#18933=EDGE_CURVE ( 'NONE', #40387, #2188, #10187, .T. ) ;
#18935=PLANE ( 'NONE',  #36888 ) ;
#18955=ORIENTED_EDGE ( 'NONE', *, *, #28133, .T. ) ;
#18963=DIRECTION ( 'NONE',  ( 0.000000000000000000, 0.000000000000000000, 1.000000000000000000 ) ) ;
#18970=CARTESIAN_POINT ( 'NONE',  ( 10.00000000000000000, 12.26510123303259725, 35.53030884539089840 ) ) ;
#18972=ORIENTED_EDGE ( 'NONE', *, *, #3756, .T. ) ;
#18974=ORIENTED_EDGE ( 'NONE', *, *, #46054, .T. ) ;
#18979=VECTOR ( 'NONE', #32406, 1000.000000000000000 ) ;
#18981=LINE ( 'NONE', #38572, #9993 ) ;
#18997=DIRECTION ( 'NONE',  ( -1.000000000000000000, 0.000000000000000000, 0.000000000000000000 ) ) ;
#18998=AXIS2_PLACEMENT_3D ( 'NONE', #20841, #21299, #2703 ) ;
#19010=AXIS2_PLACEMENT_3D ( 'NONE', #41284, #7739, #26587 ) ;
#19012=EDGE_CURVE ( 'NONE', #1618, #38183, #10992, .T. ) ;
#19026=PLANE ( 'NONE',  #11651 ) ;
#19028=VERTEX_POINT ( 'NONE', #21270 ) ;
#19035=ORIENTED_EDGE ( 'NONE', *, *, #44312, .F. ) ;
#19046=ORIENTED_EDGE ( 'NONE', *, *, #562, .T. ) ;
#19047=ORIENTED_EDGE ( 'NONE', *, *, #39259, .F. ) ;
#19064=CARTESIAN_POINT ( 'NONE',  ( 10.00000000000000000, 29.81001611431041098, -22.74946021919100403 ) ) ;
#19066=ADVANCED_FACE ( 'NONE', ( #43566 ), #10025, .F. ) ;
#19072=CARTESIAN_POINT ( 'NONE',  ( 0.000000000000000000, -35.95386929396264009, 10.96151621346475658 ) ) ;
#19074=AXIS2_PLACEMENT_3D ( 'NONE', #1815, #46846, #27774 ) ;
#19079=CIRCLE ( 'NONE', #17508, 16.00000000000000000 ) ;
#19084=ORIENTED_EDGE ( 'NONE', *, *, #2220, .T. ) ;
#19086=AXIS2_PLACEMENT_3D ( 'NONE', #10270, #17853, #24736 ) ;
#19092=EDGE_LOOP ( 'NONE', ( #30154, #28831, #510, #3627 ) ) ;
#19096=ORIENTED_EDGE ( 'NONE', *, *, #22637, .T. ) ;
#19097=ORIENTED_EDGE ( 'NONE', *, *, #10857, .T. ) ;
#19100=EDGE_CURVE ( 'NONE', #35670, #8149, #692, .T. ) ;
#19110=CARTESIAN_POINT ( 'NONE',  ( -3.000000000000000000, -23.29833615347104825, -3.418703333116803744 ) ) ;
#19124=ADVANCED_FACE ( 'NONE', ( #26894 ), #7794, .T. ) ;
#19128=ORIENTED_EDGE ( 'NONE', *, *, #46717, .T. ) ;
#19130=CARTESIAN_POINT ( 'NONE',  ( 10.00000000000000000, 5.202137450156907761, -37.22597642581151689 ) ) ;
#19135=VECTOR ( 'NONE', #37723, 999.9999999999998863 ) ;
#19138=DIRECTION ( 'NONE',  ( 0.000000000000000000, 0.3090169943749450088, 0.9510565162951544194 ) ) ;
#19139=DIRECTION ( 'NONE',  ( 0.000000000000000000, -0.3090169943749573878, 0.9510565162951503115 ) ) ;
#19141=ORIENTED_EDGE ( 'NONE', *, *, #23990, .F. ) ;
#19145=ORIENTED_EDGE ( 'NONE', *, *, #2127, .T. ) ;
#19148=DIRECTION ( 'NONE',  ( 0.000000000000000000, 0.000000000000000000, 1.000000000000000000 ) ) ;
#19153=VERTEX_POINT ( 'NONE', #30328 ) ;
#19157=CARTESIAN_POINT ( 'NONE',  ( 10.00000000000000000, -35.38097989696503021, -12.42422080174676147 ) ) ;
#19161=EDGE_CURVE ( 'NONE', #44883, #29381, #26412, .T. ) ;
#19180=AXIS2_PLACEMENT_3D ( 'NONE', #41125, #29604, #37927 ) ;
#19181=CARTESIAN_POINT ( 'NONE',  ( 0.000000000000000000, 0.000000000000000000, 0.000000000000000000 ) ) ;
#19183=VERTEX_POINT ( 'NONE', #20757 ) ;
#19193=DIRECTION ( 'NONE',  ( -1.000000000000000000, 0.000000000000000000, 0.000000000000000000 ) ) ;
#19195=LINE ( 'NONE', #30460, #42473 ) ;
#19200=AXIS2_PLACEMENT_3D ( 'NONE', #3752, #19562, #15672 ) ;
#19211=DIRECTION ( 'NONE',  ( -1.000000000000000000, 0.000000000000000000, 0.000000000000000000 ) ) ;
#19221=LINE ( 'NONE', #26809, #35189 ) ;
#19236=DIRECTION ( 'NONE',  ( 0.000000000000000000, 0.000000000000000000, 1.000000000000000000 ) ) ;
#19243=CARTESIAN_POINT ( 'NONE',  ( -3.000000000000000000, -10.45096189432314837, -21.10159698893440350 ) ) ;
#19270=VECTOR ( 'NONE', #24423, 1000.000000000000000 ) ;
#19279=ADVANCED_FACE ( 'NONE', ( #45985 ), #20262, .T. ) ;
#19282=VECTOR ( 'NONE', #10720, 1000.000000000000000 ) ;
#19284=ORIENTED_EDGE ( 'NONE', *, *, #20660, .T. ) ;
#19287=EDGE_LOOP ( 'NONE', ( #26818, #11372, #17984, #18832 ) ) ;
#19295=DIRECTION ( 'NONE',  ( 1.000000000000000000, -0.000000000000000000, -0.000000000000000000 ) ) ;
#19296=CIRCLE ( 'NONE', #34143, 42.00000000000000000 ) ;
#19303=CARTESIAN_POINT ( 'NONE',  ( 0.000000000000000000, 0.000000000000000000, 0.000000000000000000 ) ) ;
#19307=CARTESIAN_POINT ( 'NONE',  ( 4.999999999999999112, 40.68715046381943523, -10.41901085202036370 ) ) ;
#19308=VECTOR ( 'NONE', #36294, 1000.000000000000114 ) ;
#19311=DIRECTION ( 'NONE',  ( 0.000000000000000000, 0.000000000000000000, 1.000000000000000000 ) ) ;
#19316=VECTOR ( 'NONE', #38344, 1000.000000000000000 ) ;
#19318=UNCERTAINTY_MEASURE_WITH_UNIT (LENGTH_MEASURE( 1.000000000000000082E-05 ), #29558, 'distance_accuracy_value', 'NONE');
#19321=PLANE ( 'NONE',  #6527 ) ;
#19327=VECTOR ( 'NONE', #23328, 1000.000000000000114 ) ;
#19331=ORIENTED_EDGE ( 'NONE', *, *, #24364, .F. ) ;
#19332=EDGE_CURVE ( 'NONE', #38183, #32221, #3337, .T. ) ;
#19333=ADVANCED_FACE ( 'NONE', ( #25374 ), #32723, .F. ) ;
#19341=VERTEX_POINT ( 'NONE', #29305 ) ;
#19343=CARTESIAN_POINT ( 'NONE',  ( 10.00000000000000000, -22.74946021919153694, 29.81001611431000597 ) ) ;
#19354=ORIENTED_EDGE ( 'NONE', *, *, #45479, .F. ) ;
#19356=DIRECTION ( 'NONE',  ( 0.000000000000000000, 0.000000000000000000, 1.000000000000000000 ) ) ;
#19359=CARTESIAN_POINT ( 'NONE',  ( 5.000000000000000000, 41.91543099594818500, 2.663952781846291362 ) ) ;
#19370=DIRECTION ( 'NONE',  ( -1.000000000000000000, 0.000000000000000000, 0.000000000000000000 ) ) ;
#19378=LINE ( 'NONE', #778, #1009 ) ;
#19379=EDGE_CURVE ( 'NONE', #25227, #36913, #12605, .T. ) ;
#19394=CIRCLE ( 'NONE', #46784, 42.00000000000000000 ) ;
#19399=EDGE_CURVE ( 'NONE', #40287, #17719, #81, .T. ) ;
#19412=CARTESIAN_POINT ( 'NONE',  ( 10.00000000000000000, 32.34446384430010113, -26.79245525562679831 ) ) ;
#19415=CARTESIAN_POINT ( 'NONE',  ( 0.000000000000000000, -27.05870788708213226, -26.08949754953053102 ) ) ;
#19430=LINE ( 'NONE', #38293, #45542 ) ;
#19437=ORIENTED_EDGE ( 'NONE', *, *, #33298, .T. ) ;
#19455=ORIENTED_EDGE ( 'NONE', *, *, #33801, .T. ) ;
#19457=AXIS2_PLACEMENT_3D ( 'NONE', #176, #11936, #44731 ) ;
#19477=DIRECTION ( 'NONE',  ( 0.000000000000000000, 0.000000000000000000, -1.000000000000000000 ) ) ;
#19489=ORIENTED_EDGE ( 'NONE', *, *, #44041, .F. ) ;
#19490=AXIS2_PLACEMENT_3D ( 'NONE', #41987, #2020, #43599 ) ;
#19491=LINE ( 'NONE', #15602, #16378 ) ;
#19495=AXIS2_PLACEMENT_3D ( 'NONE', #30935, #38027, #8157 ) ;
#19502=DIRECTION ( 'NONE',  ( -1.000000000000000000, 0.000000000000000000, -0.000000000000000000 ) ) ;
#19506=ORIENTED_EDGE ( 'NONE', *, *, #10038, .T. ) ;
#19507=DIRECTION ( 'NONE',  ( 1.000000000000000000, -0.000000000000000000, -0.000000000000000000 ) ) ;
#19510=DIRECTION ( 'NONE',  ( 0.000000000000000000, 0.8910065241883657894, 0.4539904997395509678 ) ) ;
#19517=ORIENTED_EDGE ( 'NONE', *, *, #40656, .T. ) ;
#19530=CARTESIAN_POINT ( 'NONE',  ( 0.000000000000000000, 0.000000000000000000, 0.000000000000000000 ) ) ;
#19534=DIRECTION ( 'NONE',  ( 0.000000000000000000, 0.000000000000000000, 1.000000000000000000 ) ) ;
#19535=DIRECTION ( 'NONE',  ( 0.000000000000000000, 0.8910065241883688980, -0.4539904997395447506 ) ) ;
#19539=VERTEX_POINT ( 'NONE', #13117 ) ;
#19542=EDGE_CURVE ( 'NONE', #3270, #21795, #7810, .T. ) ;
#19551=CIRCLE ( 'NONE', #17989, 42.00000000000000000 ) ;
#19552=CIRCLE ( 'NONE', #25817, 42.00000000000000000 ) ;
#19553=EDGE_LOOP ( 'NONE', ( #6006, #7413, #28435, #9948 ) ) ;
#19555=ORIENTED_EDGE ( 'NONE', *, *, #12780, .F. ) ;
#19557=EDGE_LOOP ( 'NONE', ( #26560, #32815, #38203, #19097 ) ) ;
#19558=AXIS2_PLACEMENT_3D ( 'NONE', #5396, #20307, #35246 ) ;
#19561=VERTEX_POINT ( 'NONE', #38832 ) ;
#19562=DIRECTION ( 'NONE',  ( -1.000000000000000000, 0.000000000000000000, 0.000000000000000000 ) ) ;
#19566=DIRECTION ( 'NONE',  ( -1.000000000000000000, -0.000000000000000000, -0.000000000000000000 ) ) ;
#19573=DIRECTION ( 'NONE',  ( 0.000000000000000000, 0.000000000000000000, 1.000000000000000000 ) ) ;
#19577=DIRECTION ( 'NONE',  ( -1.000000000000000000, 0.000000000000000000, 0.000000000000000000 ) ) ;
#19594=CIRCLE ( 'NONE', #40710, 37.49900000000000944 ) ;
#19599=LINE ( 'NONE', #1008, #47531 ) ;
#19603=EDGE_CURVE ( 'NONE', #24691, #20853, #38330, .T. ) ;
#19604=ORIENTED_EDGE ( 'NONE', *, *, #18329, .T. ) ;
#19622=CIRCLE ( 'NONE', #39992, 15.99999999999999822 ) ;
#19626=AXIS2_PLACEMENT_3D ( 'NONE', #46034, #42352, #31356 ) ;
#19634=ORIENTED_EDGE ( 'NONE', *, *, #34742, .T. ) ;
#19636=VERTEX_POINT ( 'NONE', #10153 ) ;
#19650=CARTESIAN_POINT ( 'NONE',  ( -3.000000000000000000, 14.60985201121704513, 18.46759930825707841 ) ) ;
#19653=DIRECTION ( 'NONE',  ( -1.000000000000000000, 0.000000000000000000, 0.000000000000000000 ) ) ;
#19656=DIRECTION ( 'NONE',  ( 0.000000000000000000, 0.000000000000000000, 1.000000000000000000 ) ) ;
#19667=ORIENTED_EDGE ( 'NONE', *, *, #12819, .T. ) ;
#19681=VERTEX_POINT ( 'NONE', #20938 ) ;
#19683=ORIENTED_EDGE ( 'NONE', *, *, #44385, .F. ) ;
#19697=DIRECTION ( 'NONE',  ( 0.000000000000000000, 0.000000000000000000, -1.000000000000000000 ) ) ;
#19701=CARTESIAN_POINT ( 'NONE',  ( 0.000000000000000000, 0.000000000000000000, 0.000000000000000000 ) ) ;
#19702=EDGE_CURVE ( 'NONE', #25280, #39350, #36098, .T. ) ;
#19703=AXIS2_PLACEMENT_3D ( 'NONE', #406, #1123, #45675 ) ;
#19705=DIRECTION ( 'NONE',  ( -0.000000000000000000, 0.4067366430758000417, -0.9135454576426009776 ) ) ;
#19707=CARTESIAN_POINT ( 'NONE',  ( -3.000000000000000000, 16.83928648764923253, 16.46020748918050458 ) ) ;
#19709=VERTEX_POINT ( 'NONE', #28527 ) ;
#19713=DIRECTION ( 'NONE',  ( 0.000000000000000000, -0.9945218953682730678, -0.1045284632676570791 ) ) ;
#19726=AXIS2_PLACEMENT_3D ( 'NONE', #2060, #39983, #6441 ) ;
#19729=CIRCLE ( 'NONE', #26001, 37.49900000000001654 ) ;
#19735=ORIENTED_EDGE ( 'NONE', *, *, #39417, .T. ) ;
#19743=CARTESIAN_POINT ( 'NONE',  ( 0.000000000000000000, 32.34446384430010113, -26.79245525562679831 ) ) ;
#19745=CARTESIAN_POINT ( 'NONE',  ( 10.00000000000000000, 17.67226234102874116, -33.17418723428288274 ) ) ;
#19753=CARTESIAN_POINT ( 'NONE',  ( 10.00000000000000000, -31.52238457039580055, -27.75498641678775869 ) ) ;
#19754=ORIENTED_EDGE ( 'NONE', *, *, #43384, .F. ) ;
#19756=CARTESIAN_POINT ( 'NONE',  ( 10.00000000000000000, 0.000000000000000000, 0.000000000000000000 ) ) ;
#19764=DIRECTION ( 'NONE',  ( 0.000000000000000000, 0.000000000000000000, 1.000000000000000000 ) ) ;
#19765=EDGE_CURVE ( 'NONE', #26327, #17279, #9574, .T. ) ;
#19777=ORIENTED_EDGE ( 'NONE', *, *, #35148, .F. ) ;
#19782=AXIS2_PLACEMENT_3D ( 'NONE', #29242, #48318, #44172 ) ;
#19785=CIRCLE ( 'NONE', #249, 16.00000000000000000 ) ;
#19787=AXIS2_PLACEMENT_3D ( 'NONE', #11094, #17713, #39767 ) ;
#19796=ORIENTED_EDGE ( 'NONE', *, *, #45881, .F. ) ;
#19804=PRODUCT_DEFINITION_SHAPE ( 'NONE', 'NONE',  #22354 ) ;
#19810=DIRECTION ( 'NONE',  ( -1.000000000000000000, -0.000000000000000000, 0.000000000000000000 ) ) ;
#19815=CIRCLE ( 'NONE', #42520, 37.49900000000000233 ) ;
#19817=ADVANCED_FACE ( 'NONE', ( #25703 ), #28900, .T. ) ;
#19822=VERTEX_POINT ( 'NONE', #10297 ) ;
#19825=ORIENTED_EDGE ( 'NONE', *, *, #44312, .T. ) ;
#19826=DIRECTION ( 'NONE',  ( 1.000000000000000000, 0.000000000000000000, 0.000000000000000000 ) ) ;
#19838=CIRCLE ( 'NONE', #5783, 16.00000000000000000 ) ;
#19845=AXIS2_PLACEMENT_3D ( 'NONE', #20432, #20934, #35852 ) ;
#19847=CARTESIAN_POINT ( 'NONE',  ( 10.00000000000000000, 9.188173127307898369, -40.98264845739739570 ) ) ;
#19850=CARTESIAN_POINT ( 'NONE',  ( -3.000000000000000000, 9.615535125379096826, -24.73947219025905042 ) ) ;
#19864=ORIENTED_EDGE ( 'NONE', *, *, #26075, .T. ) ;
#19871=FACE_OUTER_BOUND ( 'NONE', #34899, .T. ) ;
#19883=ORIENTED_EDGE ( 'NONE', *, *, #20226, .T. ) ;
#19890=CIRCLE ( 'NONE', #47269, 16.00000000000000000 ) ;
#19900=ORIENTED_EDGE ( 'NONE', *, *, #42827, .F. ) ;
#19901=DIRECTION ( 'NONE',  ( 1.000000000000000000, -0.000000000000000000, 0.000000000000000000 ) ) ;
#19904=DIRECTION ( 'NONE',  ( -1.000000000000000000, -0.000000000000000000, -0.000000000000000000 ) ) ;
#19910=CARTESIAN_POINT ( 'NONE',  ( 0.000000000000000000, -27.75498641678764855, 31.52238457039590358 ) ) ;
#19913=EDGE_LOOP ( 'NONE', ( #20482, #18134, #38819, #45739 ) ) ;
#19921=CARTESIAN_POINT ( 'NONE',  ( 0.000000000000000000, 0.000000000000000000, 0.000000000000000000 ) ) ;
#19923=EDGE_CURVE ( 'NONE', #44741, #9216, #26707, .T. ) ;
#19926=EDGE_CURVE ( 'NONE', #30912, #9644, #35228, .T. ) ;
#19927=ORIENTED_EDGE ( 'NONE', *, *, #4707, .T. ) ;
#19928=VECTOR ( 'NONE', #13945, 1000.000000000000000 ) ;
#19938=DIRECTION ( 'NONE',  ( -1.000000000000000000, -0.000000000000000000, -0.000000000000000000 ) ) ;
#19951=CARTESIAN_POINT ( 'NONE',  ( -3.000000000000000000, 23.59884966291538078, -12.14883922797231541 ) ) ;
#19963=CYLINDRICAL_SURFACE ( 'NONE', #48064, 16.00000000000000000 ) ;
#19976=VECTOR ( 'NONE', #31843, 999.9999999999998863 ) ;
#19984=CIRCLE ( 'NONE', #24708, 37.49900000000000233 ) ;
#19999=AXIS2_PLACEMENT_3D ( 'NONE', #45086, #14987, #40453 ) ;
#20001=ADVANCED_FACE ( 'NONE', ( #262 ), #15221, .F. ) ;
#20005=ORIENTED_EDGE ( 'NONE', *, *, #38017, .T. ) ;
#20012=ORIENTED_EDGE ( 'NONE', *, *, #21197, .F. ) ;
#20013=VERTEX_POINT ( 'NONE', #40663 ) ;
#20017=LINE ( 'NONE', #46459, #1806 ) ;
#20029=ORIENTED_EDGE ( 'NONE', *, *, #45164, .T. ) ;
#20030=CARTESIAN_POINT ( 'NONE',  ( -3.000000000000000000, -23.29833615347109443, 3.418703333116492438 ) ) ;
#20033=VERTEX_POINT ( 'NONE', #44575 ) ;
#20040=CIRCLE ( 'NONE', #15377, 16.00000000000000000 ) ;
#20041=DIRECTION ( 'NONE',  ( 0.000000000000000000, 0.000000000000000000, 1.000000000000000000 ) ) ;
#20049=AXIS2_PLACEMENT_3D ( 'NONE', #7268, #14386, #21955 ) ;
#20054=CIRCLE ( 'NONE', #14627, 37.49900000000000944 ) ;
#20064=EDGE_CURVE ( 'NONE', #46270, #12261, #41495, .T. ) ;
#20077=EDGE_LOOP ( 'NONE', ( #7565, #5263, #47468, #247 ) ) ;
#20084=CARTESIAN_POINT ( 'NONE',  ( 0.000000000000000000, 20.85821328998756385, -10.92862929874494959 ) ) ;
#20086=ORIENTED_EDGE ( 'NONE', *, *, #8356, .F. ) ;
#20089=VERTEX_POINT ( 'NONE', #24233 ) ;
#20095=CARTESIAN_POINT ( 'NONE',  ( -3.000000000000000000, 5.835314593368772229, -22.81335362449846826 ) ) ;
#20101=CARTESIAN_POINT ( 'NONE',  ( -3.000000000000000000, 26.50000000000000355, 1.500000000000000000 ) ) ;
#20107=AXIS2_PLACEMENT_3D ( 'NONE', #40030, #36585, #28533 ) ;
#20109=AXIS2_PLACEMENT_3D ( 'NONE', #35362, #2545, #5513 ) ;
#20118=ADVANCED_FACE ( 'NONE', ( #38207 ), #31360, .T. ) ;
#20124=VECTOR ( 'NONE', #47964, 999.9999999999998863 ) ;
#20147=DIRECTION ( 'NONE',  ( 0.000000000000000000, 0.1564344650402313408, -0.9876883405951376593 ) ) ;
#20150=CARTESIAN_POINT ( 'NONE',  ( -3.000000000000000000, -1.278221433540145391, -26.51162292216073979 ) ) ;
#20165=ORIENTED_EDGE ( 'NONE', *, *, #29201, .F. ) ;
#20171=ORIENTED_EDGE ( 'NONE', *, *, #31180, .T. ) ;
#20191=DIRECTION ( 'NONE',  ( -1.000000000000000000, -0.000000000000000000, 0.000000000000000000 ) ) ;
#20208=PLANE ( 'NONE',  #2485 ) ;
#20212=ORIENTED_EDGE ( 'NONE', *, *, #12231, .T. ) ;
#20217=VECTOR ( 'NONE', #27796, 1000.000000000000000 ) ;
#20226=EDGE_CURVE ( 'NONE', #46270, #36913, #13941, .T. ) ;
#20236=VERTEX_POINT ( 'NONE', #32547 ) ;
#20241=VERTEX_POINT ( 'NONE', #31849 ) ;
#20244=ORIENTED_EDGE ( 'NONE', *, *, #23956, .T. ) ;
#20246=CARTESIAN_POINT ( 'NONE',  ( 10.00000000000000000, 41.91543099594818500, -2.663952781846293139 ) ) ;
#20254=CARTESIAN_POINT ( 'NONE',  ( 0.000000000000000000, 22.07842321921481243, 8.187992925817422218 ) ) ;
#20256=CARTESIAN_POINT ( 'NONE',  ( 10.00000000000000000, 9.188173127307297960, 40.98264845739753071 ) ) ;
#20260=ORIENTED_EDGE ( 'NONE', *, *, #27000, .F. ) ;
#20262=CYLINDRICAL_SURFACE ( 'NONE', #42269, 37.49900000000000233 ) ;
#20266=LINE ( 'NONE', #16853, #32716 ) ;
#20267=ORIENTED_EDGE ( 'NONE', *, *, #11878, .T. ) ;
#20268=EDGE_CURVE ( 'NONE', #1521, #23469, #10246, .T. ) ;
#20270=DIRECTION ( 'NONE',  ( -1.000000000000000000, 0.000000000000000000, 0.000000000000000000 ) ) ;
#20276=CARTESIAN_POINT ( 'NONE',  ( 10.00000000000000000, 0.000000000000000000, 0.000000000000000000 ) ) ;
#20280=ORIENTED_EDGE ( 'NONE', *, *, #4841, .T. ) ;
#20281=DIRECTION ( 'NONE',  ( -1.000000000000000000, -0.000000000000000000, 0.000000000000000000 ) ) ;
#20284=ORIENTED_EDGE ( 'NONE', *, *, #46634, .F. ) ;
#20299=LINE ( 'NONE', #27430, #40764 ) ;
#20307=DIRECTION ( 'NONE',  ( -1.000000000000000000, 0.000000000000000000, 0.000000000000000000 ) ) ;
#20309=ORIENTED_EDGE ( 'NONE', *, *, #38063, .T. ) ;
#20311=ORIENTED_EDGE ( 'NONE', *, *, #3177, .T. ) ;
#20315=EDGE_CURVE ( 'NONE', #33061, #38396, #47763, .T. ) ;
#20316=FACE_OUTER_BOUND ( 'NONE', #15104, .T. ) ;
#20317=CARTESIAN_POINT ( 'NONE',  ( 0.000000000000000000, 30.00120703465236716, -22.64427369931138756 ) ) ;
#20323=CARTESIAN_POINT ( 'NONE',  ( 10.00000000000000000, 16.65560815589464028, -38.55633173626993937 ) ) ;
#20328=CARTESIAN_POINT ( 'NONE',  ( 10.00000000000000000, -33.79645857604501913, -16.45098606841161626 ) ) ;
#20332=EDGE_LOOP ( 'NONE', ( #36211, #42143, #33986, #39927 ) ) ;
#20343=ORIENTED_EDGE ( 'NONE', *, *, #36836, .T. ) ;
#20347=AXIS2_PLACEMENT_3D ( 'NONE', #12270, #45799, #38440 ) ;
#20348=DIRECTION ( 'NONE',  ( 0.000000000000000000, 0.000000000000000000, 1.000000000000000000 ) ) ;
#20363=PLANE ( 'NONE',  #2476 ) ;
#20370=EDGE_LOOP ( 'NONE', ( #30596, #11361, #35690, #14216 ) ) ;
#20372=CARTESIAN_POINT ( 'NONE',  ( 0.000000000000000000, 30.80686688397041451, -21.53537804866048688 ) ) ;
#20376=CYLINDRICAL_SURFACE ( 'NONE', #13338, 16.00000000000000000 ) ;
#20379=LINE ( 'NONE', #20150, #2612 ) ;
#20382=DIRECTION ( 'NONE',  ( 0.000000000000000000, 0.000000000000000000, 1.000000000000000000 ) ) ;
#20383=VECTOR ( 'NONE', #15463, 1000.000000000000000 ) ;
#20384=DIRECTION ( 'NONE',  ( -1.000000000000000000, -0.000000000000000000, 0.000000000000000000 ) ) ;
#20386=EDGE_CURVE ( 'NONE', #7735, #2104, #45015, .T. ) ;
#20391=CYLINDRICAL_SURFACE ( 'NONE', #13493, 37.49900000000000233 ) ;
#20394=ORIENTED_EDGE ( 'NONE', *, *, #11672, .F. ) ;
#20401=VECTOR ( 'NONE', #25297, 1000.000000000000000 ) ;
#20405=DIRECTION ( 'NONE',  ( 0.000000000000000000, 0.000000000000000000, 1.000000000000000000 ) ) ;
#20408=ADVANCED_FACE ( 'NONE', ( #14673 ), #29589, .T. ) ;
#20411=CIRCLE ( 'NONE', #46219, 16.00000000000000000 ) ;
#20416=ORIENTED_EDGE ( 'NONE', *, *, #33757, .F. ) ;
#20430=DIRECTION ( 'NONE',  ( 0.000000000000000000, -0.3090169943749349057, -0.9510565162951577500 ) ) ;
#20432=CARTESIAN_POINT ( 'NONE',  ( 10.00000000000000000, -37.58145647212453611, -0.6853352020794456489 ) ) ;
#20436=CARTESIAN_POINT ( 'NONE',  ( -3.000000000000000000, 0.000000000000000000, 0.000000000000000000 ) ) ;
#20439=DIRECTION ( 'NONE',  ( 0.000000000000000000, 0.000000000000000000, 1.000000000000000000 ) ) ;
#20440=AXIS2_PLACEMENT_3D ( 'NONE', #24135, #39066, #5529 ) ;
#20441=DIRECTION ( 'NONE',  ( 0.000000000000000000, 0.000000000000000000, -1.000000000000000000 ) ) ;
#20459=CARTESIAN_POINT ( 'NONE',  ( 0.000000000000000000, -35.47612816024539484, 22.48208911017487921 ) ) ;
#20466=ORIENTED_EDGE ( 'NONE', *, *, #16272, .T. ) ;
#20478=ORIENTED_EDGE ( 'NONE', *, *, #25070, .T. ) ;
#20482=ORIENTED_EDGE ( 'NONE', *, *, #14549, .F. ) ;
#20483=CYLINDRICAL_SURFACE ( 'NONE', #112, 16.00000000000000000 ) ;
#20491=CIRCLE ( 'NONE', #21250, 42.00000000000000000 ) ;
#20502=ORIENTED_EDGE ( 'NONE', *, *, #2575, .F. ) ;
#20506=CARTESIAN_POINT ( 'NONE',  ( 0.000000000000000000, -10.41901085202107247, 40.68715046381925049 ) ) ;
#20515=CIRCLE ( 'NONE', #5673, 16.00000000000000355 ) ;
#20528=CARTESIAN_POINT ( 'NONE',  ( 0.000000000000000000, 35.95386929396256903, -10.96151621346501237 ) ) ;
#20535=ORIENTED_EDGE ( 'NONE', *, *, #23791, .F. ) ;
#20536=EDGE_CURVE ( 'NONE', #34175, #1618, #37912, .T. ) ;
#20544=FACE_OUTER_BOUND ( 'NONE', #31800, .T. ) ;
#20551=ORIENTED_EDGE ( 'NONE', *, *, #34429, .F. ) ;
#20554=CIRCLE ( 'NONE', #8049, 42.00000000000000000 ) ;
#20556=ORIENTED_EDGE ( 'NONE', *, *, #44991, .F. ) ;
#20559=CARTESIAN_POINT ( 'NONE',  ( -10.00000000000000000, 0.000000000000000000, 0.000000000000000000 ) ) ;
#20561=CIRCLE ( 'NONE', #8819, 42.00000000000000000 ) ;
#20568=CARTESIAN_POINT ( 'NONE',  ( -3.000000000000000000, -25.60904388321925396, 6.976881207771172377 ) ) ;
#20571=DIRECTION ( 'NONE',  ( 0.000000000000000000, -0.5000000000000046629, 0.8660254037844359321 ) ) ;
#20581=ORIENTED_EDGE ( 'NONE', *, *, #24257, .F. ) ;
#20582=CARTESIAN_POINT ( 'NONE',  ( 10.00000000000000000, 0.000000000000000000, 0.000000000000000000 ) ) ;
#20584=AXIS2_PLACEMENT_3D ( 'NONE', #10080, #32593, #24999 ) ;
#20586=VECTOR ( 'NONE', #2567, 1000.000000000000000 ) ;
#20593=CARTESIAN_POINT ( 'NONE',  ( 0.000000000000000000, 15.48615015657581750, 39.04073710021349797 ) ) ;
#20596=DIRECTION ( 'NONE',  ( -1.000000000000000000, 0.000000000000000000, 0.000000000000000000 ) ) ;
#20602=CARTESIAN_POINT ( 'NONE',  ( -10.00000000000000000, 0.000000000000000000, 0.000000000000000000 ) ) ;
#20604=DIRECTION ( 'NONE',  ( -1.000000000000000000, 0.000000000000000000, -0.000000000000000000 ) ) ;
#20605=EDGE_LOOP ( 'NONE', ( #2959, #39169, #33193, #4443 ) ) ;
#20608=ADVANCED_FACE ( 'NONE', ( #35689 ), #5839, .T. ) ;
#20615=ORIENTED_EDGE ( 'NONE', *, *, #6821, .T. ) ;
#20631=DIRECTION ( 'NONE',  ( 0.000000000000000000, 0.000000000000000000, 1.000000000000000000 ) ) ;
#20634=CARTESIAN_POINT ( 'NONE',  ( 10.00000000000000000, 0.000000000000000000, 0.000000000000000000 ) ) ;
#20635=VECTOR ( 'NONE', #42045, 1000.000000000000000 ) ;
#20644=AXIS2_PLACEMENT_3D ( 'NONE', #3192, #29404, #44327 ) ;
#20645=VERTEX_POINT ( 'NONE', #46713 ) ;
#20657=ORIENTED_EDGE ( 'NONE', *, *, #48208, .F. ) ;
#20658=ADVANCED_FACE ( 'NONE', ( #13171 ), #36402, .F. ) ;
#20659=EDGE_LOOP ( 'NONE', ( #36103, #26147, #28629, #3013 ) ) ;
#20660=EDGE_CURVE ( 'NONE', #19709, #42524, #8709, .T. ) ;
#20662=VECTOR ( 'NONE', #850, 1000.000000000000000 ) ;
#20671=DIRECTION ( 'NONE',  ( 0.000000000000000000, -0.6691306063588672304, 0.7431448254773862505 ) ) ;
#20672=ORIENTED_EDGE ( 'NONE', *, *, #46487, .T. ) ;
#20685=CARTESIAN_POINT ( 'NONE',  ( -3.000000000000000000, -18.13022148937263012, 15.02647892043544608 ) ) ;
#20691=CYLINDRICAL_SURFACE ( 'NONE', #27758, 16.00000000000000000 ) ;
#20698=DIRECTION ( 'NONE',  ( 0.000000000000000000, 0.2079116908177525702, 0.9781476007338071321 ) ) ;
#20703=CARTESIAN_POINT ( 'NONE',  ( -3.000000000000000000, -25.60904388321916159, -6.976881207771517879 ) ) ;
#20714=ORIENTED_EDGE ( 'NONE', *, *, #10364, .F. ) ;
#20716=CIRCLE ( 'NONE', #41825, 37.49900000000000944 ) ;
#20717=EDGE_LOOP ( 'NONE', ( #41397, #37026, #32582, #39339 ) ) ;
#20732=AXIS2_PLACEMENT_3D ( 'NONE', #32658, #32894, #18688 ) ;
#20735=ORIENTED_EDGE ( 'NONE', *, *, #18718, .T. ) ;
#20738=CARTESIAN_POINT ( 'NONE',  ( 10.00000000000000000, 35.95386929396256903, -10.96151621346501237 ) ) ;
#20739=FACE_OUTER_BOUND ( 'NONE', #39088, .T. ) ;
#20741=DIRECTION ( 'NONE',  ( 0.000000000000000000, 0.000000000000000000, 1.000000000000000000 ) ) ;
#20745=ORIENTED_EDGE ( 'NONE', *, *, #24369, .T. ) ;
#20747=ORIENTED_EDGE ( 'NONE', *, *, #34810, .T. ) ;
#20757=CARTESIAN_POINT ( 'NONE',  ( 0.000000000000000000, -41.91543099594819921, 2.663952781846001816 ) ) ;
#20780=VECTOR ( 'NONE', #28373, 1000.000000000000000 ) ;
#20781=ADVANCED_FACE ( 'NONE', ( #14858 ), #33455, .T. ) ;
#20783=DIRECTION ( 'NONE',  ( 0.000000000000000000, 0.000000000000000000, 1.000000000000000000 ) ) ;
#20785=DIRECTION ( 'NONE',  ( 0.000000000000000000, 0.1564344650402311743, -0.9876883405951377704 ) ) ;
#20791=ORIENTED_EDGE ( 'NONE', *, *, #32925, .T. ) ;
#20810=VECTOR ( 'NONE', #45728, 1000.000000000000000 ) ;
#20824=AXIS2_PLACEMENT_3D ( 'NONE', #7927, #19193, #822 ) ;
#20825=FACE_OUTER_BOUND ( 'NONE', #38609, .T. ) ;
#20838=VECTOR ( 'NONE', #34720, 1000.000000000000000 ) ;
#20841=CARTESIAN_POINT ( 'NONE',  ( -3.000000000000000000, 20.85821328998756385, -10.92862929874494959 ) ) ;
#20853=VERTEX_POINT ( 'NONE', #44236 ) ;
#20854=CARTESIAN_POINT ( 'NONE',  ( -3.000000000000000000, 16.61724383029361718, 20.69703378468926402 ) ) ;
#20858=CIRCLE ( 'NONE', #25525, 15.99999999999999822 ) ;
#20866=FACE_OUTER_BOUND ( 'NONE', #12025, .T. ) ;
#20884=PLANE ( 'NONE',  #18053 ) ;
#20897=CARTESIAN_POINT ( 'NONE',  ( 0.000000000000000000, -36.13751322684434797, 21.40280677340357940 ) ) ;
#20900=CARTESIAN_POINT ( 'NONE',  ( 10.00000000000000000, 0.000000000000000000, 0.000000000000000000 ) ) ;
#20905=VERTEX_POINT ( 'NONE', #4336 ) ;
#20908=AXIS2_PLACEMENT_3D ( 'NONE', #14080, #43939, #48097 ) ;
#20919=AXIS2_PLACEMENT_3D ( 'NONE', #3849, #18758, #43997 ) ;
#20926=DIRECTION ( 'NONE',  ( -1.000000000000000000, -0.000000000000000000, 0.000000000000000000 ) ) ;
#20927=VERTEX_POINT ( 'NONE', #38333 ) ;
#20934=DIRECTION ( 'NONE',  ( -1.000000000000000000, -0.000000000000000000, 0.000000000000000000 ) ) ;
#20938=CARTESIAN_POINT ( 'NONE',  ( 0.000000000000000000, 22.48208911017500355, 35.47612816024530957 ) ) ;
#20946=LINE ( 'NONE', #28771, #20586 ) ;
#20952=ORIENTED_EDGE ( 'NONE', *, *, #8275, .F. ) ;
#20961=ADVANCED_FACE ( 'NONE', ( #45200 ), #20208, .F. ) ;
#20964=ORIENTED_EDGE ( 'NONE', *, *, #21197, .T. ) ;
#20973=LINE ( 'NONE', #42779, #3172 ) ;
#20976=ORIENTED_EDGE ( 'NONE', *, *, #44541, .T. ) ;
#20980=DIRECTION ( 'NONE',  ( 0.000000000000000000, 0.9510565162951543083, -0.3090169943749448977 ) ) ;
#20990=ADVANCED_FACE ( 'NONE', ( #38583 ), #5048, .T. ) ;
#20996=DIRECTION ( 'NONE',  ( 0.000000000000000000, 0.000000000000000000, 1.000000000000000000 ) ) ;
#20998=DIRECTION ( 'NONE',  ( -1.000000000000000000, -0.000000000000000000, -0.000000000000000000 ) ) ;
#21011=AXIS2_PLACEMENT_3D ( 'NONE', #9043, #35216, #9508 ) ;
#21017=DIRECTION ( 'NONE',  ( -1.000000000000000000, 0.000000000000000000, 0.000000000000000000 ) ) ;
#21031=CARTESIAN_POINT ( 'NONE',  ( 10.00000000000000000, -4.992566952384716927, -37.16516213103282951 ) ) ;
#21055=ADVANCED_BREP_SHAPE_REPRESENTATION ( '', ( #2931, #11636 ), #21829 ) ;
#21056=EDGE_CURVE ( 'NONE', #34673, #17574, #39257, .T. ) ;
#21057=LINE ( 'NONE', #28657, #25250 ) ;
#21062=ORIENTED_EDGE ( 'NONE', *, *, #5306, .T. ) ;
#21066=EDGE_LOOP ( 'NONE', ( #15328, #40422, #8255, #34806 ) ) ;
#21067=AXIS2_PLACEMENT_3D ( 'NONE', #13471, #2216, #42369 ) ;
#21071=DIRECTION ( 'NONE',  ( 0.000000000000000000, 0.5877852522924797984, -0.8090169943749426773 ) ) ;
#21082=VERTEX_POINT ( 'NONE', #31740 ) ;
#21085=PLANE ( 'NONE',  #31626 ) ;
#21099=EDGE_CURVE ( 'NONE', #12494, #26652, #39294, .T. ) ;
#21104=DIRECTION ( 'NONE',  ( 0.000000000000000000, 0.000000000000000000, 1.000000000000000000 ) ) ;
#21114=EDGE_CURVE ( 'NONE', #18029, #40235, #15814, .T. ) ;
#21126=ORIENTED_EDGE ( 'NONE', *, *, #33546, .F. ) ;
#21133=VERTEX_POINT ( 'NONE', #39557 ) ;
#21138=CIRCLE ( 'NONE', #37538, 16.00000000000000000 ) ;
#21140=EDGE_LOOP ( 'NONE', ( #29756, #16766, #37454, #7247 ) ) ;
#21157=DIRECTION ( 'NONE',  ( -0.000000000000000000, -0.5877852522924789103, 0.8090169943749432324 ) ) ;
#21163=EDGE_CURVE ( 'NONE', #2768, #894, #9547, .T. ) ;
#21169=DIRECTION ( 'NONE',  ( -1.000000000000000000, -0.000000000000000000, 0.000000000000000000 ) ) ;
#21170=CYLINDRICAL_SURFACE ( 'NONE', #35330, 37.49900000000000233 ) ;
#21172=CARTESIAN_POINT ( 'NONE',  ( 10.00000000000000000, -29.81001611431024756, 22.74946021919122785 ) ) ;
#21173=ADVANCED_FACE ( 'NONE', ( #11382 ), #29718, .F. ) ;
#21174=CIRCLE ( 'NONE', #11791, 42.00000000000000000 ) ;
#21176=CARTESIAN_POINT ( 'NONE',  ( 0.000000000000000000, 0.000000000000000000, 0.000000000000000000 ) ) ;
#21184=ORIENTED_EDGE ( 'NONE', *, *, #48330, .T. ) ;
#21197=EDGE_CURVE ( 'NONE', #6467, #20013, #25315, .T. ) ;
#21200=VERTEX_POINT ( 'NONE', #3775 ) ;
#21217=DIRECTION ( 'NONE',  ( -1.000000000000000000, 0.000000000000000000, 0.000000000000000000 ) ) ;
#21218=DIRECTION ( 'NONE',  ( -1.000000000000000000, 0.000000000000000000, 0.000000000000000000 ) ) ;
#21220=ADVANCED_FACE ( 'NONE', ( #48321 ), #3279, .T. ) ;
#21222=LINE ( 'NONE', #25381, #3790 ) ;
#21237=PRESENTATION_STYLE_ASSIGNMENT (( #47661 ) ) ;
#21250=AXIS2_PLACEMENT_3D ( 'NONE', #28853, #13931, #32759 ) ;
#21269=VECTOR ( 'NONE', #42495, 1000.000000000000000 ) ;
#21270=CARTESIAN_POINT ( 'NONE',  ( 0.000000000000000000, -14.54903810567676636, 22.19967320028756319 ) ) ;
#21290=CARTESIAN_POINT ( 'NONE',  ( 5.000000000000000000, 16.65560815589464028, -38.55633173626993226 ) ) ;
#21299=DIRECTION ( 'NONE',  ( 0.000000000000000000, 0.4067366430757888285, 0.9135454576426060846 ) ) ;
#21307=VECTOR ( 'NONE', #14735, 1000.000000000000000 ) ;
#21308=ADVANCED_FACE ( 'NONE', ( #12107 ), #22856, .T. ) ;
#21319=AXIS2_PLACEMENT_3D ( 'NONE', #43403, #27996, #1557 ) ;
#21323=DIRECTION ( 'NONE',  ( -1.000000000000000000, 0.000000000000000000, 0.000000000000000000 ) ) ;
#21327=ORIENTED_EDGE ( 'NONE', *, *, #33255, .T. ) ;
#21332=ORIENTED_EDGE ( 'NONE', *, *, #14592, .F. ) ;
#21339=CARTESIAN_POINT ( 'NONE',  ( 0.000000000000000000, 0.000000000000000000, 21.00000000000000000 ) ) ;
#21341=DIRECTION ( 'NONE',  ( -1.000000000000000000, 0.000000000000000000, -0.000000000000000000 ) ) ;
#21346=CIRCLE ( 'NONE', #16674, 42.00000000000000000 ) ;
#21357=CIRCLE ( 'NONE', #19010, 37.49900000000000233 ) ;
#21362=CARTESIAN_POINT ( 'NONE',  ( 0.000000000000000000, 37.22597642581150268, 5.202137450157037435 ) ) ;
#21367=FACE_OUTER_BOUND ( 'NONE', #37270, .T. ) ;
#21375=AXIS2_PLACEMENT_3D ( 'NONE', #12469, #42319, #19311 ) ;
#21378=ORIENTED_EDGE ( 'NONE', *, *, #11064, .T. ) ;
#21390=CARTESIAN_POINT ( 'NONE',  ( -3.000000000000000000, 0.000000000000000000, 0.000000000000000000 ) ) ;
#21400=AXIS2_PLACEMENT_3D ( 'NONE', #34011, #15429, #30361 ) ;
#21409=CARTESIAN_POINT ( 'NONE',  ( -3.000000000000000000, -14.54903810567645195, -22.19967320028775504 ) ) ;
#21410=DIRECTION ( 'NONE',  ( -1.000000000000000000, -0.000000000000000000, -0.000000000000000000 ) ) ;
#21414=CARTESIAN_POINT ( 'NONE',  ( 0.000000000000000000, -25.60904388321925396, 6.976881207771172377 ) ) ;
#21433=AXIS2_PLACEMENT_3D ( 'NONE', #16610, #31562, #12959 ) ;
#21440=CIRCLE ( 'NONE', #16770, 16.00000000000000000 ) ;
#21441=EDGE_CURVE ( 'NONE', #8888, #1459, #39290, .T. ) ;
#21444=CARTESIAN_POINT ( 'NONE',  ( -3.000000000000000000, 5.835314593368477354, 22.81335362449854642 ) ) ;
#21448=DIRECTION ( 'NONE',  ( -1.000000000000000000, -0.000000000000000000, -0.000000000000000000 ) ) ;
#21450=AXIS2_PLACEMENT_3D ( 'NONE', #41415, #22806, #44837 ) ;
#21454=ADVANCED_FACE ( 'NONE', ( #47066 ), #31924, .T. ) ;
#21456=ORIENTED_EDGE ( 'NONE', *, *, #35320, .F. ) ;
#21457=AXIS2_PLACEMENT_3D ( 'NONE', #7805, #14916, #15881 ) ;
#21459=ORIENTED_EDGE ( 'NONE', *, *, #12315, .F. ) ;
#21461=DIRECTION ( 'NONE',  ( 1.000000000000000000, 0.000000000000000000, -0.000000000000000000 ) ) ;
#21469=CARTESIAN_POINT ( 'NONE',  ( 0.000000000000000000, -41.91543099594816368, -2.663952781846588014 ) ) ;
#21474=ORIENTED_EDGE ( 'NONE', *, *, #37861, .F. ) ;
#21483=AXIS2_PLACEMENT_3D ( 'NONE', #26585, #7966, #19236 ) ;
#21484=EDGE_CURVE ( 'NONE', #25099, #34175, #47953, .T. ) ;
#21485=FACE_OUTER_BOUND ( 'NONE', #29192, .T. ) ;
#21489=CARTESIAN_POINT ( 'NONE',  ( 4.999999999999999112, 2.663952781846732343, -41.91543099594814947 ) ) ;
#21494=SHAPE_REPRESENTATION_RELATIONSHIP ( 'NONE' , 'NONE' ,  #12525, #21055 ) ;
#21512=AXIS2_PLACEMENT_3D ( 'NONE', #45430, #14185, #14678 ) ;
#21518=CIRCLE ( 'NONE', #420, 16.00000000000000000 ) ;
#21523=DIRECTION ( 'NONE',  ( -1.000000000000000000, -0.000000000000000000, -0.000000000000000000 ) ) ;
#21527=ORIENTED_EDGE ( 'NONE', *, *, #40914, .F. ) ;
#21531=ORIENTED_EDGE ( 'NONE', *, *, #6612, .T. ) ;
#21535=EDGE_LOOP ( 'NONE', ( #20976, #37410, #8484, #43497 ) ) ;
#21537=DIRECTION ( 'NONE',  ( 0.000000000000000000, 0.000000000000000000, 1.000000000000000000 ) ) ;
#21546=FACE_OUTER_BOUND ( 'NONE', #13139, .T. ) ;
#21547=EDGE_CURVE ( 'NONE', #27887, #42524, #24308, .T. ) ;
#21550=FACE_OUTER_BOUND ( 'NONE', #34320, .T. ) ;
#21553=VECTOR ( 'NONE', #12332, 999.9999999999998863 ) ;
#21559=CARTESIAN_POINT ( 'NONE',  ( 0.000000000000000000, -37.58145647212453611, -0.6853352020794456489 ) ) ;
#21560=AXIS2_PLACEMENT_3D ( 'NONE', #12378, #20191, #35355 ) ;
#21562=DIRECTION ( 'NONE',  ( -0.000000000000000000, 0.9510565162951539753, -0.3090169943749460635 ) ) ;
#21568=CARTESIAN_POINT ( 'NONE',  ( 10.00000000000000000, 0.000000000000000000, 0.000000000000000000 ) ) ;
#21573=DIRECTION ( 'NONE',  ( 0.000000000000000000, 0.000000000000000000, 1.000000000000000000 ) ) ;
#21574=DIRECTION ( 'NONE',  ( -1.000000000000000000, -0.000000000000000000, -0.000000000000000000 ) ) ;
#21601=CARTESIAN_POINT ( 'NONE',  ( 10.00000000000000000, -27.05870788708213226, -26.08949754953053102 ) ) ;
#21603=DIRECTION ( 'NONE',  ( 0.000000000000000000, 0.000000000000000000, -1.000000000000000000 ) ) ;
#21613=EDGE_CURVE ( 'NONE', #8546, #44380, #33744, .T. ) ;
#21615=LINE ( 'NONE', #43415, #16607 ) ;
#21624=ADVANCED_FACE ( 'NONE', ( #10767 ), #15171, .F. ) ;
#21630=AXIS2_PLACEMENT_3D ( 'NONE', #26905, #38158, #8296 ) ;
#21631=LINE ( 'NONE', #7658, #38564 ) ;
#21643=CARTESIAN_POINT ( 'NONE',  ( 0.000000000000000000, -22.64427369931191336, 30.00120703465197280 ) ) ;
#21654=ORIENTED_EDGE ( 'NONE', *, *, #30904, .F. ) ;
#21670=CARTESIAN_POINT ( 'NONE',  ( 0.000000000000000000, 0.000000000000000000, 0.000000000000000000 ) ) ;
#21681=LINE ( 'NONE', #13619, #45292 ) ;
#21689=EDGE_LOOP ( 'NONE', ( #46912, #38966, #42775, #40657 ) ) ;
#21690=CARTESIAN_POINT ( 'NONE',  ( 0.000000000000000000, 0.000000000000000000, 0.000000000000000000 ) ) ;
#21694=DIRECTION ( 'NONE',  ( 0.000000000000000000, 0.000000000000000000, 1.000000000000000000 ) ) ;
#21696=VECTOR ( 'NONE', #26917, 1000.000000000000000 ) ;
#21697=CARTESIAN_POINT ( 'NONE',  ( 0.000000000000000000, -33.17418723428294669, -17.67226234102862747 ) ) ;
#21702=ORIENTED_EDGE ( 'NONE', *, *, #7428, .F. ) ;
#21713=VECTOR ( 'NONE', #40199, 1000.000000000000000 ) ;
#21717=AXIS2_PLACEMENT_3D ( 'NONE', #26255, #33582, #11078 ) ;
#21724=ADVANCED_FACE ( 'NONE', ( #5121 ), #5357, .T. ) ;
#21728=LINE ( 'NONE', #10721, #44880 ) ;
#21731=PLANE ( 'NONE',  #40167 ) ;
#21733=VERTEX_POINT ( 'NONE', #38898 ) ;
#21736=DIRECTION ( 'NONE',  ( 0.000000000000000000, 0.000000000000000000, 1.000000000000000000 ) ) ;
#21748=CARTESIAN_POINT ( 'NONE',  ( 10.00000000000000000, -37.16516213103280108, 4.992566952384862589 ) ) ;
#21765=DIRECTION ( 'NONE',  ( 1.000000000000000000, -0.000000000000000000, -0.000000000000000000 ) ) ;
#21768=CARTESIAN_POINT ( 'NONE',  ( -3.000000000000000000, 16.61724383029390140, -20.69703378468903665 ) ) ;
#21777=AXIS2_PLACEMENT_3D ( 'NONE', #33458, #7263, #13896 ) ;
#21778=CARTESIAN_POINT ( 'NONE',  ( 10.00000000000000000, 0.6853352020790449695, 37.58145647212454321 ) ) ;
#21782=ORIENTED_EDGE ( 'NONE', *, *, #33765, .T. ) ;
#21792=EDGE_LOOP ( 'NONE', ( #46908, #8276, #42014, #40115 ) ) ;
#21793=LINE ( 'NONE', #48231, #35450 ) ;
#21795=VERTEX_POINT ( 'NONE', #42078 ) ;
#21805=DIRECTION ( 'NONE',  ( -1.000000000000000000, -0.000000000000000000, 0.000000000000000000 ) ) ;
#21815=ORIENTED_EDGE ( 'NONE', *, *, #5306, .F. ) ;
#21818=ORIENTED_EDGE ( 'NONE', *, *, #46257, .T. ) ;
#21820=DIRECTION ( 'NONE',  ( 0.000000000000000000, 0.9510565162951544194, -0.3090169943749447867 ) ) ;
#21824=PLANE ( 'NONE',  #14937 ) ;
#21829=( GEOMETRIC_REPRESENTATION_CONTEXT ( 3 ) GLOBAL_UNCERTAINTY_ASSIGNED_CONTEXT ( ( #19318 ) ) GLOBAL_UNIT_ASSIGNED_CONTEXT ( ( #29558, #9988, #3112 ) ) REPRESENTATION_CONTEXT ( 'NONE', 'WORKASPACE' ) );
#21834=CARTESIAN_POINT ( 'NONE',  ( 0.000000000000000000, 0.000000000000000000, 0.000000000000000000 ) ) ;
#21836=DIRECTION ( 'NONE',  ( -0.000000000000000000, 0.8660254037844368202, 0.5000000000000031086 ) ) ;
#21842=ORIENTED_EDGE ( 'NONE', *, *, #36070, .T. ) ;
#21847=CARTESIAN_POINT ( 'NONE',  ( 10.00000000000000000, -36.88895765772628010, -6.736453364083947015 ) ) ;
#21849=DIRECTION ( 'NONE',  ( 0.000000000000000000, 0.9510565162951539753, -0.3090169943749460635 ) ) ;
#21850=ORIENTED_EDGE ( 'NONE', *, *, #33255, .F. ) ;
#21861=ADVANCED_FACE ( 'NONE', ( #43752 ), #10466, .T. ) ;
#21866=CARTESIAN_POINT ( 'NONE',  ( 10.00000000000000000, -30.80686688396994910, -21.53537804866113703 ) ) ;
#21878=CARTESIAN_POINT ( 'NONE',  ( -3.000000000000000000, -3.948201729842038432, -23.21447184625298021 ) ) ;
#21880=CARTESIAN_POINT ( 'NONE',  ( 0.000000000000000000, 0.000000000000000000, 0.000000000000000000 ) ) ;
#21883=ORIENTED_EDGE ( 'NONE', *, *, #21114, .F. ) ;
#21884=DIRECTION ( 'NONE',  ( 1.000000000000000000, -0.000000000000000000, 0.000000000000000000 ) ) ;
#21885=DIRECTION ( 'NONE',  ( -1.000000000000000000, 0.000000000000000000, 0.000000000000000000 ) ) ;
#21888=CARTESIAN_POINT ( 'NONE',  ( -3.000000000000000000, -0.9646360437375307573, 23.52805723605590060 ) ) ;
#21891=CARTESIAN_POINT ( 'NONE',  ( 10.00000000000000000, 0.000000000000000000, 0.000000000000000000 ) ) ;
#21892=DIRECTION ( 'NONE',  ( -1.000000000000000000, 0.000000000000000000, 0.000000000000000000 ) ) ;
#21897=CARTESIAN_POINT ( 'NONE',  ( 0.000000000000000000, 31.52238457039637609, -27.75498641678709788 ) ) ;
#21899=LINE ( 'NONE', #37328, #10541 ) ;
#21905=EDGE_CURVE ( 'NONE', #39461, #5144, #33831, .T. ) ;
#21920=CYLINDRICAL_SURFACE ( 'NONE', #31303, 42.00000000000000000 ) ;
#21926=CARTESIAN_POINT ( 'NONE',  ( 10.00000000000000000, 0.000000000000000000, 0.000000000000000000 ) ) ;
#21930=ORIENTED_EDGE ( 'NONE', *, *, #45885, .F. ) ;
#21933=FACE_OUTER_BOUND ( 'NONE', #14731, .T. ) ;
#21955=DIRECTION ( 'NONE',  ( 0.000000000000000000, 0.000000000000000000, 1.000000000000000000 ) ) ;
#21958=DIRECTION ( 'NONE',  ( -1.000000000000000000, -0.000000000000000000, 0.000000000000000000 ) ) ;
#21963=ORIENTED_EDGE ( 'NONE', *, *, #8245, .T. ) ;
#21968=ORIENTED_EDGE ( 'NONE', *, *, #22761, .F. ) ;
#21971=CIRCLE ( 'NONE', #14969, 15.99999999999999645 ) ;
#21976=VERTEX_POINT ( 'NONE', #10218 ) ;
#21977=EDGE_CURVE ( 'NONE', #33061, #41296, #22893, .T. ) ;
#21981=CARTESIAN_POINT ( 'NONE',  ( 0.000000000000000000, -2.663952781846440576, 41.91543099594817789 ) ) ;
#21996=LINE ( 'NONE', #36920, #27576 ) ;
#22031=ORIENTED_EDGE ( 'NONE', *, *, #47329, .T. ) ;
#22049=ORIENTED_EDGE ( 'NONE', *, *, #30080, .T. ) ;
#22050=EDGE_CURVE ( 'NONE', #12709, #30788, #26367, .T. ) ;
#22062=FACE_OUTER_BOUND ( 'NONE', #7262, .T. ) ;
#22065=CIRCLE ( 'NONE', #45507, 16.00000000000000000 ) ;
#22066=CARTESIAN_POINT ( 'NONE',  ( 0.000000000000000000, -37.16516213103280108, 4.992566952384862589 ) ) ;
#22069=EDGE_LOOP ( 'NONE', ( #39990, #48425, #29774, #30488 ) ) ;
#22078=CARTESIAN_POINT ( 'NONE',  ( 10.00000000000000000, 37.16516213103277977, 4.992566952385115719 ) ) ;
#22082=ORIENTED_EDGE ( 'NONE', *, *, #13036, .F. ) ;
#22090=VERTEX_POINT ( 'NONE', #37132 ) ;
#22091=CIRCLE ( 'NONE', #8042, 16.00000000000000000 ) ;
#22093=EDGE_CURVE ( 'NONE', #7802, #17130, #31557, .T. ) ;
#22103=CARTESIAN_POINT ( 'NONE',  ( 10.00000000000000000, -41.81611651403864727, 3.925862922256025289 ) ) ;
#22118=EDGE_LOOP ( 'NONE', ( #42477, #30553, #17168, #30578 ) ) ;
#22122=CYLINDRICAL_SURFACE ( 'NONE', #8270, 16.00000000000000000 ) ;
#22132=DIRECTION ( 'NONE',  ( -1.000000000000000000, -0.000000000000000000, 0.000000000000000000 ) ) ;
#22144=LINE ( 'NONE', #2821, #33129 ) ;
#22159=CARTESIAN_POINT ( 'NONE',  ( 10.00000000000000000, 27.05870788708267582, -26.08949754952995903 ) ) ;
#22164=AXIS2_PLACEMENT_3D ( 'NONE', #45621, #38785, #11857 ) ;
#22169=CIRCLE ( 'NONE', #39409, 16.00000000000000000 ) ;
#22179=EDGE_CURVE ( 'NONE', #19681, #42002, #12177, .T. ) ;
#22202=AXIS2_PLACEMENT_3D ( 'NONE', #29048, #29536, #25611 ) ;
#22206=CARTESIAN_POINT ( 'NONE',  ( 0.000000000000000000, -30.00120703465189465, -22.64427369931201639 ) ) ;
#22217=EDGE_CURVE ( 'NONE', #18104, #43027, #22934, .T. ) ;
#22236=VECTOR ( 'NONE', #41662, 1000.000000000000000 ) ;
#22243=AXIS2_PLACEMENT_3D ( 'NONE', #1509, #35515, #46294 ) ;
#22244=ORIENTED_EDGE ( 'NONE', *, *, #43381, .F. ) ;
#22248=FACE_OUTER_BOUND ( 'NONE', #27650, .T. ) ;
#22250=DIRECTION ( 'NONE',  ( 0.000000000000000000, 0.000000000000000000, 1.000000000000000000 ) ) ;
#22253=VERTEX_POINT ( 'NONE', #45439 ) ;
#22281=AXIS2_PLACEMENT_3D ( 'NONE', #484, #23238, #19535 ) ;
#22285=EDGE_CURVE ( 'NONE', #9186, #36861, #20946, .T. ) ;
#22293=CYLINDRICAL_SURFACE ( 'NONE', #12820, 42.00000000000000000 ) ;
#22295=EDGE_CURVE ( 'NONE', #12545, #48002, #30772, .T. ) ;
#22306=DIRECTION ( 'NONE',  ( 0.000000000000000000, 0.000000000000000000, -1.000000000000000000 ) ) ;
#22318=ORIENTED_EDGE ( 'NONE', *, *, #41297, .T. ) ;
#22321=VERTEX_POINT ( 'NONE', #35382 ) ;
#22325=EDGE_CURVE ( 'NONE', #14880, #40287, #39304, .T. ) ;
#22327=VECTOR ( 'NONE', #7458, 1000.000000000000000 ) ;
#22346=EDGE_CURVE ( 'NONE', #46699, #42002, #8855, .T. ) ;
#22354=PRODUCT_DEFINITION ( 'UNKNOWN', '', #35818, #3673 ) ;
#22355=VECTOR ( 'NONE', #23264, 1000.000000000000000 ) ;
#22362=DIRECTION ( 'NONE',  ( -1.000000000000000000, -0.000000000000000000, -0.000000000000000000 ) ) ;
#22365=CARTESIAN_POINT ( 'NONE',  ( 10.00000000000000000, -0.8828120875903202602, 37.48860685352291000 ) ) ;
#22372=PLANE ( 'NONE',  #16382 ) ;
#22376=ORIENTED_EDGE ( 'NONE', *, *, #23415, .T. ) ;
#22385=EDGE_CURVE ( 'NONE', #13149, #9644, #27633, .T. ) ;
#22404=CARTESIAN_POINT ( 'NONE',  ( 5.000000000000000000, -32.34446384429951138, -26.79245525562750530 ) ) ;
#22410=CIRCLE ( 'NONE', #27102, 16.00000000000000000 ) ;
#22425=ORIENTED_EDGE ( 'NONE', *, *, #10501, .T. ) ;
#22436=EDGE_CURVE ( 'NONE', #37649, #44937, #44660, .T. ) ;
#22437=DIRECTION ( 'NONE',  ( -1.000000000000000000, -0.000000000000000000, -0.000000000000000000 ) ) ;
#22440=CARTESIAN_POINT ( 'NONE',  ( 10.00000000000000000, 0.000000000000000000, 0.000000000000000000 ) ) ;
#22444=LINE ( 'NONE', #42239, #24444 ) ;
#22455=DIRECTION ( 'NONE',  ( 0.000000000000000000, -0.5877852522924624790, -0.8090169943749553338 ) ) ;
#22463=CARTESIAN_POINT ( 'NONE',  ( 4.999999999999999112, 10.41901085202078292, 40.68715046381932865 ) ) ;
#22464=DIRECTION ( 'NONE',  ( 0.000000000000000000, 0.000000000000000000, 1.000000000000000000 ) ) ;
#22465=EDGE_CURVE ( 'NONE', #22704, #43358, #41244, .T. ) ;
#22470=EDGE_LOOP ( 'NONE', ( #8280, #46879, #25936, #8084 ) ) ;
#22475=DIRECTION ( 'NONE',  ( -1.000000000000000000, 0.000000000000000000, 0.000000000000000000 ) ) ;
#22486=VERTEX_POINT ( 'NONE', #15050 ) ;
#22488=ORIENTED_EDGE ( 'NONE', *, *, #43384, .T. ) ;
#22489=PLANE ( 'NONE',  #47842 ) ;
#22494=ADVANCED_FACE ( 'NONE', ( #3782 ), #26057, .T. ) ;
#22498=VERTEX_POINT ( 'NONE', #14319 ) ;
#22500=EDGE_CURVE ( 'NONE', #37649, #35793, #40744, .T. ) ;
#22501=CARTESIAN_POINT ( 'NONE',  ( 10.00000000000000000, 0.000000000000000000, 0.000000000000000000 ) ) ;
#22504=CARTESIAN_POINT ( 'NONE',  ( 5.000000000000000000, 21.40280677340421889, -36.13751322684397138 ) ) ;
#22508=LINE ( 'NONE', #14920, #46905 ) ;
#22515=DIRECTION ( 'NONE',  ( 0.000000000000000000, -0.1564344650402380854, 0.9876883405951365491 ) ) ;
#22518=EDGE_LOOP ( 'NONE', ( #31830, #34090, #20556, #37231 ) ) ;
#22521=LINE ( 'NONE', #491, #228 ) ;
#22523=DIRECTION ( 'NONE',  ( 0.000000000000000000, -0.8090169943749422332, -0.5877852522924803536 ) ) ;
#22525=DIRECTION ( 'NONE',  ( 1.000000000000000000, 0.000000000000000000, -0.000000000000000000 ) ) ;
#22541=ORIENTED_EDGE ( 'NONE', *, *, #46582, .F. ) ;
#22544=CARTESIAN_POINT ( 'NONE',  ( -3.000000000000000000, -0.9646360437372163421, -23.52805723605591126 ) ) ;
#22547=FACE_OUTER_BOUND ( 'NONE', #1866, .T. ) ;
#22551=VERTEX_POINT ( 'NONE', #6976 ) ;
#22552=CARTESIAN_POINT ( 'NONE',  ( 10.00000000000000000, -16.23288003029521320, 33.80338159004277543 ) ) ;
#22598=ADVANCED_FACE ( 'NONE', ( #5248 ), #16016, .T. ) ;
#22614=FACE_OUTER_BOUND ( 'NONE', #31289, .T. ) ;
#22629=DIRECTION ( 'NONE',  ( -1.000000000000000000, 0.000000000000000000, 0.000000000000000000 ) ) ;
#22634=EDGE_CURVE ( 'NONE', #14425, #14988, #22864, .T. ) ;
#22637=EDGE_CURVE ( 'NONE', #1846, #39388, #5757, .T. ) ;
#22639=DIRECTION ( 'NONE',  ( 1.000000000000000000, 0.000000000000000000, -0.000000000000000000 ) ) ;
#22646=AXIS2_PLACEMENT_3D ( 'NONE', #11150, #37817, #4304 ) ;
#22647=ORIENTED_EDGE ( 'NONE', *, *, #33498, .F. ) ;
#22648=CYLINDRICAL_SURFACE ( 'NONE', #10974, 16.00000000000000000 ) ;
#22651=VERTEX_POINT ( 'NONE', #30228 ) ;
#22653=EDGE_CURVE ( 'NONE', #4179, #41802, #19195, .T. ) ;
#22662=CARTESIAN_POINT ( 'NONE',  ( 10.00000000000000000, -41.91543099594819921, 2.663952781846001816 ) ) ;
#22676=ORIENTED_EDGE ( 'NONE', *, *, #13128, .T. ) ;
#22679=LINE ( 'NONE', #33461, #29034 ) ;
#22685=DIRECTION ( 'NONE',  ( 0.000000000000000000, 0.8090169943749445647, 0.5877852522924770229 ) ) ;
#22692=ORIENTED_EDGE ( 'NONE', *, *, #29201, .T. ) ;
#22704=VERTEX_POINT ( 'NONE', #28230 ) ;
#22707=EDGE_CURVE ( 'NONE', #11522, #11877, #1889, .T. ) ;
#22708=FACE_OUTER_BOUND ( 'NONE', #3940, .T. ) ;
#22716=ORIENTED_EDGE ( 'NONE', *, *, #40173, .T. ) ;
#22720=PLANE ( 'NONE',  #41668 ) ;
#22724=EDGE_LOOP ( 'NONE', ( #22692, #28006, #20714, #27904 ) ) ;
#22726=CARTESIAN_POINT ( 'NONE',  ( -3.000000000000000000, -20.55727247249726020, -16.78983467731313084 ) ) ;
#22734=CARTESIAN_POINT ( 'NONE',  ( 10.00000000000000000, -5.202137450156129717, -37.22597642581163768 ) ) ;
#22743=VERTEX_POINT ( 'NONE', #20897 ) ;
#22755=CARTESIAN_POINT ( 'NONE',  ( 4.999999999999999112, -3.925862922256468046, 41.81611651403860463 ) ) ;
#22761=EDGE_CURVE ( 'NONE', #30860, #30648, #30041, .T. ) ;
#22762=AXIS2_PLACEMENT_3D ( 'NONE', #5046, #42975, #39292 ) ;
#22764=CYLINDRICAL_SURFACE ( 'NONE', #14874, 42.00000000000000000 ) ;
#22770=DIRECTION ( 'NONE',  ( 0.000000000000000000, -0.4539904997395352027, -0.8910065241883737830 ) ) ;
#22783=AXIS2_PLACEMENT_3D ( 'NONE', #42025, #24366, #19713 ) ;
#22786=DIRECTION ( 'NONE',  ( 0.000000000000000000, 0.000000000000000000, -1.000000000000000000 ) ) ;
#22788=VECTOR ( 'NONE', #37832, 1000.000000000000000 ) ;
#22790=VERTEX_POINT ( 'NONE', #2511 ) ;
#22793=CARTESIAN_POINT ( 'NONE',  ( 0.000000000000000000, 0.000000000000000000, 0.000000000000000000 ) ) ;
#22805=PLANE ( 'NONE',  #26261 ) ;
#22806=DIRECTION ( 'NONE',  ( 1.000000000000000000, 0.000000000000000000, 0.000000000000000000 ) ) ;
#22812=LINE ( 'NONE', #4466, #30847 ) ;
#22816=EDGE_CURVE ( 'NONE', #41422, #5993, #12062, .T. ) ;
#22820=EDGE_CURVE ( 'NONE', #15589, #46205, #34706, .T. ) ;
#22821=CARTESIAN_POINT ( 'NONE',  ( 0.000000000000000000, -10.74501242461258244, -35.92658777277521409 ) ) ;
#22823=EDGE_CURVE ( 'NONE', #13181, #27382, #10344, .T. ) ;
#22824=CARTESIAN_POINT ( 'NONE',  ( 0.000000000000000000, 0.000000000000000000, 0.000000000000000000 ) ) ;
#22836=VERTEX_POINT ( 'NONE', #44126 ) ;
#22842=DIRECTION ( 'NONE',  ( 0.000000000000000000, -0.9876883405951393247, 0.1564344650402204329 ) ) ;
#22843=VERTEX_POINT ( 'NONE', #32624 ) ;
#22845=EDGE_LOOP ( 'NONE', ( #23722, #2650, #2232, #25093 ) ) ;
#22852=ORIENTED_EDGE ( 'NONE', *, *, #18329, .F. ) ;
#22853=DIRECTION ( 'NONE',  ( 0.000000000000000000, 0.000000000000000000, 1.000000000000000000 ) ) ;
#22856=CYLINDRICAL_SURFACE ( 'NONE', #24441, 37.49900000000000233 ) ;
#22861=CYLINDRICAL_SURFACE ( 'NONE', #24770, 16.00000000000000000 ) ;
#22862=VECTOR ( 'NONE', #30867, 1000.000000000000000 ) ;
#22863=CARTESIAN_POINT ( 'NONE',  ( 0.000000000000000000, -25.88420570971381807, -27.13269053701123212 ) ) ;
#22864=LINE ( 'NONE', #824, #4184 ) ;
#22868=CARTESIAN_POINT ( 'NONE',  ( 0.000000000000000000, 33.80338159004283938, 16.23288003029508886 ) ) ;
#22871=ORIENTED_EDGE ( 'NONE', *, *, #40052, .T. ) ;
#22874=FACE_OUTER_BOUND ( 'NONE', #46978, .T. ) ;
#22893=CIRCLE ( 'NONE', #26811, 16.00000000000000000 ) ;
#22899=AXIS2_PLACEMENT_3D ( 'NONE', #29482, #44412, #10880 ) ;
#22909=LINE ( 'NONE', #33209, #14335 ) ;
#22910=DIRECTION ( 'NONE',  ( 0.000000000000000000, 0.000000000000000000, 1.000000000000000000 ) ) ;
#22929=AXIS2_PLACEMENT_3D ( 'NONE', #19701, #16301, #16537 ) ;
#22934=CIRCLE ( 'NONE', #24509, 37.49900000000000233 ) ;
#22946=AXIS2_PLACEMENT_3D ( 'NONE', #26196, #15900, #11272 ) ;
#22972=ORIENTED_EDGE ( 'NONE', *, *, #46816, .T. ) ;
#22974=AXIS2_PLACEMENT_3D ( 'NONE', #30338, #11499, #3898 ) ;
#22989=CYLINDRICAL_SURFACE ( 'NONE', #19180, 42.00000000000000000 ) ;
#22992=LINE ( 'NONE', #35388, #30891 ) ;
#23011=DIRECTION ( 'NONE',  ( 0.000000000000000000, 0.000000000000000000, 1.000000000000000000 ) ) ;
#23042=EDGE_CURVE ( 'NONE', #6278, #45279, #22812, .T. ) ;
#23044=ADVANCED_FACE ( 'NONE', ( #543 ), #12527, .F. ) ;
#23047=ORIENTED_EDGE ( 'NONE', *, *, #31299, .F. ) ;
#23058=DIRECTION ( 'NONE',  ( -1.000000000000000000, -0.000000000000000000, -0.000000000000000000 ) ) ;
#23072=DIRECTION ( 'NONE',  ( 0.000000000000000000, 0.8660254037844432595, -0.4999999999999919509 ) ) ;
#23080=ORIENTED_EDGE ( 'NONE', *, *, #27000, .T. ) ;
#23094=EDGE_LOOP ( 'NONE', ( #38566, #25976, #35215, #36153 ) ) ;
#23127=ORIENTED_EDGE ( 'NONE', *, *, #24369, .F. ) ;
#23130=CARTESIAN_POINT ( 'NONE',  ( 0.000000000000000000, 16.45098606841126454, 33.79645857604518966 ) ) ;
#23135=ORIENTED_EDGE ( 'NONE', *, *, #33706, .F. ) ;
#23139=LINE ( 'NONE', #15329, #3129 ) ;
#23156=DIRECTION ( 'NONE',  ( -1.000000000000000000, 0.000000000000000000, 0.000000000000000000 ) ) ;
#23159=CARTESIAN_POINT ( 'NONE',  ( -10.00000000000000000, 0.000000000000000000, 0.000000000000000000 ) ) ;
#23166=VERTEX_POINT ( 'NONE', #46786 ) ;
#23183=CIRCLE ( 'NONE', #45877, 16.00000000000000000 ) ;
#23184=ORIENTED_EDGE ( 'NONE', *, *, #26386, .F. ) ;
#23187=CYLINDRICAL_SURFACE ( 'NONE', #3049, 42.00000000000000000 ) ;
#23204=DIRECTION ( 'NONE',  ( -1.000000000000000000, 0.000000000000000000, 0.000000000000000000 ) ) ;
#23212=ORIENTED_EDGE ( 'NONE', *, *, #11460, .T. ) ;
#23219=VERTEX_POINT ( 'NONE', #31625 ) ;
#23227=DIRECTION ( 'NONE',  ( 1.000000000000000000, -0.000000000000000000, 0.000000000000000000 ) ) ;
#23232=VECTOR ( 'NONE', #26545, 1000.000000000000000 ) ;
#23238=DIRECTION ( 'NONE',  ( -1.000000000000000000, 0.000000000000000000, -0.000000000000000000 ) ) ;
#23243=VERTEX_POINT ( 'NONE', #35029 ) ;
#23250=EDGE_CURVE ( 'NONE', #23509, #13181, #32417, .T. ) ;
#23264=DIRECTION ( 'NONE',  ( 1.000000000000000000, -0.000000000000000000, 0.000000000000000000 ) ) ;
#23269=CARTESIAN_POINT ( 'NONE',  ( 0.000000000000000000, -27.13269053701078448, -25.88420570971428702 ) ) ;
#23271=DIRECTION ( 'NONE',  ( -1.000000000000000000, 0.000000000000000000, -0.000000000000000000 ) ) ;
#23273=EDGE_LOOP ( 'NONE', ( #1173, #47740, #11446, #33140 ) ) ;
#23281=CARTESIAN_POINT ( 'NONE',  ( 10.00000000000000000, 35.53030884539102630, -12.26510123303222599 ) ) ;
#23282=ORIENTED_EDGE ( 'NONE', *, *, #22295, .F. ) ;
#23285=DIRECTION ( 'NONE',  ( -1.000000000000000000, 0.000000000000000000, 0.000000000000000000 ) ) ;
#23296=CIRCLE ( 'NONE', #9211, 37.49900000000000233 ) ;
#23309=CARTESIAN_POINT ( 'NONE',  ( 10.00000000000000000, -9.188173127307003085, -40.98264845739760176 ) ) ;
#23310=ADVANCED_FACE ( 'NONE', ( #25447 ), #10045, .T. ) ;
#23315=VERTEX_POINT ( 'NONE', #24967 ) ;
#23318=ORIENTED_EDGE ( 'NONE', *, *, #21613, .F. ) ;
#23321=AXIS2_PLACEMENT_3D ( 'NONE', #47100, #17947, #10376 ) ;
#23328=DIRECTION ( 'NONE',  ( 0.000000000000000000, 0.9945218953682742891, -0.1045284632676436315 ) ) ;
#23343=CARTESIAN_POINT ( 'NONE',  ( 0.000000000000000000, 0.8828120875900632436, 37.48860685352291000 ) ) ;
#23346=LINE ( 'NONE', #11854, #11471 ) ;
#23347=CARTESIAN_POINT ( 'NONE',  ( -10.00000000000000000, 0.000000000000000000, 0.000000000000000000 ) ) ;
#23349=EDGE_LOOP ( 'NONE', ( #41896, #43662, #20012, #26527 ) ) ;
#23352=DIRECTION ( 'NONE',  ( 0.000000000000000000, 0.7071067811865487940, -0.7071067811865462405 ) ) ;
#23356=CIRCLE ( 'NONE', #42898, 42.00000000000000000 ) ;
#23359=ORIENTED_EDGE ( 'NONE', *, *, #7193, .T. ) ;
#23362=EDGE_CURVE ( 'NONE', #12471, #34159, #1927, .T. ) ;
#23368=ADVANCED_FACE ( 'NONE', ( #18597 ), #33517, .T. ) ;
#23369=EDGE_CURVE ( 'NONE', #21200, #48285, #32567, .T. ) ;
#23373=DIRECTION ( 'NONE',  ( 0.000000000000000000, 0.000000000000000000, 1.000000000000000000 ) ) ;
#23376=LINE ( 'NONE', #9408, #20217 ) ;
#23380=ORIENTED_EDGE ( 'NONE', *, *, #24103, .F. ) ;
#23382=EDGE_LOOP ( 'NONE', ( #34176, #6970, #48324, #27236 ) ) ;
#23394=ADVANCED_FACE ( 'NONE', ( #21550 ), #2938, .T. ) ;
#23403=EDGE_CURVE ( 'NONE', #41148, #35055, #45693, .T. ) ;
#23407=ORIENTED_EDGE ( 'NONE', *, *, #12664, .F. ) ;
#23413=CARTESIAN_POINT ( 'NONE',  ( 10.00000000000000000, -37.58145647212455032, 0.6853352020789044152 ) ) ;
#23415=EDGE_CURVE ( 'NONE', #35410, #39037, #45498, .T. ) ;
#23416=CIRCLE ( 'NONE', #15596, 16.00000000000000000 ) ;
#23422=EDGE_CURVE ( 'NONE', #31590, #15551, #47296, .T. ) ;
#23424=VERTEX_POINT ( 'NONE', #7818 ) ;
#23427=CARTESIAN_POINT ( 'NONE',  ( 5.000000000000000000, -38.55633173626998911, -16.65560815589452304 ) ) ;
#23429=EDGE_LOOP ( 'NONE', ( #15871, #4769, #28923, #45704 ) ) ;
#23433=VERTEX_POINT ( 'NONE', #20459 ) ;
#23440=FACE_OUTER_BOUND ( 'NONE', #35421, .T. ) ;
#23441=ORIENTED_EDGE ( 'NONE', *, *, #13480, .T. ) ;
#23446=EDGE_CURVE ( 'NONE', #3270, #24628, #22992, .T. ) ;
#23457=DIRECTION ( 'NONE',  ( 0.000000000000000000, 0.000000000000000000, 1.000000000000000000 ) ) ;
#23458=VECTOR ( 'NONE', #16249, 1000.000000000000000 ) ;
#23469=VERTEX_POINT ( 'NONE', #1630 ) ;
#23488=EDGE_CURVE ( 'NONE', #47828, #24283, #41061, .T. ) ;
#23494=ORIENTED_EDGE ( 'NONE', *, *, #19542, .F. ) ;
#23495=DIRECTION ( 'NONE',  ( -1.000000000000000000, 0.000000000000000000, 0.000000000000000000 ) ) ;
#23509=VERTEX_POINT ( 'NONE', #26434 ) ;
#23510=DIRECTION ( 'NONE',  ( 0.000000000000000000, 0.000000000000000000, 1.000000000000000000 ) ) ;
#23530=EDGE_CURVE ( 'NONE', #26404, #911, #1169, .T. ) ;
#23537=DIRECTION ( 'NONE',  ( -1.000000000000000000, 0.000000000000000000, 0.000000000000000000 ) ) ;
#23544=EDGE_LOOP ( 'NONE', ( #30246, #7857, #30995, #9303 ) ) ;
#23551=EDGE_LOOP ( 'NONE', ( #17697, #41975, #11038, #1724 ) ) ;
#23554=CIRCLE ( 'NONE', #2449, 37.49900000000000944 ) ;
#23559=CARTESIAN_POINT ( 'NONE',  ( 10.00000000000000000, 30.00120703465205452, 22.64427369931179967 ) ) ;
#23571=LINE ( 'NONE', #16250, #46179 ) ;
#23588=EDGE_LOOP ( 'NONE', ( #44229, #12148, #34481, #39472 ) ) ;
#23593=CYLINDRICAL_SURFACE ( 'NONE', #44061, 37.49900000000000233 ) ;
#23599=EDGE_CURVE ( 'NONE', #41810, #8149, #43479, .T. ) ;
#23606=ORIENTED_EDGE ( 'NONE', *, *, #16403, .F. ) ;
#23609=DIRECTION ( 'NONE',  ( 0.000000000000000000, 0.8090169943749445647, 0.5877852522924770229 ) ) ;
#23613=ORIENTED_EDGE ( 'NONE', *, *, #19399, .F. ) ;
#23627=DIRECTION ( 'NONE',  ( -1.000000000000000000, -0.000000000000000000, -0.000000000000000000 ) ) ;
#23631=FACE_OUTER_BOUND ( 'NONE', #44782, .T. ) ;
#23636=ORIENTED_EDGE ( 'NONE', *, *, #23042, .F. ) ;
#23639=CIRCLE ( 'NONE', #45504, 37.49900000000001654 ) ;
#23667=VERTEX_POINT ( 'NONE', #44913 ) ;
#23668=AXIS2_PLACEMENT_3D ( 'NONE', #13417, #20998, #25142 ) ;
#23669=EDGE_CURVE ( 'NONE', #18905, #1468, #7219, .T. ) ;
#23679=ORIENTED_EDGE ( 'NONE', *, *, #38868, .F. ) ;
#23682=ORIENTED_EDGE ( 'NONE', *, *, #44199, .F. ) ;
#23692=DIRECTION ( 'NONE',  ( 0.000000000000000000, 0.000000000000000000, 1.000000000000000000 ) ) ;
#23695=EDGE_CURVE ( 'NONE', #1711, #19709, #21899, .T. ) ;
#23706=EDGE_CURVE ( 'NONE', #14949, #43486, #26316, .T. ) ;
#23708=LINE ( 'NONE', #19307, #25551 ) ;
#23716=VECTOR ( 'NONE', #2079, 1000.000000000000000 ) ;
#23722=ORIENTED_EDGE ( 'NONE', *, *, #11878, .F. ) ;
#23724=DIRECTION ( 'NONE',  ( 0.000000000000000000, 0.000000000000000000, -1.000000000000000000 ) ) ;
#23737=LINE ( 'NONE', #16399, #6734 ) ;
#23741=VECTOR ( 'NONE', #26928, 1000.000000000000000 ) ;
#23761=CARTESIAN_POINT ( 'NONE',  ( 0.000000000000000000, 22.48208911017551515, -35.47612816024499693 ) ) ;
#23771=AXIS2_PLACEMENT_3D ( 'NONE', #38827, #5287, #39286 ) ;
#23776=LINE ( 'NONE', #46295, #1395 ) ;
#23780=AXIS2_PLACEMENT_3D ( 'NONE', #7534, #32977, #37142 ) ;
#23781=CARTESIAN_POINT ( 'NONE',  ( 0.000000000000000000, -9.188173127307001309, -40.98264845739759465 ) ) ;
#23786=VECTOR ( 'NONE', #27909, 999.9999999999998863 ) ;
#23787=PRODUCT_CONTEXT ( 'NONE', #3183, 'mechanical' ) ;
#23788=CARTESIAN_POINT ( 'NONE',  ( 10.00000000000000000, 37.48860685352291000, -0.8828120875901940279 ) ) ;
#23790=ORIENTED_EDGE ( 'NONE', *, *, #12761, .F. ) ;
#23791=EDGE_CURVE ( 'NONE', #4718, #25973, #48334, .T. ) ;
#23806=EDGE_LOOP ( 'NONE', ( #45202, #15872, #9050, #981 ) ) ;
#23823=CARTESIAN_POINT ( 'NONE',  ( 0.000000000000000000, -37.58145647212455032, 0.6853352020789044152 ) ) ;
#23833=EDGE_CURVE ( 'NONE', #27870, #15338, #45765, .T. ) ;
#23837=DIRECTION ( 'NONE',  ( -1.000000000000000000, 0.000000000000000000, 0.000000000000000000 ) ) ;
#23841=DIRECTION ( 'NONE',  ( 0.000000000000000000, 0.9510565162951503115, 0.3090169943749573878 ) ) ;
#23845=DIRECTION ( 'NONE',  ( 0.000000000000000000, 0.000000000000000000, 1.000000000000000000 ) ) ;
#23847=DIRECTION ( 'NONE',  ( -1.000000000000000000, 0.000000000000000000, 0.000000000000000000 ) ) ;
#23852=CIRCLE ( 'NONE', #46542, 16.00000000000000000 ) ;
#23864=CARTESIAN_POINT ( 'NONE',  ( 10.00000000000000000, -29.81001611431024756, 22.74946021919122785 ) ) ;
#23865=ORIENTED_EDGE ( 'NONE', *, *, #14878, .F. ) ;
#23870=CARTESIAN_POINT ( 'NONE',  ( 0.000000000000000000, 36.88895765772642221, -6.736453364083161865 ) ) ;
#23871=AXIS2_PLACEMENT_3D ( 'NONE', #37793, #23837, #4513 ) ;
#23878=CARTESIAN_POINT ( 'NONE',  ( 0.000000000000000000, -26.23277895567251505, 4.042438405569750870 ) ) ;
#23881=CARTESIAN_POINT ( 'NONE',  ( 10.00000000000000000, 0.000000000000000000, 0.000000000000000000 ) ) ;
#23883=DIRECTION ( 'NONE',  ( -0.000000000000000000, 0.5877852522924696954, 0.8090169943749498938 ) ) ;
#23892=VERTEX_POINT ( 'NONE', #10315 ) ;
#23895=AXIS2_PLACEMENT_3D ( 'NONE', #16731, #30690, #27270 ) ;
#23904=AXIS2_PLACEMENT_3D ( 'NONE', #6204, #13793, #2992 ) ;
#23911=AXIS2_PLACEMENT_3D ( 'NONE', #27494, #24286, #31169 ) ;
#23913=ORIENTED_EDGE ( 'NONE', *, *, #48173, .F. ) ;
#23917=CARTESIAN_POINT ( 'NONE',  ( 0.000000000000000000, 0.000000000000000000, 0.000000000000000000 ) ) ;
#23941=DIRECTION ( 'NONE',  ( 0.000000000000000000, 0.000000000000000000, 1.000000000000000000 ) ) ;
#23949=ORIENTED_EDGE ( 'NONE', *, *, #14592, .T. ) ;
#23953=AXIS2_PLACEMENT_3D ( 'NONE', #43809, #28655, #25927 ) ;
#23956=EDGE_CURVE ( 'NONE', #45280, #44883, #34006, .T. ) ;
#23960=LINE ( 'NONE', #34960, #9113 ) ;
#23964=CARTESIAN_POINT ( 'NONE',  ( -3.000000000000000000, 8.688484142254221609, -21.88630264137359660 ) ) ;
#23966=EDGE_CURVE ( 'NONE', #44892, #9789, #40714, .T. ) ;
#23967=CIRCLE ( 'NONE', #17698, 16.00000000000000711 ) ;
#23968=DIRECTION ( 'NONE',  ( -1.000000000000000000, 0.000000000000000000, 0.000000000000000000 ) ) ;
#23971=CYLINDRICAL_SURFACE ( 'NONE', #8873, 37.49900000000000233 ) ;
#23977=ORIENTED_EDGE ( 'NONE', *, *, #28618, .T. ) ;
#23984=EDGE_CURVE ( 'NONE', #27526, #5723, #44990, .T. ) ;
#23985=CARTESIAN_POINT ( 'NONE',  ( 5.000000000000000000, 32.34446384429971744, 26.79245525562726016 ) ) ;
#23987=ORIENTED_EDGE ( 'NONE', *, *, #11813, .T. ) ;
#23990=EDGE_CURVE ( 'NONE', #9753, #46024, #25054, .T. ) ;
#24011=LINE ( 'NONE', #31855, #8025 ) ;
#24017=DIRECTION ( 'NONE',  ( -1.000000000000000000, 0.000000000000000000, -0.000000000000000000 ) ) ;
#24038=AXIS2_PLACEMENT_3D ( 'NONE', #34653, #12408, #19477 ) ;
#24043=LINE ( 'NONE', #27964, #2317 ) ;
#24071=CIRCLE ( 'NONE', #45169, 42.00000000000000000 ) ;
#24073=DIRECTION ( 'NONE',  ( -1.000000000000000000, 0.000000000000000000, 0.000000000000000000 ) ) ;
#24077=CARTESIAN_POINT ( 'NONE',  ( 0.000000000000000000, 0.000000000000000000, 0.000000000000000000 ) ) ;
#24084=DIRECTION ( 'NONE',  ( -1.000000000000000000, 0.000000000000000000, 0.000000000000000000 ) ) ;
#24089=CARTESIAN_POINT ( 'NONE',  ( 0.000000000000000000, 6.762365576493645669, -25.66652317338392209 ) ) ;
#24102=CARTESIAN_POINT ( 'NONE',  ( 4.999999999999999112, -10.41901085202107247, 40.68715046381925049 ) ) ;
#24103=EDGE_CURVE ( 'NONE', #27674, #29067, #14489, .T. ) ;
#24104=CARTESIAN_POINT ( 'NONE',  ( 0.000000000000000000, -12.26510123303284594, 35.53030884539080603 ) ) ;
#24111=ORIENTED_EDGE ( 'NONE', *, *, #30300, .F. ) ;
#24116=ORIENTED_EDGE ( 'NONE', *, *, #8773, .F. ) ;
#24118=CARTESIAN_POINT ( 'NONE',  ( 10.00000000000000000, -0.6853352020793173072, 37.58145647212453611 ) ) ;
#24122=CARTESIAN_POINT ( 'NONE',  ( 0.000000000000000000, 27.05870788708231700, 26.08949754953034272 ) ) ;
#24135=CARTESIAN_POINT ( 'NONE',  ( 10.00000000000000000, 0.000000000000000000, 0.000000000000000000 ) ) ;
#24142=DIRECTION ( 'NONE',  ( 0.000000000000000000, 0.4067366430757887730, 0.9135454576426059736 ) ) ;
#24146=ORIENTED_EDGE ( 'NONE', *, *, #5265, .T. ) ;
#24154=ORIENTED_EDGE ( 'NONE', *, *, #40417, .F. ) ;
#24158=CIRCLE ( 'NONE', #16332, 37.49900000000000944 ) ;
#24162=ORIENTED_EDGE ( 'NONE', *, *, #14706, .F. ) ;
#24163=EDGE_LOOP ( 'NONE', ( #12224, #41067, #17608, #31647 ) ) ;
#24167=ADVANCED_FACE ( 'NONE', ( #31104 ), #970, .T. ) ;
#24179=CYLINDRICAL_SURFACE ( 'NONE', #46373, 16.00000000000000000 ) ;
#24185=ORIENTED_EDGE ( 'NONE', *, *, #8622, .T. ) ;
#24195=EDGE_CURVE ( 'NONE', #30860, #14490, #23737, .T. ) ;
#24197=LINE ( 'NONE', #39133, #30040 ) ;
#24206=AXIS2_PLACEMENT_3D ( 'NONE', #45127, #26523, #575 ) ;
#24209=VERTEX_POINT ( 'NONE', #1715 ) ;
#24210=EDGE_CURVE ( 'NONE', #16571, #13285, #30603, .T. ) ;
#24212=EDGE_CURVE ( 'NONE', #5067, #33061, #45522, .T. ) ;
#24216=VERTEX_POINT ( 'NONE', #38195 ) ;
#24222=DIRECTION ( 'NONE',  ( 0.000000000000000000, 0.8910065241883688980, -0.4539904997395445840 ) ) ;
#24223=ORIENTED_EDGE ( 'NONE', *, *, #43280, .T. ) ;
#24228=VERTEX_POINT ( 'NONE', #45790 ) ;
#24232=CARTESIAN_POINT ( 'NONE',  ( 10.00000000000000000, 0.000000000000000000, 0.000000000000000000 ) ) ;
#24233=CARTESIAN_POINT ( 'NONE',  ( 0.000000000000000000, 41.91543099594818500, 2.663952781846294915 ) ) ;
#24244=CARTESIAN_POINT ( 'NONE',  ( 10.00000000000000000, 35.53030884539102630, -12.26510123303222599 ) ) ;
#24251=DIRECTION ( 'NONE',  ( -1.000000000000000000, 0.000000000000000000, -0.000000000000000000 ) ) ;
#24257=EDGE_CURVE ( 'NONE', #1330, #11693, #5881, .T. ) ;
#24258=ORIENTED_EDGE ( 'NONE', *, *, #48287, .F. ) ;
#24263=CIRCLE ( 'NONE', #3131, 42.00000000000000000 ) ;
#24271=AXIS2_PLACEMENT_3D ( 'NONE', #18402, #7389, #11060 ) ;
#24275=CARTESIAN_POINT ( 'NONE',  ( -3.000000000000000000, -19.89357724624987256, -12.59942793731086041 ) ) ;
#24277=EDGE_CURVE ( 'NONE', #15551, #46699, #16105, .T. ) ;
#24281=CYLINDRICAL_SURFACE ( 'NONE', #43428, 37.49900000000000233 ) ;
#24283=VERTEX_POINT ( 'NONE', #47224 ) ;
#24286=DIRECTION ( 'NONE',  ( -1.000000000000000000, -0.000000000000000000, -0.000000000000000000 ) ) ;
#24305=AXIS2_PLACEMENT_3D ( 'NONE', #29888, #33789, #22786 ) ;
#24308=LINE ( 'NONE', #16488, #17368 ) ;
#24317=DIRECTION ( 'NONE',  ( -1.000000000000000000, 0.000000000000000000, 0.000000000000000000 ) ) ;
#24332=AXIS2_PLACEMENT_3D ( 'NONE', #25911, #3646, #40850 ) ;
#24335=CARTESIAN_POINT ( 'NONE',  ( 10.00000000000000000, 0.000000000000000000, 0.000000000000000000 ) ) ;
#24336=DIRECTION ( 'NONE',  ( 0.000000000000000000, 0.000000000000000000, 1.000000000000000000 ) ) ;
#24337=AXIS2_PLACEMENT_3D ( 'NONE', #43077, #35727, #42841 ) ;
#24339=DIRECTION ( 'NONE',  ( -1.000000000000000000, -0.000000000000000000, -0.000000000000000000 ) ) ;
#24359=ADVANCED_FACE ( 'NONE', ( #2657 ), #6115, .T. ) ;
#24364=EDGE_CURVE ( 'NONE', #24727, #46139, #26270, .T. ) ;
#24366=DIRECTION ( 'NONE',  ( 0.000000000000000000, -0.1045284632676570791, 0.9945218953682730678 ) ) ;
#24368=DIRECTION ( 'NONE',  ( -1.000000000000000000, -0.000000000000000000, -0.000000000000000000 ) ) ;
#24369=EDGE_CURVE ( 'NONE', #34495, #16571, #45028, .T. ) ;
#24375=DIRECTION ( 'NONE',  ( -0.000000000000000000, 0.5877852522924696954, 0.8090169943749498938 ) ) ;
#24396=AXIS2_PLACEMENT_3D ( 'NONE', #42743, #35131, #5774 ) ;
#24402=ORIENTED_EDGE ( 'NONE', *, *, #42812, .F. ) ;
#24404=LINE ( 'NONE', #47411, #38007 ) ;
#24423=DIRECTION ( 'NONE',  ( 1.000000000000000000, -0.000000000000000000, -0.000000000000000000 ) ) ;
#24424=LINE ( 'NONE', #6085, #9731 ) ;
#24429=ADVANCED_FACE ( 'NONE', ( #47925 ), #450, .T. ) ;
#24438=AXIS2_PLACEMENT_3D ( 'NONE', #47172, #35908, #43514 ) ;
#24441=AXIS2_PLACEMENT_3D ( 'NONE', #16255, #11612, #27269 ) ;
#24444=VECTOR ( 'NONE', #23883, 1000.000000000000227 ) ;
#24446=CARTESIAN_POINT ( 'NONE',  ( 0.000000000000000000, 0.000000000000000000, 0.000000000000000000 ) ) ;
#24449=DIRECTION ( 'NONE',  ( 0.000000000000000000, 0.2079116908177664758, -0.9781476007338042455 ) ) ;
#24452=ORIENTED_EDGE ( 'NONE', *, *, #32614, .F. ) ;
#24453=ORIENTED_EDGE ( 'NONE', *, *, #15737, .T. ) ;
#24455=EDGE_LOOP ( 'NONE', ( #33248, #4263, #8141, #26760 ) ) ;
#24459=ORIENTED_EDGE ( 'NONE', *, *, #3252, .T. ) ;
#24488=LINE ( 'NONE', #12754, #47653 ) ;
#24491=LINE ( 'NONE', #9316, #9913 ) ;
#24509=AXIS2_PLACEMENT_3D ( 'NONE', #38590, #38340, #38841 ) ;
#24512=AXIS2_PLACEMENT_3D ( 'NONE', #16696, #20596, #36003 ) ;
#24515=FACE_OUTER_BOUND ( 'NONE', #46486, .T. ) ;
#24523=CARTESIAN_POINT ( 'NONE',  ( 10.00000000000000000, 0.000000000000000000, 0.000000000000000000 ) ) ;
#24531=DIRECTION ( 'NONE',  ( 0.000000000000000000, 0.000000000000000000, 1.000000000000000000 ) ) ;
#24550=DIRECTION ( 'NONE',  ( 0.000000000000000000, 0.000000000000000000, -1.000000000000000000 ) ) ;
#24553=EDGE_CURVE ( 'NONE', #24690, #13149, #23967, .T. ) ;
#24573=LINE ( 'NONE', #32860, #1872 ) ;
#24574=VERTEX_POINT ( 'NONE', #34941 ) ;
#24577=EDGE_CURVE ( 'NONE', #23219, #13751, #13031, .T. ) ;
#24586=CARTESIAN_POINT ( 'NONE',  ( 0.000000000000000000, -22.48208911017474065, -35.47612816024548721 ) ) ;
#24587=AXIS2_PLACEMENT_3D ( 'NONE', #17801, #36159, #32502 ) ;
#24594=EDGE_CURVE ( 'NONE', #26813, #28893, #38377, .T. ) ;
#24595=DIRECTION ( 'NONE',  ( 0.000000000000000000, 0.7431448254773862505, 0.6691306063588672304 ) ) ;
#24597=CARTESIAN_POINT ( 'NONE',  ( 10.00000000000000000, 0.000000000000000000, 0.000000000000000000 ) ) ;
#24599=CARTESIAN_POINT ( 'NONE',  ( 10.00000000000000000, 33.17418723428333749, -17.67226234102790272 ) ) ;
#24606=FACE_BOUND ( 'NONE', #20370, .T. ) ;
#24607=CARTESIAN_POINT ( 'NONE',  ( 0.000000000000000000, 27.05870788708267582, -26.08949754952995903 ) ) ;
#24613=CARTESIAN_POINT ( 'NONE',  ( 10.00000000000000000, 10.96151621346487914, 35.95386929396260456 ) ) ;
#24628=VERTEX_POINT ( 'NONE', #8021 ) ;
#24637=FACE_OUTER_BOUND ( 'NONE', #26836, .T. ) ;
#24658=CARTESIAN_POINT ( 'NONE',  ( 0.000000000000000000, 0.000000000000000000, 0.000000000000000000 ) ) ;
#24659=ORIENTED_EDGE ( 'NONE', *, *, #25487, .T. ) ;
#24665=LINE ( 'NONE', #5343, #44766 ) ;
#24690=VERTEX_POINT ( 'NONE', #17291 ) ;
#24691=VERTEX_POINT ( 'NONE', #1912 ) ;
#24692=EDGE_CURVE ( 'NONE', #29358, #19822, #18468, .T. ) ;
#24693=AXIS2_PLACEMENT_3D ( 'NONE', #32296, #46985, #32066 ) ;
#24697=CARTESIAN_POINT ( 'NONE',  ( 0.000000000000000000, -26.23277895567245821, -4.042438405570103477 ) ) ;
#24700=ORIENTED_EDGE ( 'NONE', *, *, #38571, .F. ) ;
#24701=AXIS2_PLACEMENT_3D ( 'NONE', #15055, #7701, #7472 ) ;
#24708=AXIS2_PLACEMENT_3D ( 'NONE', #36354, #29252, #32908 ) ;
#24713=ORIENTED_EDGE ( 'NONE', *, *, #38451, .T. ) ;
#24717=EDGE_CURVE ( 'NONE', #14664, #16979, #24404, .T. ) ;
#24725=DIRECTION ( 'NONE',  ( -1.000000000000000000, 0.000000000000000000, -0.000000000000000000 ) ) ;
#24727=VERTEX_POINT ( 'NONE', #17541 ) ;
#24729=LINE ( 'NONE', #35250, #41652 ) ;
#24732=CARTESIAN_POINT ( 'NONE',  ( 10.00000000000000000, 12.42422080174639021, 35.38097989696516521 ) ) ;
#24736=DIRECTION ( 'NONE',  ( 0.000000000000000000, 0.000000000000000000, 1.000000000000000000 ) ) ;
#24738=FACE_OUTER_BOUND ( 'NONE', #27362, .T. ) ;
#24758=EDGE_CURVE ( 'NONE', #29067, #38747, #39101, .T. ) ;
#24769=DIRECTION ( 'NONE',  ( -0.000000000000000000, 0.9781476007338042455, 0.2079116908177664758 ) ) ;
#24770=AXIS2_PLACEMENT_3D ( 'NONE', #30693, #44901, #19656 ) ;
#24777=CARTESIAN_POINT ( 'NONE',  ( -3.000000000000000000, 6.762365576493643893, -25.66652317338391853 ) ) ;
#24780=AXIS2_PLACEMENT_3D ( 'NONE', #35143, #42988, #16554 ) ;
#24787=DIRECTION ( 'NONE',  ( -1.000000000000000000, 0.000000000000000000, 0.000000000000000000 ) ) ;
#24790=LINE ( 'NONE', #10588, #43829 ) ;
#24804=LINE ( 'NONE', #43878, #25178 ) ;
#24830=DIRECTION ( 'NONE',  ( -0.000000000000000000, 0.9510565162951539753, -0.3090169943749460635 ) ) ;
#24834=AXIS2_PLACEMENT_3D ( 'NONE', #46176, #4579, #22685 ) ;
#24835=ORIENTED_EDGE ( 'NONE', *, *, #36676, .F. ) ;
#24839=PLANE ( 'NONE',  #47255 ) ;
#24845=CARTESIAN_POINT ( 'NONE',  ( 10.00000000000000000, 16.65560815589411092, 38.55633173627015964 ) ) ;
#24846=AXIS2_PLACEMENT_3D ( 'NONE', #30495, #45417, #19697 ) ;
#24856=CARTESIAN_POINT ( 'NONE',  ( 0.000000000000000000, -20.55727247249748046, 16.78983467731285018 ) ) ;
#24857=EDGE_LOOP ( 'NONE', ( #48072, #31264, #12978, #47554 ) ) ;
#24865=ADVANCED_FACE ( 'NONE', ( #21933 ), #11430, .T. ) ;
#24874=ORIENTED_EDGE ( 'NONE', *, *, #23833, .T. ) ;
#24880=ORIENTED_EDGE ( 'NONE', *, *, #10310, .F. ) ;
#24883=EDGE_CURVE ( 'NONE', #39350, #12661, #15403, .T. ) ;
#24885=VERTEX_POINT ( 'NONE', #22662 ) ;
#24891=DIRECTION ( 'NONE',  ( -1.000000000000000000, 0.000000000000000000, 0.000000000000000000 ) ) ;
#24893=VECTOR ( 'NONE', #32499, 1000.000000000000000 ) ;
#24898=AXIS2_PLACEMENT_3D ( 'NONE', #33905, #4784, #1595 ) ;
#24902=ORIENTED_EDGE ( 'NONE', *, *, #11602, .F. ) ;
#24907=CARTESIAN_POINT ( 'NONE',  ( 10.00000000000000000, 5.202137450156389953, 37.22597642581160216 ) ) ;
#24910=ORIENTED_EDGE ( 'NONE', *, *, #2, .T. ) ;
#24911=CARTESIAN_POINT ( 'NONE',  ( 10.00000000000000000, 0.000000000000000000, 0.000000000000000000 ) ) ;
#24912=VECTOR ( 'NONE', #7878, 1000.000000000000000 ) ;
#24914=ADVANCED_FACE ( 'NONE', ( #33201 ), #41045, .T. ) ;
#24927=EDGE_LOOP ( 'NONE', ( #5590, #10519, #15534, #26382 ) ) ;
#24953=LINE ( 'NONE', #39898, #46344 ) ;
#24963=CARTESIAN_POINT ( 'NONE',  ( 0.000000000000000000, 37.22597642581158084, -5.202137450156524068 ) ) ;
#24967=CARTESIAN_POINT ( 'NONE',  ( -3.000000000000000000, -25.60904388321925396, 6.976881207771172377 ) ) ;
#24970=CYLINDRICAL_SURFACE ( 'NONE', #31213, 16.00000000000000000 ) ;
#24971=CARTESIAN_POINT ( 'NONE',  ( -3.000000000000000000, 26.50000000000000000, -1.500000000000001332 ) ) ;
#24978=EDGE_CURVE ( 'NONE', #7678, #19681, #19296, .T. ) ;
#24986=DIRECTION ( 'NONE',  ( 0.000000000000000000, 0.000000000000000000, 1.000000000000000000 ) ) ;
#24993=DIRECTION ( 'NONE',  ( 0.000000000000000000, 0.000000000000000000, 1.000000000000000000 ) ) ;
#24999=DIRECTION ( 'NONE',  ( 0.000000000000000000, -0.4067366430757897722, -0.9135454576426056406 ) ) ;
#25015=CARTESIAN_POINT ( 'NONE',  ( 0.000000000000000000, 0.000000000000000000, 0.000000000000000000 ) ) ;
#25023=CIRCLE ( 'NONE', #31268, 16.00000000000000000 ) ;
#25025=DIRECTION ( 'NONE',  ( -1.000000000000000000, 0.000000000000000000, 0.000000000000000000 ) ) ;
#25030=DIRECTION ( 'NONE',  ( 0.000000000000000000, 0.000000000000000000, 1.000000000000000000 ) ) ;
#25035=AXIS2_PLACEMENT_3D ( 'NONE', #10148, #43459, #3038 ) ;
#25036=ORIENTED_EDGE ( 'NONE', *, *, #45031, .F. ) ;
#25039=ORIENTED_EDGE ( 'NONE', *, *, #25846, .T. ) ;
#25051=CIRCLE ( 'NONE', #12566, 16.00000000000000000 ) ;
#25053=EDGE_LOOP ( 'NONE', ( #44305, #7836, #36584, #19604 ) ) ;
#25054=LINE ( 'NONE', #18184, #17621 ) ;
#25069=CARTESIAN_POINT ( 'NONE',  ( 10.00000000000000000, 29.81001611431009479, 22.74946021919143391 ) ) ;
#25070=EDGE_CURVE ( 'NONE', #12381, #36640, #45188, .T. ) ;
#25076=CYLINDRICAL_SURFACE ( 'NONE', #7246, 37.49900000000000233 ) ;
#25078=DIRECTION ( 'NONE',  ( -1.000000000000000000, 0.000000000000000000, 0.000000000000000000 ) ) ;
#25087=EDGE_CURVE ( 'NONE', #1468, #7735, #23183, .T. ) ;
#25089=VECTOR ( 'NONE', #18643, 1000.000000000000227 ) ;
#25093=ORIENTED_EDGE ( 'NONE', *, *, #46732, .T. ) ;
#25094=CARTESIAN_POINT ( 'NONE',  ( 0.000000000000000000, 0.000000000000000000, 0.000000000000000000 ) ) ;
#25099=VERTEX_POINT ( 'NONE', #1602 ) ;
#25104=ORIENTED_EDGE ( 'NONE', *, *, #25155, .T. ) ;
#25107=ORIENTED_EDGE ( 'NONE', *, *, #3171, .T. ) ;
#25119=ORIENTED_EDGE ( 'NONE', *, *, #47448, .F. ) ;
#25126=CARTESIAN_POINT ( 'NONE',  ( 0.000000000000000000, 2.663952781846728790, -41.91543099594814947 ) ) ;
#25128=CARTESIAN_POINT ( 'NONE',  ( -3.000000000000000000, 14.60985201121729737, -18.46759930825687945 ) ) ;
#25133=ADVANCED_FACE ( 'NONE', ( #6242 ), #27804, .T. ) ;
#25142=DIRECTION ( 'NONE',  ( 0.000000000000000000, 0.000000000000000000, 1.000000000000000000 ) ) ;
#25147=DIRECTION ( 'NONE',  ( 0.000000000000000000, -0.3090169943749349057, -0.9510565162951576390 ) ) ;
#25150=EDGE_CURVE ( 'NONE', #25783, #25211, #34954, .T. ) ;
#25155=EDGE_CURVE ( 'NONE', #16565, #1521, #1349, .T. ) ;
#25158=CARTESIAN_POINT ( 'NONE',  ( 0.000000000000000000, 26.79245525562762253, -32.34446384429942611 ) ) ;
#25164=ORIENTED_EDGE ( 'NONE', *, *, #32978, .T. ) ;
#25167=ORIENTED_EDGE ( 'NONE', *, *, #23403, .T. ) ;
#25178=VECTOR ( 'NONE', #17198, 1000.000000000000000 ) ;
#25188=ORIENTED_EDGE ( 'NONE', *, *, #45108, .F. ) ;
#25192=LINE ( 'NONE', #10768, #2345 ) ;
#25196=FACE_OUTER_BOUND ( 'NONE', #30797, .T. ) ;
#25200=CARTESIAN_POINT ( 'NONE',  ( 0.000000000000000000, 39.04073710021366139, -15.48615015657542315 ) ) ;
#25202=ORIENTED_EDGE ( 'NONE', *, *, #14706, .T. ) ;
#25211=VERTEX_POINT ( 'NONE', #28264 ) ;
#25212=CARTESIAN_POINT ( 'NONE',  ( 0.000000000000000000, -40.68715046381937128, 10.41901085202062660 ) ) ;
#25221=VERTEX_POINT ( 'NONE', #48071 ) ;
#25222=EDGE_CURVE ( 'NONE', #27986, #8792, #18195, .T. ) ;
#25227=VERTEX_POINT ( 'NONE', #44162 ) ;
#25235=ORIENTED_EDGE ( 'NONE', *, *, #8275, .T. ) ;
#25236=CARTESIAN_POINT ( 'NONE',  ( -3.000000000000000000, 23.50000000000000000, -1.500000000000001332 ) ) ;
#25237=ORIENTED_EDGE ( 'NONE', *, *, #10493, .T. ) ;
#25250=VECTOR ( 'NONE', #35985, 1000.000000000000000 ) ;
#25274=EDGE_LOOP ( 'NONE', ( #18792, #44988, #23441, #9161 ) ) ;
#25280=VERTEX_POINT ( 'NONE', #7444 ) ;
#25295=PLANE ( 'NONE',  #35832 ) ;
#25296=CARTESIAN_POINT ( 'NONE',  ( 0.000000000000000000, -33.80338159004296017, 16.23288003029484727 ) ) ;
#25297=DIRECTION ( 'NONE',  ( -1.000000000000000000, 0.000000000000000000, 0.000000000000000000 ) ) ;
#25298=VECTOR ( 'NONE', #27966, 1000.000000000000000 ) ;
#25300=ORIENTED_EDGE ( 'NONE', *, *, #7529, .T. ) ;
#25303=VERTEX_POINT ( 'NONE', #6720 ) ;
#25306=VECTOR ( 'NONE', #21562, 1000.000000000000114 ) ;
#25308=CARTESIAN_POINT ( 'NONE',  ( 10.00000000000000000, -17.67226234102801286, -33.17418723428327354 ) ) ;
#25309=DIRECTION ( 'NONE',  ( 0.000000000000000000, 0.000000000000000000, 1.000000000000000000 ) ) ;
#25315=LINE ( 'NONE', #18466, #32992 ) ;
#25342=ORIENTED_EDGE ( 'NONE', *, *, #29629, .F. ) ;
#25358=ORIENTED_EDGE ( 'NONE', *, *, #35405, .T. ) ;
#25367=DIRECTION ( 'NONE',  ( 0.000000000000000000, 0.000000000000000000, 1.000000000000000000 ) ) ;
#25368=VECTOR ( 'NONE', #37805, 1000.000000000000000 ) ;
#25372=DIRECTION ( 'NONE',  ( 0.000000000000000000, 0.9876883405951381034, -0.1564344650402276216 ) ) ;
#25374=FACE_OUTER_BOUND ( 'NONE', #8842, .T. ) ;
#25378=AXIS2_PLACEMENT_3D ( 'NONE', #12899, #3908, #5540 ) ;
#25381=CARTESIAN_POINT ( 'NONE',  ( -3.000000000000000000, -19.89357724624987256, -12.59942793731086041 ) ) ;
#25384=CARTESIAN_POINT ( 'NONE',  ( 10.00000000000000000, 17.67226234102874116, -33.17418723428288274 ) ) ;
#25387=AXIS2_PLACEMENT_3D ( 'NONE', #42489, #27560, #34642 ) ;
#25399=DIRECTION ( 'NONE',  ( 0.000000000000000000, 0.000000000000000000, 1.000000000000000000 ) ) ;
#25405=EDGE_CURVE ( 'NONE', #43819, #41954, #30438, .T. ) ;
#25406=CARTESIAN_POINT ( 'NONE',  ( 10.00000000000000000, 0.000000000000000000, 0.000000000000000000 ) ) ;
#25413=DIRECTION ( 'NONE',  ( 0.000000000000000000, 0.5877852522924741363, -0.8090169943749465631 ) ) ;
#25417=EDGE_CURVE ( 'NONE', #48416, #44214, #41223, .T. ) ;
#25438=DIRECTION ( 'NONE',  ( 0.000000000000000000, 1.000000000000000000, -0.000000000000000000 ) ) ;
#25444=DIRECTION ( 'NONE',  ( -1.000000000000000000, 0.000000000000000000, 0.000000000000000000 ) ) ;
#25446=LINE ( 'NONE', #37678, #1797 ) ;
#25447=FACE_OUTER_BOUND ( 'NONE', #9589, .T. ) ;
#25448=CIRCLE ( 'NONE', #34053, 16.00000000000000000 ) ;
#25461=EDGE_CURVE ( 'NONE', #30912, #9341, #37296, .T. ) ;
#25477=DIRECTION ( 'NONE',  ( 0.000000000000000000, 0.000000000000000000, 1.000000000000000000 ) ) ;
#25483=DIRECTION ( 'NONE',  ( 0.000000000000000000, -0.4999999999999912847, -0.8660254037844435926 ) ) ;
#25484=DIRECTION ( 'NONE',  ( 0.000000000000000000, 0.4539904997395414754, 0.8910065241883706744 ) ) ;
#25487=EDGE_CURVE ( 'NONE', #29919, #29511, #48226, .T. ) ;
#25488=DIRECTION ( 'NONE',  ( -1.000000000000000000, -0.000000000000000000, -0.000000000000000000 ) ) ;
#25491=DIRECTION ( 'NONE',  ( -1.000000000000000000, -0.000000000000000000, 0.000000000000000000 ) ) ;
#25494=FACE_OUTER_BOUND ( 'NONE', #3155, .T. ) ;
#25502=EDGE_CURVE ( 'NONE', #6185, #32005, #39656, .T. ) ;
#25525=AXIS2_PLACEMENT_3D ( 'NONE', #3780, #45149, #41970 ) ;
#25532=DIRECTION ( 'NONE',  ( 1.000000000000000000, 0.000000000000000000, 0.000000000000000000 ) ) ;
#25542=DIRECTION ( 'NONE',  ( -1.000000000000000000, -0.000000000000000000, -0.000000000000000000 ) ) ;
#25551=VECTOR ( 'NONE', #46000, 1000.000000000000000 ) ;
#25553=CYLINDRICAL_SURFACE ( 'NONE', #25035, 37.49900000000000233 ) ;
#25566=DIRECTION ( 'NONE',  ( -1.000000000000000000, 0.000000000000000000, -0.000000000000000000 ) ) ;
#25579=ORIENTED_EDGE ( 'NONE', *, *, #37524, .F. ) ;
#25584=CIRCLE ( 'NONE', #4501, 15.99999999999999822 ) ;
#25589=VECTOR ( 'NONE', #15952, 1000.000000000000000 ) ;
#25590=LINE ( 'NONE', #40532, #40238 ) ;
#25596=ORIENTED_EDGE ( 'NONE', *, *, #43560, .T. ) ;
#25601=VECTOR ( 'NONE', #354, 1000.000000000000000 ) ;
#25611=DIRECTION ( 'NONE',  ( 0.000000000000000000, 0.000000000000000000, 1.000000000000000000 ) ) ;
#25625=DIRECTION ( 'NONE',  ( 0.000000000000000000, 0.000000000000000000, -1.000000000000000000 ) ) ;
#25627=EDGE_CURVE ( 'NONE', #31834, #16291, #32135, .T. ) ;
#25630=LINE ( 'NONE', #40571, #31829 ) ;
#25634=DIRECTION ( 'NONE',  ( 0.000000000000000000, -0.9781476007338070211, 0.2079116908177532363 ) ) ;
#25649=EDGE_LOOP ( 'NONE', ( #6504, #21459, #32432, #9099 ) ) ;
#25652=CARTESIAN_POINT ( 'NONE',  ( 50.00005079999999680, 2.571758278209441661E-15, -21.00000000000000000 ) ) ;
#25657=ORIENTED_EDGE ( 'NONE', *, *, #10219, .T. ) ;
#25669=CARTESIAN_POINT ( 'NONE',  ( 5.000000000000000000, -15.48615015657610705, 39.04073710021338428 ) ) ;
#25670=DIRECTION ( 'NONE',  ( -1.000000000000000000, -0.000000000000000000, -0.000000000000000000 ) ) ;
#25672=DIRECTION ( 'NONE',  ( 0.000000000000000000, -0.7431448254773954654, 0.6691306063588569053 ) ) ;
#25677=CARTESIAN_POINT ( 'NONE',  ( 0.000000000000000000, 35.92658777277525672, -10.74501242461245809 ) ) ;
#25682=AXIS2_PLACEMENT_3D ( 'NONE', #4838, #44999, #4119 ) ;
#25692=DIRECTION ( 'NONE',  ( -1.000000000000000000, 0.000000000000000000, 0.000000000000000000 ) ) ;
#25694=ADVANCED_FACE ( 'NONE', ( #33074 ), #6896, .T. ) ;
#25703=FACE_OUTER_BOUND ( 'NONE', #6421, .T. ) ;
#25711=CARTESIAN_POINT ( 'NONE',  ( 10.00000000000000000, -39.04073710021356192, 15.48615015657568250 ) ) ;
#25715=DIRECTION ( 'NONE',  ( 0.000000000000000000, 0.000000000000000000, 1.000000000000000000 ) ) ;
#25733=ORIENTED_EDGE ( 'NONE', *, *, #17838, .F. ) ;
#25736=ADVANCED_FACE ( 'NONE', ( #32372 ), #40441, .T. ) ;
#25743=EDGE_CURVE ( 'NONE', #15551, #22551, #13773, .T. ) ;
#25749=FACE_OUTER_BOUND ( 'NONE', #1599, .T. ) ;
#25757=EDGE_CURVE ( 'NONE', #12132, #4179, #6419, .T. ) ;
#25760=CARTESIAN_POINT ( 'NONE',  ( 0.000000000000000000, -35.47612816024506088, -22.48208911017539435 ) ) ;
#25764=DIRECTION ( 'NONE',  ( 0.000000000000000000, -0.9781476007338040235, -0.2079116908177671419 ) ) ;
#25771=ORIENTED_EDGE ( 'NONE', *, *, #48173, .T. ) ;
#25774=CYLINDRICAL_SURFACE ( 'NONE', #9313, 16.00000000000000000 ) ;
#25783=VERTEX_POINT ( 'NONE', #22552 ) ;
#25804=DIRECTION ( 'NONE',  ( 0.000000000000000000, 0.000000000000000000, 1.000000000000000000 ) ) ;
#25817=AXIS2_PLACEMENT_3D ( 'NONE', #39155, #31347, #5624 ) ;
#25843=DIRECTION ( 'NONE',  ( -1.000000000000000000, 0.000000000000000000, 0.000000000000000000 ) ) ;
#25846=EDGE_CURVE ( 'NONE', #21200, #10349, #3719, .T. ) ;
#25855=CARTESIAN_POINT ( 'NONE',  ( 10.00000000000000000, 0.6853352020795618893, -37.58145647212453611 ) ) ;
#25876=FACE_OUTER_BOUND ( 'NONE', #4545, .T. ) ;
#25907=EDGE_CURVE ( 'NONE', #45279, #32185, #3953, .T. ) ;
#25908=EDGE_CURVE ( 'NONE', #7802, #39726, #28670, .T. ) ;
#25911=CARTESIAN_POINT ( 'NONE',  ( -10.00000000000000000, 0.000000000000000000, 0.000000000000000000 ) ) ;
#25927=DIRECTION ( 'NONE',  ( 0.000000000000000000, 0.000000000000000000, 1.000000000000000000 ) ) ;
#25930=AXIS2_PLACEMENT_3D ( 'NONE', #28911, #36500, #32363 ) ;
#25932=CARTESIAN_POINT ( 'NONE',  ( 10.00000000000000000, 0.000000000000000000, 0.000000000000000000 ) ) ;
#25934=VECTOR ( 'NONE', #10155, 1000.000000000000000 ) ;
#25936=ORIENTED_EDGE ( 'NONE', *, *, #26427, .F. ) ;
#25938=VECTOR ( 'NONE', #45007, 1000.000000000000000 ) ;
#25947=ORIENTED_EDGE ( 'NONE', *, *, #34922, .F. ) ;
#25950=EDGE_CURVE ( 'NONE', #35793, #37523, #1251, .T. ) ;
#25953=VERTEX_POINT ( 'NONE', #35737 ) ;
#25965=ADVANCED_FACE ( 'NONE', ( #38707 ), #17128, .F. ) ;
#25967=DIRECTION ( 'NONE',  ( -1.000000000000000000, -0.000000000000000000, 0.000000000000000000 ) ) ;
#25972=ORIENTED_EDGE ( 'NONE', *, *, #14863, .F. ) ;
#25973=VERTEX_POINT ( 'NONE', #20084 ) ;
#25976=ORIENTED_EDGE ( 'NONE', *, *, #10501, .F. ) ;
#25977=AXIS2_PLACEMENT_3D ( 'NONE', #29736, #48102, #14586 ) ;
#25992=DIRECTION ( 'NONE',  ( 0.000000000000000000, 0.9510565162951523099, 0.3090169943749517811 ) ) ;
#25993=CARTESIAN_POINT ( 'NONE',  ( 10.00000000000000000, 27.13269053701132094, -25.88420570971372570 ) ) ;
#25994=DIRECTION ( 'NONE',  ( 0.000000000000000000, 0.000000000000000000, 1.000000000000000000 ) ) ;
#25997=ORIENTED_EDGE ( 'NONE', *, *, #3304, .T. ) ;
#25998=CARTESIAN_POINT ( 'NONE',  ( 4.999999999999999112, 9.188173127307294408, 40.98264845739752360 ) ) ;
#26001=AXIS2_PLACEMENT_3D ( 'NONE', #18021, #6302, #25372 ) ;
#26017=CARTESIAN_POINT ( 'NONE',  ( 0.000000000000000000, 35.38097989696512968, 12.42422080174651100 ) ) ;
#26019=ORIENTED_EDGE ( 'NONE', *, *, #25150, .T. ) ;
#26034=EDGE_CURVE ( 'NONE', #33558, #12152, #3745, .T. ) ;
#26039=VECTOR ( 'NONE', #13889, 999.9999999999998863 ) ;
#26043=DIRECTION ( 'NONE',  ( -1.000000000000000000, -0.000000000000000000, -0.000000000000000000 ) ) ;
#26056=FACE_OUTER_BOUND ( 'NONE', #27175, .T. ) ;
#26057=CYLINDRICAL_SURFACE ( 'NONE', #2622, 42.00000000000000000 ) ;
#26069=VERTEX_POINT ( 'NONE', #13228 ) ;
#26075=EDGE_CURVE ( 'NONE', #43777, #13859, #3336, .T. ) ;
#26085=VERTEX_POINT ( 'NONE', #40335 ) ;
#26098=FACE_OUTER_BOUND ( 'NONE', #44647, .T. ) ;
#26099=CARTESIAN_POINT ( 'NONE',  ( 10.00000000000000000, 0.000000000000000000, 0.000000000000000000 ) ) ;
#26111=AXIS2_PLACEMENT_3D ( 'NONE', #40671, #21341, #32379 ) ;
#26114=VERTEX_POINT ( 'NONE', #7515 ) ;
#26116=AXIS2_PLACEMENT_3D ( 'NONE', #12389, #23627, #16535 ) ;
#26121=CARTESIAN_POINT ( 'NONE',  ( 0.000000000000000000, -37.22597642581153821, -5.202137450156795850 ) ) ;
#26128=DIRECTION ( 'NONE',  ( -1.000000000000000000, 0.000000000000000000, -0.000000000000000000 ) ) ;
#26133=DIRECTION ( 'NONE',  ( 0.000000000000000000, -0.2079116908177532086, -0.9781476007338069101 ) ) ;
#26141=EDGE_LOOP ( 'NONE', ( #14207, #1983, #16819, #30635 ) ) ;
#26143=AXIS2_PLACEMENT_3D ( 'NONE', #15229, #41407, #30157 ) ;
#26144=EDGE_CURVE ( 'NONE', #38104, #41802, #33920, .T. ) ;
#26147=ORIENTED_EDGE ( 'NONE', *, *, #31177, .F. ) ;
#26152=DIRECTION ( 'NONE',  ( 0.000000000000000000, 0.000000000000000000, -1.000000000000000000 ) ) ;
#26153=VECTOR ( 'NONE', #9460, 1000.000000000000000 ) ;
#26162=DIRECTION ( 'NONE',  ( -1.000000000000000000, 0.000000000000000000, 0.000000000000000000 ) ) ;
#26165=VERTEX_POINT ( 'NONE', #44465 ) ;
#26173=ORIENTED_EDGE ( 'NONE', *, *, #42934, .F. ) ;
#26181=AXIS2_PLACEMENT_3D ( 'NONE', #40740, #3537, #7459 ) ;
#26182=DIRECTION ( 'NONE',  ( 0.000000000000000000, 0.000000000000000000, 1.000000000000000000 ) ) ;
#26184=VECTOR ( 'NONE', #38768, 1000.000000000000000 ) ;
#26196=CARTESIAN_POINT ( 'NONE',  ( 10.00000000000000000, 0.000000000000000000, 0.000000000000000000 ) ) ;
#26202=AXIS2_PLACEMENT_3D ( 'NONE', #3196, #29877, #32816 ) ;
#26209=ORIENTED_EDGE ( 'NONE', *, *, #37862, .T. ) ;
#26211=ORIENTED_EDGE ( 'NONE', *, *, #16020, .T. ) ;
#26218=ORIENTED_EDGE ( 'NONE', *, *, #33298, .F. ) ;
#26221=ORIENTED_EDGE ( 'NONE', *, *, #6966, .F. ) ;
#26243=CARTESIAN_POINT ( 'NONE',  ( -3.000000000000000000, 14.60985201121729737, -18.46759930825687945 ) ) ;
#26246=EDGE_CURVE ( 'NONE', #14664, #3154, #22444, .T. ) ;
#26248=FACE_OUTER_BOUND ( 'NONE', #34707, .T. ) ;
#26255=CARTESIAN_POINT ( 'NONE',  ( 10.00000000000000000, -30.80686688396994910, -21.53537804866113703 ) ) ;
#26261=AXIS2_PLACEMENT_3D ( 'NONE', #37733, #41649, #4215 ) ;
#26267=ORIENTED_EDGE ( 'NONE', *, *, #36135, .T. ) ;
#26270=CIRCLE ( 'NONE', #24693, 16.00000000000000000 ) ;
#26274=AXIS2_PLACEMENT_3D ( 'NONE', #10090, #24787, #39231 ) ;
#26275=EDGE_CURVE ( 'NONE', #15797, #2768, #34638, .T. ) ;
#26293=DIRECTION ( 'NONE',  ( 0.000000000000000000, 0.7071067811865487940, -0.7071067811865462405 ) ) ;
#26302=ADVANCED_FACE ( 'NONE', ( #27557 ), #45422, .T. ) ;
#26307=AXIS2_PLACEMENT_3D ( 'NONE', #13011, #32322, #42863 ) ;
#26310=EDGE_CURVE ( 'NONE', #33751, #22836, #15571, .T. ) ;
#26316=LINE ( 'NONE', #44666, #36356 ) ;
#26324=ADVANCED_FACE ( 'NONE', ( #23631 ), #27322, .T. ) ;
#26327=VERTEX_POINT ( 'NONE', #31483 ) ;
#26330=AXIS2_PLACEMENT_3D ( 'NONE', #10699, #18738, #7006 ) ;
#26334=EDGE_LOOP ( 'NONE', ( #21654, #33947, #32520, #47459 ) ) ;
#26335=VECTOR ( 'NONE', #27394, 1000.000000000000000 ) ;
#26336=CARTESIAN_POINT ( 'NONE',  ( 0.000000000000000000, -26.08949754953044220, 27.05870788708222818 ) ) ;
#26340=CARTESIAN_POINT ( 'NONE',  ( 0.000000000000000000, 33.00180498840046539, 17.80606268964551120 ) ) ;
#26346=EDGE_LOOP ( 'NONE', ( #17735, #13288, #17575, #1581 ) ) ;
#26362=DIRECTION ( 'NONE',  ( -1.000000000000000000, 0.000000000000000000, 0.000000000000000000 ) ) ;
#26364=EDGE_CURVE ( 'NONE', #23315, #6278, #15815, .T. ) ;
#26367=LINE ( 'NONE', #7985, #15122 ) ;
#26372=DIRECTION ( 'NONE',  ( 0.000000000000000000, -0.9510565162951565288, 0.3090169943749384029 ) ) ;
#26376=EDGE_CURVE ( 'NONE', #239, #5723, #2556, .T. ) ;
#26382=ORIENTED_EDGE ( 'NONE', *, *, #26798, .T. ) ;
#26383=EDGE_LOOP ( 'NONE', ( #13570, #31176, #28746, #7590 ) ) ;
#26385=VECTOR ( 'NONE', #31025, 1000.000000000000000 ) ;
#26386=EDGE_CURVE ( 'NONE', #46514, #5548, #28357, .T. ) ;
#26393=EDGE_CURVE ( 'NONE', #40235, #26069, #31968, .T. ) ;
#26396=ORIENTED_EDGE ( 'NONE', *, *, #45885, .T. ) ;
#26404=VERTEX_POINT ( 'NONE', #6486 ) ;
#26412=LINE ( 'NONE', #41346, #36802 ) ;
#26425=CARTESIAN_POINT ( 'NONE',  ( 0.000000000000000000, 8.688484142254221609, -21.88630264137359660 ) ) ;
#26427=EDGE_CURVE ( 'NONE', #17574, #32005, #28761, .T. ) ;
#26429=CYLINDRICAL_SURFACE ( 'NONE', #45905, 16.00000000000000000 ) ;
#26434=CARTESIAN_POINT ( 'NONE',  ( 10.00000000000000000, 12.42422080174688404, -35.38097989696498047 ) ) ;
#26437=VECTOR ( 'NONE', #18746, 1000.000000000000000 ) ;
#26444=VERTEX_POINT ( 'NONE', #43686 ) ;
#26454=DIRECTION ( 'NONE',  ( 0.000000000000000000, -0.5877852522924689183, -0.8090169943749504489 ) ) ;
#26468=CARTESIAN_POINT ( 'NONE',  ( 10.00000000000000000, 37.22597642581158084, -5.202137450156524068 ) ) ;
#26476=CARTESIAN_POINT ( 'NONE',  ( 0.000000000000000000, 32.34446384429971033, 26.79245525562726371 ) ) ;
#26479=ADVANCED_FACE ( 'NONE', ( #2804 ), #25076, .T. ) ;
#26486=CARTESIAN_POINT ( 'NONE',  ( -3.000000000000000000, -22.67460108101774807, -6.353146135318215038 ) ) ;
#26490=ADVANCED_FACE ( 'NONE', ( #42737 ), #2322, .F. ) ;
#26511=ADVANCED_FACE ( 'NONE', ( #37309 ), #29714, .T. ) ;
#26523=DIRECTION ( 'NONE',  ( 1.000000000000000000, 0.000000000000000000, 0.000000000000000000 ) ) ;
#26527=ORIENTED_EDGE ( 'NONE', *, *, #32926, .F. ) ;
#26529=CARTESIAN_POINT ( 'NONE',  ( -3.000000000000000000, 5.835314593368772229, -22.81335362449846826 ) ) ;
#26532=VERTEX_POINT ( 'NONE', #33155 ) ;
#26545=DIRECTION ( 'NONE',  ( -1.000000000000000000, 0.000000000000000000, 0.000000000000000000 ) ) ;
#26548=DIRECTION ( 'NONE',  ( -1.000000000000000000, 0.000000000000000000, 0.000000000000000000 ) ) ;
#26553=LINE ( 'NONE', #7934, #2040 ) ;
#26556=CARTESIAN_POINT ( 'NONE',  ( 10.00000000000000000, -10.74501242461258244, -35.92658777277521409 ) ) ;
#26560=ORIENTED_EDGE ( 'NONE', *, *, #45150, .T. ) ;
#26565=CARTESIAN_POINT ( 'NONE',  ( 10.00000000000000000, -2.663952781846440576, 41.91543099594817789 ) ) ;
#26571=ORIENTED_EDGE ( 'NONE', *, *, #14421, .T. ) ;
#26577=CARTESIAN_POINT ( 'NONE',  ( 10.00000000000000000, 0.000000000000000000, 0.000000000000000000 ) ) ;
#26580=ORIENTED_EDGE ( 'NONE', *, *, #10558, .F. ) ;
#26585=CARTESIAN_POINT ( 'NONE',  ( 10.00000000000000000, -37.22597642581161637, 5.202137450156258502 ) ) ;
#26587=DIRECTION ( 'NONE',  ( 0.000000000000000000, -0.8910065241883627918, -0.4539904997395568520 ) ) ;
#26593=ORIENTED_EDGE ( 'NONE', *, *, #20386, .T. ) ;
#26603=CARTESIAN_POINT ( 'NONE',  ( 0.000000000000000000, 10.74501242461282757, 35.92658777277515014 ) ) ;
#26607=EDGE_CURVE ( 'NONE', #293, #10700, #15083, .T. ) ;
#26620=CYLINDRICAL_SURFACE ( 'NONE', #19457, 16.00000000000000000 ) ;
#26623=CARTESIAN_POINT ( 'NONE',  ( -3.000000000000000000, 24.81905959214261514, 9.408202855044825341 ) ) ;
#26624=ADVANCED_FACE ( 'NONE', ( #48080 ), #14566, .T. ) ;
#26625=ORIENTED_EDGE ( 'NONE', *, *, #4744, .F. ) ;
#26631=VERTEX_POINT ( 'NONE', #41704 ) ;
#26637=ADVANCED_FACE ( 'NONE', ( #41961 ), #8639, .F. ) ;
#26645=ORIENTED_EDGE ( 'NONE', *, *, #47028, .T. ) ;
#26649=CIRCLE ( 'NONE', #37619, 16.00000000000000000 ) ;
#26652=VERTEX_POINT ( 'NONE', #16253 ) ;
#26676=AXIS2_PLACEMENT_3D ( 'NONE', #21643, #28976, #29468 ) ;
#26678=DIRECTION ( 'NONE',  ( -1.000000000000000000, -0.000000000000000000, 0.000000000000000000 ) ) ;
#26680=CARTESIAN_POINT ( 'NONE',  ( -3.000000000000000000, -18.13022148937243472, -15.02647892043568767 ) ) ;
#26688=ORIENTED_EDGE ( 'NONE', *, *, #13649, .F. ) ;
#26689=EDGE_LOOP ( 'NONE', ( #40496, #1984, #26593, #22871 ) ) ;
#26707=LINE ( 'NONE', #18390, #12574 ) ;
#26719=STYLED_ITEM ( 'NONE', ( #12347 ), #2931 ) ;
#26726=CARTESIAN_POINT ( 'NONE',  ( 10.00000000000000178, 2.571758278209441661E-15, -21.00000000000000000 ) ) ;
#26732=PLANE ( 'NONE',  #35844 ) ;
#26745=VERTEX_POINT ( 'NONE', #19412 ) ;
#26746=EDGE_CURVE ( 'NONE', #12928, #41352, #7280, .T. ) ;
#26753=ORIENTED_EDGE ( 'NONE', *, *, #15985, .T. ) ;
#26760=ORIENTED_EDGE ( 'NONE', *, *, #26034, .T. ) ;
#26762=ORIENTED_EDGE ( 'NONE', *, *, #37012, .T. ) ;
#26764=CARTESIAN_POINT ( 'NONE',  ( 0.000000000000000000, -12.26510123303234501, -35.53030884539098366 ) ) ;
#26765=CARTESIAN_POINT ( 'NONE',  ( 0.000000000000000000, 6.555932627142952995, -37.01155633439051940 ) ) ;
#26791=EDGE_CURVE ( 'NONE', #16717, #38747, #20554, .T. ) ;
#26796=CARTESIAN_POINT ( 'NONE',  ( 0.000000000000000000, 0.000000000000000000, 0.000000000000000000 ) ) ;
#26798=EDGE_CURVE ( 'NONE', #38628, #19539, #5966, .T. ) ;
#26807=LINE ( 'NONE', #38076, #20662 ) ;
#26809=CARTESIAN_POINT ( 'NONE',  ( 0.000000000000000000, 8.688484142253939169, 21.88630264137371029 ) ) ;
#26811=AXIS2_PLACEMENT_3D ( 'NONE', #35697, #46952, #36161 ) ;
#26813=VERTEX_POINT ( 'NONE', #35807 ) ;
#26818=ORIENTED_EDGE ( 'NONE', *, *, #24883, .F. ) ;
#26824=CARTESIAN_POINT ( 'NONE',  ( 10.00000000000000000, -22.64427369931148348, -30.00120703465229965 ) ) ;
#26834=CARTESIAN_POINT ( 'NONE',  ( 10.00000000000000000, -37.58145647212455032, 16.68533520207890319 ) ) ;
#26836=EDGE_LOOP ( 'NONE', ( #29654, #19489, #43518, #32171 ) ) ;
#26837=CARTESIAN_POINT ( 'NONE',  ( 10.00000000000000000, 37.01155633439059756, 6.555932627142549762 ) ) ;
#26848=VECTOR ( 'NONE', #9970, 1000.000000000000000 ) ;
#26856=CARTESIAN_POINT ( 'NONE',  ( 0.000000000000000000, 36.13751322684419165, 21.40280677340384585 ) ) ;
#26857=ORIENTED_EDGE ( 'NONE', *, *, #4576, .F. ) ;
#26861=EDGE_CURVE ( 'NONE', #21976, #33652, #29964, .T. ) ;
#26862=AXIS2_PLACEMENT_3D ( 'NONE', #22824, #4237, #19148 ) ;
#26863=ORIENTED_EDGE ( 'NONE', *, *, #18522, .F. ) ;
#26867=CIRCLE ( 'NONE', #22946, 37.49900000000000944 ) ;
#26869=EDGE_CURVE ( 'NONE', #26327, #30863, #42919, .T. ) ;
#26887=AXIS2_PLACEMENT_3D ( 'NONE', #36812, #26043, #22853 ) ;
#26891=CARTESIAN_POINT ( 'NONE',  ( -3.000000000000000000, 18.84667830672579925, 18.68964196561269020 ) ) ;
#26894=FACE_OUTER_BOUND ( 'NONE', #21689, .T. ) ;
#26905=CARTESIAN_POINT ( 'NONE',  ( -3.000000000000000000, -22.67460108101783334, 6.353146135317912169 ) ) ;
#26910=DIRECTION ( 'NONE',  ( 0.000000000000000000, 0.000000000000000000, -1.000000000000000000 ) ) ;
#26914=CARTESIAN_POINT ( 'NONE',  ( 0.000000000000000000, 21.32104025579114648, 30.84782396557224970 ) ) ;
#26917=DIRECTION ( 'NONE',  ( 1.000000000000000000, -0.000000000000000000, 0.000000000000000000 ) ) ;
#26928=DIRECTION ( 'NONE',  ( -1.000000000000000000, 0.000000000000000000, 0.000000000000000000 ) ) ;
#26933=AXIS2_PLACEMENT_3D ( 'NONE', #6384, #6861, #32787 ) ;
#26941=ORIENTED_EDGE ( 'NONE', *, *, #23488, .T. ) ;
#26950=EDGE_LOOP ( 'NONE', ( #11690, #13286, #40649, #3840 ) ) ;
#26953=VERTEX_POINT ( 'NONE', #22066 ) ;
#26956=DIRECTION ( 'NONE',  ( 0.000000000000000000, 0.000000000000000000, -1.000000000000000000 ) ) ;
#26960=DIRECTION ( 'NONE',  ( -1.000000000000000000, 0.000000000000000000, -0.000000000000000000 ) ) ;
#26975=AXIS2_PLACEMENT_3D ( 'NONE', #21778, #36703, #4411 ) ;
#26980=ORIENTED_EDGE ( 'NONE', *, *, #46708, .F. ) ;
#26982=CIRCLE ( 'NONE', #1963, 42.00000000000000000 ) ;
#26983=CARTESIAN_POINT ( 'NONE',  ( -3.000000000000000000, -18.13022148937243472, -15.02647892043568767 ) ) ;
#27000=EDGE_CURVE ( 'NONE', #46255, #1961, #32611, .T. ) ;
#27008=EDGE_CURVE ( 'NONE', #4028, #20089, #23416, .T. ) ;
#27009=AXIS2_PLACEMENT_3D ( 'NONE', #8687, #35366, #1851 ) ;
#27010=AXIS2_PLACEMENT_3D ( 'NONE', #29351, #21523, #22250 ) ;
#27013=DIRECTION ( 'NONE',  ( 1.000000000000000000, 0.000000000000000000, -0.000000000000000000 ) ) ;
#27018=DIRECTION ( 'NONE',  ( 0.000000000000000000, -0.9510565162951565288, 0.3090169943749382364 ) ) ;
#27024=AXIS2_PLACEMENT_3D ( 'NONE', #38165, #1942, #15892 ) ;
#27025=DIRECTION ( 'NONE',  ( -1.000000000000000000, -0.000000000000000000, -0.000000000000000000 ) ) ;
#27027=ORIENTED_EDGE ( 'NONE', *, *, #18933, .F. ) ;
#27028=CARTESIAN_POINT ( 'NONE',  ( 0.000000000000000000, 36.13751322684449008, -21.40280677340332716 ) ) ;
#27035=CARTESIAN_POINT ( 'NONE',  ( 10.00000000000000000, 0.000000000000000000, 0.000000000000000000 ) ) ;
#27042=ORIENTED_EDGE ( 'NONE', *, *, #12447, .T. ) ;
#27045=CARTESIAN_POINT ( 'NONE',  ( 0.000000000000000000, 35.53030884539084866, 12.26510123303271982 ) ) ;
#27046=ORIENTED_EDGE ( 'NONE', *, *, #24883, .T. ) ;
#27060=CARTESIAN_POINT ( 'NONE',  ( 0.000000000000000000, 38.55633173627010279, 16.65560815589424593 ) ) ;
#27068=ORIENTED_EDGE ( 'NONE', *, *, #2215, .F. ) ;
#27077=EDGE_CURVE ( 'NONE', #1459, #29919, #757, .T. ) ;
#27079=CARTESIAN_POINT ( 'NONE',  ( 0.000000000000000000, 20.85821328998741109, 10.92862929874522315 ) ) ;
#27080=CARTESIAN_POINT ( 'NONE',  ( 10.00000000000000000, 35.38097989696528600, -12.42422080174602605 ) ) ;
#27083=DIRECTION ( 'NONE',  ( 0.000000000000000000, 0.000000000000000000, 1.000000000000000000 ) ) ;
#27102=AXIS2_PLACEMENT_3D ( 'NONE', #421, #33465, #34186 ) ;
#27121=DIRECTION ( 'NONE',  ( 0.000000000000000000, 0.5877852522924797984, -0.8090169943749426773 ) ) ;
#27130=ORIENTED_EDGE ( 'NONE', *, *, #37622, .F. ) ;
#27158=VECTOR ( 'NONE', #18149, 999.9999999999998863 ) ;
#27161=CARTESIAN_POINT ( 'NONE',  ( 0.000000000000000000, -19.89357724625003598, 12.59942793731059574 ) ) ;
#27175=EDGE_LOOP ( 'NONE', ( #32314, #41754, #26580, #961 ) ) ;
#27180=EDGE_CURVE ( 'NONE', #15804, #390, #30887, .T. ) ;
#27181=VECTOR ( 'NONE', #30893, 1000.000000000000114 ) ;
#27184=EDGE_LOOP ( 'NONE', ( #35890, #39445, #20747, #6990 ) ) ;
#27191=VERTEX_POINT ( 'NONE', #23761 ) ;
#27221=CARTESIAN_POINT ( 'NONE',  ( 0.000000000000000000, 37.22597642581158084, 10.79786254984347593 ) ) ;
#27227=DIRECTION ( 'NONE',  ( 1.000000000000000000, -0.000000000000000000, -0.000000000000000000 ) ) ;
#27231=AXIS2_PLACEMENT_3D ( 'NONE', #7253, #25843, #43977 ) ;
#27234=ORIENTED_EDGE ( 'NONE', *, *, #46555, .F. ) ;
#27236=ORIENTED_EDGE ( 'NONE', *, *, #23791, .T. ) ;
#27248=DIRECTION ( 'NONE',  ( -1.000000000000000000, 0.000000000000000000, 0.000000000000000000 ) ) ;
#27250=EDGE_CURVE ( 'NONE', #23892, #24690, #24488, .T. ) ;
#27252=EDGE_LOOP ( 'NONE', ( #29826, #10267, #30092, #25107 ) ) ;
#27259=ORIENTED_EDGE ( 'NONE', *, *, #19332, .F. ) ;
#27263=ORIENTED_EDGE ( 'NONE', *, *, #16027, .T. ) ;
#27264=LINE ( 'NONE', #16482, #46419 ) ;
#27267=EDGE_CURVE ( 'NONE', #26813, #34977, #774, .T. ) ;
#27269=DIRECTION ( 'NONE',  ( 0.000000000000000000, 0.000000000000000000, 1.000000000000000000 ) ) ;
#27270=DIRECTION ( 'NONE',  ( 0.000000000000000000, 0.8090169943749445647, 0.5877852522924771339 ) ) ;
#27273=LINE ( 'NONE', #31685, #904 ) ;
#27276=DIRECTION ( 'NONE',  ( 0.000000000000000000, 0.000000000000000000, 1.000000000000000000 ) ) ;
#27278=ADVANCED_FACE ( 'NONE', ( #24738 ), #6135, .T. ) ;
#27286=CIRCLE ( 'NONE', #7737, 42.00000000000000000 ) ;
#27288=DIRECTION ( 'NONE',  ( -1.000000000000000000, -0.000000000000000000, 0.000000000000000000 ) ) ;
#27289=ORIENTED_EDGE ( 'NONE', *, *, #47611, .T. ) ;
#27297=ADVANCED_FACE ( 'NONE', ( #5179 ), #1500, .T. ) ;
#27299=CARTESIAN_POINT ( 'NONE',  ( 10.00000000000000000, 25.88420570971400991, 27.13269053701105449 ) ) ;
#27300=ORIENTED_EDGE ( 'NONE', *, *, #46637, .T. ) ;
#27312=CARTESIAN_POINT ( 'NONE',  ( 0.000000000000000000, 0.000000000000000000, 0.000000000000000000 ) ) ;
#27322=CYLINDRICAL_SURFACE ( 'NONE', #18293, 16.00000000000000000 ) ;
#27324=FACE_OUTER_BOUND ( 'NONE', #3750, .T. ) ;
#27330=CARTESIAN_POINT ( 'NONE',  ( 10.00000000000000000, -0.6853352020787742971, -37.58145647212455032 ) ) ;
#27331=PLANE ( 'NONE',  #22783 ) ;
#27333=DIRECTION ( 'NONE',  ( 0.000000000000000000, 0.5877852522924696954, 0.8090169943749498938 ) ) ;
#27337=VERTEX_POINT ( 'NONE', #6375 ) ;
#27347=ORIENTED_EDGE ( 'NONE', *, *, #1670, .F. ) ;
#27357=CARTESIAN_POINT ( 'NONE',  ( -3.000000000000000000, 14.60985201121729737, -18.46759930825687945 ) ) ;
#27362=EDGE_LOOP ( 'NONE', ( #14571, #10067, #7056, #15438 ) ) ;
#27369=ORIENTED_EDGE ( 'NONE', *, *, #33873, .F. ) ;
#27370=EDGE_CURVE ( 'NONE', #1330, #45913, #25192, .T. ) ;
#27371=DIRECTION ( 'NONE',  ( 1.000000000000000000, -0.000000000000000000, 0.000000000000000000 ) ) ;
#27372=DIRECTION ( 'NONE',  ( -1.000000000000000000, 0.000000000000000000, 0.000000000000000000 ) ) ;
#27375=ORIENTED_EDGE ( 'NONE', *, *, #7045, .T. ) ;
#27376=DIRECTION ( 'NONE',  ( -1.000000000000000000, -0.000000000000000000, 0.000000000000000000 ) ) ;
#27380=CIRCLE ( 'NONE', #35954, 16.00000000000000000 ) ;
#27382=VERTEX_POINT ( 'NONE', #43577 ) ;
#27391=EDGE_LOOP ( 'NONE', ( #21126, #46569, #22318, #36508 ) ) ;
#27392=DIRECTION ( 'NONE',  ( 1.000000000000000000, 0.000000000000000000, 0.000000000000000000 ) ) ;
#27394=DIRECTION ( 'NONE',  ( -1.000000000000000000, 0.000000000000000000, 0.000000000000000000 ) ) ;
#27397=CARTESIAN_POINT ( 'NONE',  ( 0.000000000000000000, 3.925862922256769583, -41.81611651403857621 ) ) ;
#27405=ADVANCED_FACE ( 'NONE', ( #40150 ), #10524, .T. ) ;
#27413=CARTESIAN_POINT ( 'NONE',  ( 10.00000000000000000, -30.80686688397025108, 21.53537804866070715 ) ) ;
#27416=ORIENTED_EDGE ( 'NONE', *, *, #44489, .F. ) ;
#27417=ORIENTED_EDGE ( 'NONE', *, *, #35601, .T. ) ;
#27430=CARTESIAN_POINT ( 'NONE',  ( 5.000000000000000000, -26.79245525562738095, 32.34446384429961796 ) ) ;
#27449=DIRECTION ( 'NONE',  ( 0.000000000000000000, -0.5877852522924624790, -0.8090169943749553338 ) ) ;
#27457=CARTESIAN_POINT ( 'NONE',  ( 10.00000000000000000, 35.53030884539084866, 12.26510123303271982 ) ) ;
#27460=DIRECTION ( 'NONE',  ( 0.000000000000000000, 0.9510565162951503115, 0.3090169943749573878 ) ) ;
#27469=EDGE_LOOP ( 'NONE', ( #28299, #15199, #12394, #41907 ) ) ;
#27474=EDGE_CURVE ( 'NONE', #10349, #26114, #22508, .T. ) ;
#27477=ORIENTED_EDGE ( 'NONE', *, *, #27928, .F. ) ;
#27480=AXIS2_PLACEMENT_3D ( 'NONE', #26243, #10828, #44832 ) ;
#27484=DIRECTION ( 'NONE',  ( -0.000000000000000000, -0.7431448254773870277, -0.6691306063588662312 ) ) ;
#27488=VECTOR ( 'NONE', #12923, 1000.000000000000000 ) ;
#27494=CARTESIAN_POINT ( 'NONE',  ( 0.000000000000000000, 0.000000000000000000, 0.000000000000000000 ) ) ;
#27498=ORIENTED_EDGE ( 'NONE', *, *, #21099, .F. ) ;
#27499=CARTESIAN_POINT ( 'NONE',  ( 10.00000000000000000, -22.74946021919110706, -29.81001611431033282 ) ) ;
#27505=CARTESIAN_POINT ( 'NONE',  ( 0.000000000000000000, -30.84782396557233142, 21.32104025579104345 ) ) ;
#27511=DIRECTION ( 'NONE',  ( 0.000000000000000000, 0.000000000000000000, 1.000000000000000000 ) ) ;
#27518=LINE ( 'NONE', #43421, #41010 ) ;
#27521=CIRCLE ( 'NONE', #29077, 37.49900000000000944 ) ;
#27526=VERTEX_POINT ( 'NONE', #703 ) ;
#27529=ORIENTED_EDGE ( 'NONE', *, *, #14762, .F. ) ;
#27530=VERTEX_POINT ( 'NONE', #19064 ) ;
#27547=EDGE_LOOP ( 'NONE', ( #30127, #5569, #22541, #32881 ) ) ;
#27557=FACE_OUTER_BOUND ( 'NONE', #4544, .T. ) ;
#27560=DIRECTION ( 'NONE',  ( -1.000000000000000000, 0.000000000000000000, 0.000000000000000000 ) ) ;
#27574=ORIENTED_EDGE ( 'NONE', *, *, #25461, .F. ) ;
#27576=VECTOR ( 'NONE', #14677, 1000.000000000000000 ) ;
#27591=VECTOR ( 'NONE', #31432, 1000.000000000000000 ) ;
#27606=CARTESIAN_POINT ( 'NONE',  ( 0.000000000000000000, 0.000000000000000000, 0.000000000000000000 ) ) ;
#27610=DIRECTION ( 'NONE',  ( 0.000000000000000000, -0.8090169943749531134, 0.5877852522924653655 ) ) ;
#27621=VECTOR ( 'NONE', #15569, 1000.000000000000114 ) ;
#27631=CARTESIAN_POINT ( 'NONE',  ( 5.000000000000000000, -32.34446384429989507, 26.79245525562703278 ) ) ;
#27633=CIRCLE ( 'NONE', #6517, 42.00000000000000000 ) ;
#27650=EDGE_LOOP ( 'NONE', ( #10689, #10758, #46690, #33183 ) ) ;
#27654=AXIS2_PLACEMENT_3D ( 'NONE', #20582, #16926, #35277 ) ;
#27658=ORIENTED_EDGE ( 'NONE', *, *, #6102, .F. ) ;
#27674=VERTEX_POINT ( 'NONE', #3811 ) ;
#27687=ADVANCED_FACE ( 'NONE', ( #40774 ), #21920, .T. ) ;
#27689=DIRECTION ( 'NONE',  ( 0.000000000000000000, 0.000000000000000000, 1.000000000000000000 ) ) ;
#27698=AXIS2_PLACEMENT_3D ( 'NONE', #21176, #16555, #9681 ) ;
#27709=CARTESIAN_POINT ( 'NONE',  ( 10.00000000000000000, 0.000000000000000000, 0.000000000000000000 ) ) ;
#27710=AXIS2_PLACEMENT_3D ( 'NONE', #6134, #14190, #36694 ) ;
#27712=EDGE_CURVE ( 'NONE', #33012, #962, #29739, .T. ) ;
#27719=ORIENTED_EDGE ( 'NONE', *, *, #23530, .T. ) ;
#27747=DIRECTION ( 'NONE',  ( 0.000000000000000000, 0.000000000000000000, -1.000000000000000000 ) ) ;
#27748=AXIS2_PLACEMENT_3D ( 'NONE', #9391, #13810, #20405 ) ;
#27751=DIRECTION ( 'NONE',  ( 1.000000000000000000, 0.000000000000000000, 0.000000000000000000 ) ) ;
#27754=DIRECTION ( 'NONE',  ( -1.000000000000000000, -0.000000000000000000, 0.000000000000000000 ) ) ;
#27758=AXIS2_PLACEMENT_3D ( 'NONE', #28990, #29245, #43464 ) ;
#27762=DIRECTION ( 'NONE',  ( 1.000000000000000000, 0.000000000000000000, 0.000000000000000000 ) ) ;
#27768=EDGE_CURVE ( 'NONE', #47099, #28193, #4722, .T. ) ;
#27771=AXIS2_PLACEMENT_3D ( 'NONE', #16600, #46476, #1933 ) ;
#27772=DIRECTION ( 'NONE',  ( 0.000000000000000000, -0.4067366430758009854, 0.9135454576426004225 ) ) ;
#27774=DIRECTION ( 'NONE',  ( 0.000000000000000000, 0.000000000000000000, 1.000000000000000000 ) ) ;
#27778=ADVANCED_FACE ( 'NONE', ( #852 ), #22648, .T. ) ;
#27779=VECTOR ( 'NONE', #12854, 999.9999999999998863 ) ;
#27785=VECTOR ( 'NONE', #28379, 1000.000000000000000 ) ;
#27787=DIRECTION ( 'NONE',  ( 1.000000000000000000, 0.000000000000000000, 0.000000000000000000 ) ) ;
#27788=DIRECTION ( 'NONE',  ( -1.000000000000000000, 0.000000000000000000, 0.000000000000000000 ) ) ;
#27796=DIRECTION ( 'NONE',  ( 1.000000000000000000, -0.000000000000000000, -0.000000000000000000 ) ) ;
#27799=CIRCLE ( 'NONE', #23871, 37.49900000000000233 ) ;
#27800=VERTEX_POINT ( 'NONE', #37585 ) ;
#27801=EDGE_CURVE ( 'NONE', #15279, #13859, #19221, .T. ) ;
#27804=CYLINDRICAL_SURFACE ( 'NONE', #39627, 37.49900000000000233 ) ;
#27806=CARTESIAN_POINT ( 'NONE',  ( 0.000000000000000000, -0.9646360437375307573, 23.52805723605590060 ) ) ;
#27816=CARTESIAN_POINT ( 'NONE',  ( 0.000000000000000000, 24.81905959214261514, 9.408202855044825341 ) ) ;
#27817=CARTESIAN_POINT ( 'NONE',  ( 10.00000000000000000, -22.74946021919110706, -29.81001611431033282 ) ) ;
#27819=LINE ( 'NONE', #5526, #34784 ) ;
#27824=AXIS2_PLACEMENT_3D ( 'NONE', #17018, #6024, #2328 ) ;
#27828=ADVANCED_FACE ( 'NONE', ( #45906 ), #4781, .T. ) ;
#27830=LINE ( 'NONE', #16553, #39729 ) ;
#27834=EDGE_CURVE ( 'NONE', #18858, #7802, #23139, .T. ) ;
#27841=DIRECTION ( 'NONE',  ( -1.000000000000000000, 0.000000000000000000, 0.000000000000000000 ) ) ;
#27851=ORIENTED_EDGE ( 'NONE', *, *, #14886, .F. ) ;
#27852=VECTOR ( 'NONE', #23495, 1000.000000000000000 ) ;
#27865=DIRECTION ( 'NONE',  ( 0.000000000000000000, 0.1564344650402312298, -0.9876883405951375483 ) ) ;
#27870=VERTEX_POINT ( 'NONE', #30002 ) ;
#27877=EDGE_CURVE ( 'NONE', #45643, #2188, #34408, .T. ) ;
#27880=EDGE_LOOP ( 'NONE', ( #47156, #6580, #35249, #33561 ) ) ;
#27887=VERTEX_POINT ( 'NONE', #1593 ) ;
#27889=DIRECTION ( 'NONE',  ( 0.000000000000000000, -0.4067366430758009854, 0.9135454576426004225 ) ) ;
#27895=CARTESIAN_POINT ( 'NONE',  ( 0.000000000000000000, -21.53537804866103045, 30.80686688397002371 ) ) ;
#27896=DIRECTION ( 'NONE',  ( 0.000000000000000000, 0.8090169943749486725, -0.5877852522924713607 ) ) ;
#27904=ORIENTED_EDGE ( 'NONE', *, *, #47429, .T. ) ;
#27907=CARTESIAN_POINT ( 'NONE',  ( 0.000000000000000000, 16.23288003029543347, -33.80338159004267595 ) ) ;
#27908=AXIS2_PLACEMENT_3D ( 'NONE', #26121, #10222, #7530 ) ;
#27909=DIRECTION ( 'NONE',  ( -0.000000000000000000, -0.2079116908177653378, 0.9781476007338044676 ) ) ;
#27911=AXIS2_PLACEMENT_3D ( 'NONE', #29792, #15368, #44720 ) ;
#27928=EDGE_CURVE ( 'NONE', #25303, #39296, #5494, .T. ) ;
#27929=CARTESIAN_POINT ( 'NONE',  ( 10.00000000000000000, 37.01155633439068282, -6.555932627142014191 ) ) ;
#27947=CIRCLE ( 'NONE', #43545, 37.49900000000000233 ) ;
#27949=DIRECTION ( 'NONE',  ( -1.000000000000000000, 0.000000000000000000, -0.000000000000000000 ) ) ;
#27956=ORIENTED_EDGE ( 'NONE', *, *, #23706, .F. ) ;
#27958=CARTESIAN_POINT ( 'NONE',  ( 10.00000000000000000, 10.74501242461333028, -35.92658777277499382 ) ) ;
#27959=CARTESIAN_POINT ( 'NONE',  ( 0.000000000000000000, -17.67226234102849958, 33.17418723428301774 ) ) ;
#27961=CARTESIAN_POINT ( 'NONE',  ( 0.000000000000000000, -36.88895765772628010, -6.736453364083947015 ) ) ;
#27962=VERTEX_POINT ( 'NONE', #23864 ) ;
#27964=CARTESIAN_POINT ( 'NONE',  ( 0.000000000000000000, -0.9646360437375307573, 23.52805723605590060 ) ) ;
#27966=DIRECTION ( 'NONE',  ( -1.000000000000000000, 0.000000000000000000, 0.000000000000000000 ) ) ;
#27967=EDGE_LOOP ( 'NONE', ( #17673, #14663, #28858, #4433 ) ) ;
#27973=ADVANCED_FACE ( 'NONE', ( #38810 ), #39271, .F. ) ;
#27979=CARTESIAN_POINT ( 'NONE',  ( 0.000000000000000000, 37.48860685352291000, 0.8828120875901893649 ) ) ;
#27985=ORIENTED_EDGE ( 'NONE', *, *, #39829, .F. ) ;
#27986=VERTEX_POINT ( 'NONE', #28257 ) ;
#27988=FACE_OUTER_BOUND ( 'NONE', #13096, .T. ) ;
#27996=DIRECTION ( 'NONE',  ( -1.000000000000000000, -0.000000000000000000, -0.000000000000000000 ) ) ;
#28006=ORIENTED_EDGE ( 'NONE', *, *, #2159, .F. ) ;
#28017=AXIS2_PLACEMENT_3D ( 'NONE', #42295, #1661, #16839 ) ;
#28020=ORIENTED_EDGE ( 'NONE', *, *, #41350, .T. ) ;
#28023=CARTESIAN_POINT ( 'NONE',  ( 0.000000000000000000, 23.50000000000000000, -1.500000000000001332 ) ) ;
#28040=FACE_BOUND ( 'NONE', #326, .T. ) ;
#28064=ORIENTED_EDGE ( 'NONE', *, *, #788, .T. ) ;
#28068=VERTEX_POINT ( 'NONE', #11381 ) ;
#28076=LINE ( 'NONE', #43009, #26153 ) ;
#28081=EDGE_LOOP ( 'NONE', ( #28430, #23135, #46904, #5971 ) ) ;
#28082=EDGE_CURVE ( 'NONE', #43027, #33430, #11017, .T. ) ;
#28087=DIRECTION ( 'NONE',  ( 0.000000000000000000, 0.7071067811865439090, 0.7071067811865512365 ) ) ;
#28090=CARTESIAN_POINT ( 'NONE',  ( 4.999999999999999112, 38.55633173627034438, -16.65560815589369881 ) ) ;
#28097=VERTEX_POINT ( 'NONE', #14567 ) ;
#28102=LINE ( 'NONE', #9732, #35057 ) ;
#28105=FACE_OUTER_BOUND ( 'NONE', #34493, .T. ) ;
#28107=CARTESIAN_POINT ( 'NONE',  ( 10.00000000000000000, 33.17418723428307459, 17.67226234102837878 ) ) ;
#28108=FACE_OUTER_BOUND ( 'NONE', #18663, .T. ) ;
#28112=CARTESIAN_POINT ( 'NONE',  ( 10.00000000000000000, -36.13751322684404244, -21.40280677340410165 ) ) ;
#28133=EDGE_CURVE ( 'NONE', #23166, #2611, #29960, .T. ) ;
#28134=AXIS2_PLACEMENT_3D ( 'NONE', #24244, #24017, #38952 ) ;
#28135=CARTESIAN_POINT ( 'NONE',  ( -3.000000000000000000, 6.762365576493643893, -25.66652317338391853 ) ) ;
#28142=CIRCLE ( 'NONE', #46909, 37.49900000000000944 ) ;
#28143=CARTESIAN_POINT ( 'NONE',  ( 10.00000000000000000, 37.16516213103285082, -4.992566952384588141 ) ) ;
#28150=CARTESIAN_POINT ( 'NONE',  ( 4.999999999999999112, -2.663952781845850826, -41.91543099594819921 ) ) ;
#28155=DIRECTION ( 'NONE',  ( 1.000000000000000000, -0.000000000000000000, -0.000000000000000000 ) ) ;
#28159=DIRECTION ( 'NONE',  ( 0.000000000000000000, 0.000000000000000000, -1.000000000000000000 ) ) ;
#28160=DIRECTION ( 'NONE',  ( 0.000000000000000000, -0.7431448254773862505, -0.6691306063588671194 ) ) ;
#28162=DIRECTION ( 'NONE',  ( -1.000000000000000000, 0.000000000000000000, 0.000000000000000000 ) ) ;
#28174=VECTOR ( 'NONE', #12200, 1000.000000000000000 ) ;
#28193=VERTEX_POINT ( 'NONE', #39004 ) ;
#28215=VERTEX_POINT ( 'NONE', #5239 ) ;
#28216=CARTESIAN_POINT ( 'NONE',  ( 0.000000000000000000, 26.08949754953062694, -27.05870788708203989 ) ) ;
#28220=AXIS2_PLACEMENT_3D ( 'NONE', #47244, #39903, #28159 ) ;
#28225=DIRECTION ( 'NONE',  ( 0.000000000000000000, 0.5877852522924797984, -0.8090169943749426773 ) ) ;
#28229=CARTESIAN_POINT ( 'NONE',  ( 10.00000000000000000, 33.80338159004283938, 16.23288003029508886 ) ) ;
#28230=CARTESIAN_POINT ( 'NONE',  ( 10.00000000000000000, 36.13751322684449718, -21.40280677340333071 ) ) ;
#28232=ORIENTED_EDGE ( 'NONE', *, *, #26427, .T. ) ;
#28237=EDGE_CURVE ( 'NONE', #4382, #40081, #21174, .T. ) ;
#28239=ORIENTED_EDGE ( 'NONE', *, *, #3992, .F. ) ;
#28253=CARTESIAN_POINT ( 'NONE',  ( 0.000000000000000000, 0.000000000000000000, 0.000000000000000000 ) ) ;
#28254=DIRECTION ( 'NONE',  ( 0.000000000000000000, -0.1045284632676429099, -0.9945218953682744001 ) ) ;
#28257=CARTESIAN_POINT ( 'NONE',  ( 0.000000000000000000, -25.60904388321925396, 6.976881207771170601 ) ) ;
#28264=CARTESIAN_POINT ( 'NONE',  ( 10.00000000000000000, -16.65560815589439159, 38.55633173627004595 ) ) ;
#28270=CARTESIAN_POINT ( 'NONE',  ( 4.999999999999999112, 16.65560815589411092, 38.55633173627015253 ) ) ;
#28272=DIRECTION ( 'NONE',  ( 0.000000000000000000, 0.9876883405951372152, 0.1564344650402346160 ) ) ;
#28282=CARTESIAN_POINT ( 'NONE',  ( 10.00000000000000000, 0.000000000000000000, 0.000000000000000000 ) ) ;
#28291=CIRCLE ( 'NONE', #34534, 16.00000000000000355 ) ;
#28299=ORIENTED_EDGE ( 'NONE', *, *, #30077, .T. ) ;
#28308=CIRCLE ( 'NONE', #34547, 16.00000000000000000 ) ;
#28309=CARTESIAN_POINT ( 'NONE',  ( -10.00000000000000000, 0.000000000000000000, 0.000000000000000000 ) ) ;
#28315=DIRECTION ( 'NONE',  ( 0.000000000000000000, -0.7071067811865536790, 0.7071067811865413555 ) ) ;
#28319=VERTEX_POINT ( 'NONE', #13787 ) ;
#28330=ADVANCED_FACE ( 'NONE', ( #43157 ), #20884, .F. ) ;
#28333=ORIENTED_EDGE ( 'NONE', *, *, #35915, .F. ) ;
#28335=DIRECTION ( 'NONE',  ( 0.000000000000000000, -0.1045284632676578285, 0.9945218953682729568 ) ) ;
#28337=PLANE ( 'NONE',  #24587 ) ;
#28342=VECTOR ( 'NONE', #34590, 1000.000000000000000 ) ;
#28344=DIRECTION ( 'NONE',  ( 1.000000000000000000, -0.000000000000000000, -0.000000000000000000 ) ) ;
#28355=ORIENTED_EDGE ( 'NONE', *, *, #41444, .F. ) ;
#28357=CIRCLE ( 'NONE', #18171, 42.00000000000000000 ) ;
#28372=ORIENTED_EDGE ( 'NONE', *, *, #32925, .F. ) ;
#28373=DIRECTION ( 'NONE',  ( -0.000000000000000000, 0.4999999999999919509, 0.8660254037844432595 ) ) ;
#28377=CIRCLE ( 'NONE', #31552, 16.00000000000000000 ) ;
#28379=DIRECTION ( 'NONE',  ( -1.000000000000000000, 0.000000000000000000, -0.000000000000000000 ) ) ;
#28380=CARTESIAN_POINT ( 'NONE',  ( 10.00000000000000000, 0.000000000000000000, 0.000000000000000000 ) ) ;
#28393=EDGE_CURVE ( 'NONE', #46139, #40664, #8696, .T. ) ;
#28399=CIRCLE ( 'NONE', #19787, 37.49900000000000233 ) ;
#28406=VECTOR ( 'NONE', #13741, 1000.000000000000000 ) ;
#28413=ORIENTED_EDGE ( 'NONE', *, *, #5698, .F. ) ;
#28419=AXIS2_PLACEMENT_3D ( 'NONE', #891, #45447, #4581 ) ;
#28430=ORIENTED_EDGE ( 'NONE', *, *, #36902, .T. ) ;
#28433=DIRECTION ( 'NONE',  ( -1.000000000000000000, -0.000000000000000000, -0.000000000000000000 ) ) ;
#28434=DIRECTION ( 'NONE',  ( -1.000000000000000000, -0.000000000000000000, -0.000000000000000000 ) ) ;
#28435=ORIENTED_EDGE ( 'NONE', *, *, #9385, .F. ) ;
#28442=DIRECTION ( 'NONE',  ( -1.000000000000000000, -0.000000000000000000, 0.000000000000000000 ) ) ;
#28450=ORIENTED_EDGE ( 'NONE', *, *, #14878, .T. ) ;
#28478=AXIS2_PLACEMENT_3D ( 'NONE', #20528, #8785, #20785 ) ;
#28487=VERTEX_POINT ( 'NONE', #11558 ) ;
#28491=CIRCLE ( 'NONE', #44179, 16.00000000000000000 ) ;
#28492=AXIS2_PLACEMENT_3D ( 'NONE', #5251, #9876, #23845 ) ;
#28506=CARTESIAN_POINT ( 'NONE',  ( 0.000000000000000000, -33.79645857604525361, 16.45098606841114730 ) ) ;
#28512=DIRECTION ( 'NONE',  ( -1.000000000000000000, -0.000000000000000000, 0.000000000000000000 ) ) ;
#28526=CARTESIAN_POINT ( 'NONE',  ( 10.00000000000000000, 0.000000000000000000, 0.000000000000000000 ) ) ;
#28527=CARTESIAN_POINT ( 'NONE',  ( 0.000000000000000000, -37.48860685352290290, -0.8828120875904512665 ) ) ;
#28533=DIRECTION ( 'NONE',  ( 0.000000000000000000, 0.000000000000000000, -1.000000000000000000 ) ) ;
#28534=EDGE_CURVE ( 'NONE', #44380, #30662, #45084, .T. ) ;
#28558=ADVANCED_FACE ( 'NONE', ( #14506 ), #29432, .F. ) ;
#28559=FACE_OUTER_BOUND ( 'NONE', #26950, .T. ) ;
#28569=AXIS2_PLACEMENT_3D ( 'NONE', #45340, #41441, #11821 ) ;
#28572=ORIENTED_EDGE ( 'NONE', *, *, #37247, .F. ) ;
#28577=VECTOR ( 'NONE', #47592, 1000.000000000000000 ) ;
#28581=FACE_OUTER_BOUND ( 'NONE', #19092, .T. ) ;
#28595=CIRCLE ( 'NONE', #21560, 16.00000000000000000 ) ;
#28600=DIRECTION ( 'NONE',  ( 0.000000000000000000, -0.5877852522924689183, -0.8090169943749504489 ) ) ;
#28602=CIRCLE ( 'NONE', #45014, 16.00000000000000355 ) ;
#28604=CARTESIAN_POINT ( 'NONE',  ( 10.00000000000000000, 21.40280677340372151, 36.13751322684426981 ) ) ;
#28618=EDGE_CURVE ( 'NONE', #22486, #27674, #34776, .T. ) ;
#28621=AXIS2_PLACEMENT_3D ( 'NONE', #7641, #4218, #40935 ) ;
#28629=ORIENTED_EDGE ( 'NONE', *, *, #22500, .F. ) ;
#28634=ADVANCED_FACE ( 'NONE', ( #8584 ), #9086, .T. ) ;
#28645=VERTEX_POINT ( 'NONE', #12042 ) ;
#28652=FACE_OUTER_BOUND ( 'NONE', #23094, .T. ) ;
#28655=DIRECTION ( 'NONE',  ( 1.000000000000000000, 0.000000000000000000, 0.000000000000000000 ) ) ;
#28657=CARTESIAN_POINT ( 'NONE',  ( 0.000000000000000000, 16.83928648764923253, 16.46020748918050458 ) ) ;
#28662=DIRECTION ( 'NONE',  ( 1.000000000000000000, -0.000000000000000000, -0.000000000000000000 ) ) ;
#28663=VERTEX_POINT ( 'NONE', #20095 ) ;
#28664=VERTEX_POINT ( 'NONE', #16424 ) ;
#28670=CIRCLE ( 'NONE', #5333, 37.49900000000000944 ) ;
#28676=ORIENTED_EDGE ( 'NONE', *, *, #34237, .T. ) ;
#28684=CARTESIAN_POINT ( 'NONE',  ( 0.000000000000000000, -37.01155633439063308, 6.555932627142289526 ) ) ;
#28696=ADVANCED_FACE ( 'NONE', ( #34526 ), #1000, .T. ) ;
#28698=DIRECTION ( 'NONE',  ( -1.000000000000000000, 0.000000000000000000, 0.000000000000000000 ) ) ;
#28700=CARTESIAN_POINT ( 'NONE',  ( 10.00000000000000000, 17.80606268964540462, 33.00180498840053644 ) ) ;
#28701=ORIENTED_EDGE ( 'NONE', *, *, #34719, .T. ) ;
#28729=ORIENTED_EDGE ( 'NONE', *, *, #8183, .T. ) ;
#28733=ORIENTED_EDGE ( 'NONE', *, *, #10103, .T. ) ;
#28734=EDGE_LOOP ( 'NONE', ( #48185, #36382, #14095, #10007 ) ) ;
#28738=FACE_OUTER_BOUND ( 'NONE', #38364, .T. ) ;
#28744=CIRCLE ( 'NONE', #21717, 16.00000000000000000 ) ;
#28746=ORIENTED_EDGE ( 'NONE', *, *, #25222, .F. ) ;
#28748=CYLINDRICAL_SURFACE ( 'NONE', #40584, 16.00000000000000000 ) ;
#28754=ORIENTED_EDGE ( 'NONE', *, *, #39262, .T. ) ;
#28756=FACE_BOUND ( 'NONE', #30903, .T. ) ;
#28761=LINE ( 'NONE', #28270, #30704 ) ;
#28763=DIRECTION ( 'NONE',  ( 0.000000000000000000, -0.9876883405951393247, 0.1564344650402205161 ) ) ;
#28771=CARTESIAN_POINT ( 'NONE',  ( 0.000000000000000000, 22.07842321921492612, -8.187992925817130896 ) ) ;
#28787=CARTESIAN_POINT ( 'NONE',  ( 10.00000000000000000, 12.26510123303259725, 35.53030884539089840 ) ) ;
#28794=DIRECTION ( 'NONE',  ( 0.000000000000000000, 0.000000000000000000, 1.000000000000000000 ) ) ;
#28810=CARTESIAN_POINT ( 'NONE',  ( 10.00000000000000000, -37.22597642581153821, -5.202137450156795850 ) ) ;
#28816=ORIENTED_EDGE ( 'NONE', *, *, #11357, .T. ) ;
#28817=CYLINDRICAL_SURFACE ( 'NONE', #42131, 16.00000000000000000 ) ;
#28830=DIRECTION ( 'NONE',  ( -1.000000000000000000, -0.000000000000000000, -0.000000000000000000 ) ) ;
#28831=ORIENTED_EDGE ( 'NONE', *, *, #30432, .T. ) ;
#28836=CIRCLE ( 'NONE', #6175, 16.00000000000000355 ) ;
#28841=ORIENTED_EDGE ( 'NONE', *, *, #29787, .F. ) ;
#28843=CARTESIAN_POINT ( 'NONE',  ( 10.00000000000000000, 40.98264845739749518, 9.188173127307441845 ) ) ;
#28851=DIRECTION ( 'NONE',  ( 1.000000000000000000, 0.000000000000000000, 0.000000000000000000 ) ) ;
#28853=CARTESIAN_POINT ( 'NONE',  ( 10.00000000000000000, 0.000000000000000000, 0.000000000000000000 ) ) ;
#28856=ORIENTED_EDGE ( 'NONE', *, *, #22050, .F. ) ;
#28858=ORIENTED_EDGE ( 'NONE', *, *, #30187, .F. ) ;
#28859=DIRECTION ( 'NONE',  ( 1.000000000000000000, 0.000000000000000000, -0.000000000000000000 ) ) ;
#28863=ORIENTED_EDGE ( 'NONE', *, *, #39758, .F. ) ;
#28867=ORIENTED_EDGE ( 'NONE', *, *, #13861, .F. ) ;
#28877=CYLINDRICAL_SURFACE ( 'NONE', #39503, 16.00000000000000000 ) ;
#28880=DIRECTION ( 'NONE',  ( -1.000000000000000000, 0.000000000000000000, 0.000000000000000000 ) ) ;
#28893=VERTEX_POINT ( 'NONE', #26603 ) ;
#28900=CYLINDRICAL_SURFACE ( 'NONE', #39127, 42.00000000000000000 ) ;
#28902=ORIENTED_EDGE ( 'NONE', *, *, #1827, .F. ) ;
#28905=CYLINDRICAL_SURFACE ( 'NONE', #37570, 42.00000000000000000 ) ;
#28911=CARTESIAN_POINT ( 'NONE',  ( 10.00000000000000000, 0.000000000000000000, 0.000000000000000000 ) ) ;
#28915=ORIENTED_EDGE ( 'NONE', *, *, #17999, .F. ) ;
#28923=ORIENTED_EDGE ( 'NONE', *, *, #32060, .F. ) ;
#28925=CARTESIAN_POINT ( 'NONE',  ( -3.000000000000000000, -13.04903810567675038, 19.60159698893425428 ) ) ;
#28926=CYLINDRICAL_SURFACE ( 'NONE', #5541, 16.00000000000000000 ) ;
#28940=VERTEX_POINT ( 'NONE', #11916 ) ;
#28959=EDGE_CURVE ( 'NONE', #41768, #4382, #12631, .T. ) ;
#28961=ORIENTED_EDGE ( 'NONE', *, *, #12888, .F. ) ;
#28962=EDGE_CURVE ( 'NONE', #46699, #7678, #22679, .T. ) ;
#28967=DIRECTION ( 'NONE',  ( -0.000000000000000000, -0.4067366430757898277, -0.9135454576426055295 ) ) ;
#28974=CYLINDRICAL_SURFACE ( 'NONE', #23321, 21.00000000000000000 ) ;
#28976=DIRECTION ( 'NONE',  ( -1.000000000000000000, 0.000000000000000000, 0.000000000000000000 ) ) ;
#28984=CYLINDRICAL_SURFACE ( 'NONE', #32075, 16.00000000000000000 ) ;
#28985=CARTESIAN_POINT ( 'NONE',  ( 10.00000000000000000, -5.202137450156129717, -37.22597642581163768 ) ) ;
#28990=CARTESIAN_POINT ( 'NONE',  ( 10.00000000000000000, 22.64427369931169309, 30.00120703465213623 ) ) ;
#28992=CARTESIAN_POINT ( 'NONE',  ( -3.000000000000000000, -13.04903810567675038, 19.60159698893425428 ) ) ;
#28995=CARTESIAN_POINT ( 'NONE',  ( 10.00000000000000000, 39.04073710021344112, 15.48615015657596317 ) ) ;
#28998=DIRECTION ( 'NONE',  ( 0.000000000000000000, 0.7071067811865437980, 0.7071067811865512365 ) ) ;
#29012=EDGE_LOOP ( 'NONE', ( #37291, #9381, #44502, #47934 ) ) ;
#29014=ADVANCED_FACE ( 'NONE', ( #1868 ), #27331, .F. ) ;
#29017=ORIENTED_EDGE ( 'NONE', *, *, #25155, .F. ) ;
#29019=LINE ( 'NONE', #17522, #39860 ) ;
#29021=ORIENTED_EDGE ( 'NONE', *, *, #23599, .T. ) ;
#29022=EDGE_CURVE ( 'NONE', #17719, #13778, #14193, .T. ) ;
#29023=CIRCLE ( 'NONE', #37632, 42.00000000000000000 ) ;
#29026=DIRECTION ( 'NONE',  ( 0.000000000000000000, 0.000000000000000000, 1.000000000000000000 ) ) ;
#29034=VECTOR ( 'NONE', #18997, 1000.000000000000000 ) ;
#29036=CARTESIAN_POINT ( 'NONE',  ( 10.00000000000000000, -12.26510123303284594, 35.53030884539080603 ) ) ;
#29041=DIRECTION ( 'NONE',  ( -1.000000000000000000, -0.000000000000000000, -0.000000000000000000 ) ) ;
#29045=CARTESIAN_POINT ( 'NONE',  ( -10.00000000000000000, 0.000000000000000000, 0.000000000000000000 ) ) ;
#29046=CARTESIAN_POINT ( 'NONE',  ( -3.000000000000000000, -19.89357724625003598, 12.59942793731059574 ) ) ;
#29048=CARTESIAN_POINT ( 'NONE',  ( 0.000000000000000000, 0.000000000000000000, 0.000000000000000000 ) ) ;
#29067=VERTEX_POINT ( 'NONE', #31980 ) ;
#29069=DIRECTION ( 'NONE',  ( 0.000000000000000000, -0.8090169943749422332, -0.5877852522924803536 ) ) ;
#29077=AXIS2_PLACEMENT_3D ( 'NONE', #9353, #34818, #47047 ) ;
#29081=EDGE_CURVE ( 'NONE', #23433, #5548, #46170, .T. ) ;
#29090=CARTESIAN_POINT ( 'NONE',  ( 10.00000000000000000, 30.00120703465205452, 22.64427369931179967 ) ) ;
#29103=CARTESIAN_POINT ( 'NONE',  ( 0.000000000000000000, 12.42422080174688404, -35.38097989696498047 ) ) ;
#29105=EDGE_LOOP ( 'NONE', ( #29299, #35052, #29131, #28915 ) ) ;
#29106=CIRCLE ( 'NONE', #1761, 37.49900000000000233 ) ;
#29126=FACE_OUTER_BOUND ( 'NONE', #36681, .T. ) ;
#29127=AXIS2_PLACEMENT_3D ( 'NONE', #7572, #40385, #2922 ) ;
#29131=ORIENTED_EDGE ( 'NONE', *, *, #46816, .F. ) ;
#29134=DIRECTION ( 'NONE',  ( 0.000000000000000000, -6.982962677686267499E-15, 1.000000000000000000 ) ) ;
#29145=CARTESIAN_POINT ( 'NONE',  ( 0.000000000000000000, 16.61724383029361718, 20.69703378468926402 ) ) ;
#29151=DIRECTION ( 'NONE',  ( 1.000000000000000000, 0.000000000000000000, 0.000000000000000000 ) ) ;
#29161=CARTESIAN_POINT ( 'NONE',  ( 10.00000000000000000, 0.000000000000000000, 0.000000000000000000 ) ) ;
#29180=ADVANCED_FACE ( 'NONE', ( #43932 ), #21170, .T. ) ;
#29190=AXIS2_PLACEMENT_3D ( 'NONE', #10715, #3601, #25625 ) ;
#29192=EDGE_LOOP ( 'NONE', ( #18048, #40545, #41149, #24146 ) ) ;
#29195=AXIS2_PLACEMENT_3D ( 'NONE', #28282, #24368, #17023 ) ;
#29196=ORIENTED_EDGE ( 'NONE', *, *, #1224, .T. ) ;
#29199=CIRCLE ( 'NONE', #36217, 42.00000000000000000 ) ;
#29201=EDGE_CURVE ( 'NONE', #31219, #38104, #33163, .T. ) ;
#29202=DIRECTION ( 'NONE',  ( -1.000000000000000000, 0.000000000000000000, 0.000000000000000000 ) ) ;
#29211=PLANE ( 'NONE',  #43328 ) ;
#29236=CYLINDRICAL_SURFACE ( 'NONE', #32449, 42.00000000000000000 ) ;
#29242=CARTESIAN_POINT ( 'NONE',  ( 0.000000000000000000, 17.67226234102826510, 33.17418723428314564 ) ) ;
#29243=EDGE_CURVE ( 'NONE', #44060, #27986, #6495, .T. ) ;
#29245=DIRECTION ( 'NONE',  ( -1.000000000000000000, 0.000000000000000000, 0.000000000000000000 ) ) ;
#29247=DIRECTION ( 'NONE',  ( -1.000000000000000000, 0.000000000000000000, -0.000000000000000000 ) ) ;
#29252=DIRECTION ( 'NONE',  ( -1.000000000000000000, 0.000000000000000000, -0.000000000000000000 ) ) ;
#29254=CIRCLE ( 'NONE', #47252, 16.00000000000000355 ) ;
#29255=DIRECTION ( 'NONE',  ( 0.000000000000000000, 0.9135454576426002005, 0.4067366430758017071 ) ) ;
#29258=CIRCLE ( 'NONE', #5828, 42.00000000000000000 ) ;
#29263=ORIENTED_EDGE ( 'NONE', *, *, #19765, .F. ) ;
#29269=ORIENTED_EDGE ( 'NONE', *, *, #2405, .T. ) ;
#29272=ORIENTED_EDGE ( 'NONE', *, *, #8356, .T. ) ;
#29283=VERTEX_POINT ( 'NONE', #41000 ) ;
#29291=EDGE_LOOP ( 'NONE', ( #11723, #4425, #25104, #43946 ) ) ;
#29298=DIRECTION ( 'NONE',  ( 0.000000000000000000, 0.3090169943749410120, 0.9510565162951557516 ) ) ;
#29299=ORIENTED_EDGE ( 'NONE', *, *, #12999, .F. ) ;
#29305=CARTESIAN_POINT ( 'NONE',  ( 0.000000000000000000, -26.23277895567245821, -4.042438405570103477 ) ) ;
#29308=VECTOR ( 'NONE', #1879, 1000.000000000000114 ) ;
#29321=CARTESIAN_POINT ( 'NONE',  ( 0.000000000000000000, 0.000000000000000000, 0.000000000000000000 ) ) ;
#29322=CARTESIAN_POINT ( 'NONE',  ( 10.00000000000000000, 22.64427369931212297, -30.00120703465181293 ) ) ;
#29332=VERTEX_POINT ( 'NONE', #4031 ) ;
#29336=EDGE_CURVE ( 'NONE', #28487, #12494, #16566, .T. ) ;
#29339=EDGE_CURVE ( 'NONE', #7437, #1027, #29870, .T. ) ;
#29346=DIRECTION ( 'NONE',  ( 0.000000000000000000, 0.000000000000000000, 1.000000000000000000 ) ) ;
#29348=ORIENTED_EDGE ( 'NONE', *, *, #5363, .T. ) ;
#29351=CARTESIAN_POINT ( 'NONE',  ( 10.00000000000000000, 0.000000000000000000, 0.000000000000000000 ) ) ;
#29355=DIRECTION ( 'NONE',  ( -0.000000000000000000, -0.6691306063588671194, 0.7431448254773862505 ) ) ;
#29358=VERTEX_POINT ( 'NONE', #7695 ) ;
#29359=ADVANCED_FACE ( 'NONE', ( #26056 ), #18935, .F. ) ;
#29371=CARTESIAN_POINT ( 'NONE',  ( 10.00000000000000000, -10.41901085202107247, 40.68715046381925049 ) ) ;
#29381=VERTEX_POINT ( 'NONE', #22863 ) ;
#29383=ADVANCED_FACE ( 'NONE', ( #42927 ), #20391, .T. ) ;
#29402=ADVANCED_FACE ( 'NONE', ( #13073 ), #34846, .F. ) ;
#29404=DIRECTION ( 'NONE',  ( -1.000000000000000000, 0.000000000000000000, 0.000000000000000000 ) ) ;
#29411=CARTESIAN_POINT ( 'NONE',  ( 0.000000000000000000, -20.55727247249748046, 16.78983467731285018 ) ) ;
#29416=ORIENTED_EDGE ( 'NONE', *, *, #18290, .F. ) ;
#29418=ORIENTED_EDGE ( 'NONE', *, *, #26376, .T. ) ;
#29432=PLANE ( 'NONE',  #27480 ) ;
#29438=DIRECTION ( 'NONE',  ( 0.000000000000000000, 0.4539904997395477482, -0.8910065241883673437 ) ) ;
#29442=LINE ( 'NONE', #22078, #17842 ) ;
#29454=EDGE_LOOP ( 'NONE', ( #7659, #6344, #46748, #5069 ) ) ;
#29457=VECTOR ( 'NONE', #44483, 999.9999999999998863 ) ;
#29468=DIRECTION ( 'NONE',  ( 0.000000000000000000, 0.4539904997395414754, 0.8910065241883706744 ) ) ;
#29473=ORIENTED_EDGE ( 'NONE', *, *, #6759, .F. ) ;
#29480=VERTEX_POINT ( 'NONE', #42439 ) ;
#29482=CARTESIAN_POINT ( 'NONE',  ( 10.00000000000000000, 0.000000000000000000, 0.000000000000000000 ) ) ;
#29484=DIRECTION ( 'NONE',  ( 1.000000000000000000, -0.000000000000000000, -0.000000000000000000 ) ) ;
#29501=EDGE_CURVE ( 'NONE', #20927, #33784, #45620, .T. ) ;
#29509=CARTESIAN_POINT ( 'NONE',  ( 10.00000000000000000, -3.925862922256464493, 41.81611651403861174 ) ) ;
#29510=ADVANCED_FACE ( 'NONE', ( #41972 ), #8421, .T. ) ;
#29511=VERTEX_POINT ( 'NONE', #16015 ) ;
#29516=FACE_OUTER_BOUND ( 'NONE', #26346, .T. ) ;
#29523=VERTEX_POINT ( 'NONE', #19910 ) ;
#29531=DIRECTION ( 'NONE',  ( -1.000000000000000000, 0.000000000000000000, 0.000000000000000000 ) ) ;
#29533=CARTESIAN_POINT ( 'NONE',  ( 4.999999999999999112, -21.40280677340345505, -36.13751322684441192 ) ) ;
#29536=DIRECTION ( 'NONE',  ( -1.000000000000000000, -0.000000000000000000, -0.000000000000000000 ) ) ;
#29539=DIRECTION ( 'NONE',  ( 0.000000000000000000, -1.000000000000000000, -1.040834085586084257E-14 ) ) ;
#29552=DIRECTION ( 'NONE',  ( -1.000000000000000000, -0.000000000000000000, 0.000000000000000000 ) ) ;
#29554=DIRECTION ( 'NONE',  ( -1.000000000000000000, 0.000000000000000000, 0.000000000000000000 ) ) ;
#29558=( LENGTH_UNIT ( ) NAMED_UNIT ( * ) SI_UNIT ( .MILLI., .METRE. ) );
#29560=FACE_OUTER_BOUND ( 'NONE', #34045, .T. ) ;
#29562=EDGE_LOOP ( 'NONE', ( #17057, #23679, #13756, #9591 ) ) ;
#29565=CARTESIAN_POINT ( 'NONE',  ( -3.000000000000000000, -23.29833615347104825, -3.418703333116803744 ) ) ;
#29566=DIRECTION ( 'NONE',  ( 0.000000000000000000, 0.000000000000000000, 1.000000000000000000 ) ) ;
#29570=EDGE_CURVE ( 'NONE', #24574, #29827, #39276, .T. ) ;
#29574=VERTEX_POINT ( 'NONE', #36298 ) ;
#29581=ORIENTED_EDGE ( 'NONE', *, *, #10493, .F. ) ;
#29582=CARTESIAN_POINT ( 'NONE',  ( 0.000000000000000000, -1.278221433540501550, 26.51162292216071847 ) ) ;
#29587=VECTOR ( 'NONE', #45097, 1000.000000000000000 ) ;
#29589=CYLINDRICAL_SURFACE ( 'NONE', #24332, 42.00000000000000000 ) ;
#29590=ORIENTED_EDGE ( 'NONE', *, *, #21056, .F. ) ;
#29591=ORIENTED_EDGE ( 'NONE', *, *, #31232, .F. ) ;
#29604=DIRECTION ( 'NONE',  ( -1.000000000000000000, -0.000000000000000000, -0.000000000000000000 ) ) ;
#29612=EDGE_CURVE ( 'NONE', #23424, #5424, #21615, .T. ) ;
#29614=UNCERTAINTY_MEASURE_WITH_UNIT (LENGTH_MEASURE( 1.000000000000000082E-05 ), #14152, 'distance_accuracy_value', 'NONE');
#29617=DIRECTION ( 'NONE',  ( 1.000000000000000000, 0.000000000000000000, 0.000000000000000000 ) ) ;
#29622=CARTESIAN_POINT ( 'NONE',  ( 50.00005079999999680, 0.000000000000000000, 21.00000000000000000 ) ) ;
#29623=CARTESIAN_POINT ( 'NONE',  ( 5.000000000000000000, 27.75498641678742473, 31.52238457039609187 ) ) ;
#29629=EDGE_CURVE ( 'NONE', #7892, #46255, #24804, .T. ) ;
#29639=CYLINDRICAL_SURFACE ( 'NONE', #25930, 37.49900000000000233 ) ;
#29654=ORIENTED_EDGE ( 'NONE', *, *, #12711, .T. ) ;
#29666=EDGE_CURVE ( 'NONE', #12928, #12661, #17695, .T. ) ;
#29679=ORIENTED_EDGE ( 'NONE', *, *, #45523, .T. ) ;
#29682=CIRCLE ( 'NONE', #35933, 37.49900000000000233 ) ;
#29684=LINE ( 'NONE', #47553, #38540 ) ;
#29693=ORIENTED_EDGE ( 'NONE', *, *, #42213, .T. ) ;
#29695=ORIENTED_EDGE ( 'NONE', *, *, #2575, .T. ) ;
#29701=DIRECTION ( 'NONE',  ( -1.000000000000000000, 0.000000000000000000, -0.000000000000000000 ) ) ;
#29708=AXIS2_PLACEMENT_3D ( 'NONE', #27413, #21017, #9764 ) ;
#29714=CYLINDRICAL_SURFACE ( 'NONE', #9577, 16.00000000000000000 ) ;
#29718=PLANE ( 'NONE',  #36896 ) ;
#29719=LINE ( 'NONE', #44416, #17624 ) ;
#29726=DIRECTION ( 'NONE',  ( -1.000000000000000000, -0.000000000000000000, -0.000000000000000000 ) ) ;
#29736=CARTESIAN_POINT ( 'NONE',  ( 0.000000000000000000, 0.000000000000000000, 0.000000000000000000 ) ) ;
#29738=ORIENTED_EDGE ( 'NONE', *, *, #35532, .F. ) ;
#29739=CIRCLE ( 'NONE', #32840, 42.00000000000000000 ) ;
#29751=FACE_OUTER_BOUND ( 'NONE', #44799, .T. ) ;
#29755=EDGE_LOOP ( 'NONE', ( #10677, #20551, #36960, #45804 ) ) ;
#29756=ORIENTED_EDGE ( 'NONE', *, *, #42827, .T. ) ;
#29764=CYLINDRICAL_SURFACE ( 'NONE', #47312, 37.49900000000000233 ) ;
#29766=CYLINDRICAL_SURFACE ( 'NONE', #27231, 37.49900000000000233 ) ;
#29774=ORIENTED_EDGE ( 'NONE', *, *, #26393, .T. ) ;
#29777=ORIENTED_EDGE ( 'NONE', *, *, #33435, .F. ) ;
#29787=EDGE_CURVE ( 'NONE', #35244, #29480, #37739, .T. ) ;
#29792=CARTESIAN_POINT ( 'NONE',  ( 0.000000000000000000, 33.79645857604513992, -16.45098606841138178 ) ) ;
#29801=DIRECTION ( 'NONE',  ( 1.000000000000000000, -0.000000000000000000, -0.000000000000000000 ) ) ;
#29804=AXIS2_PLACEMENT_3D ( 'NONE', #18970, #3818, #41509 ) ;
#29805=DIRECTION ( 'NONE',  ( -1.000000000000000000, -0.000000000000000000, 0.000000000000000000 ) ) ;
#29814=ADVANCED_FACE ( 'NONE', ( #7645 ), #37261, .F. ) ;
#29817=CIRCLE ( 'NONE', #3933, 16.00000000000000000 ) ;
#29825=ADVANCED_FACE ( 'NONE', ( #7875 ), #30641, .T. ) ;
#29826=ORIENTED_EDGE ( 'NONE', *, *, #12479, .T. ) ;
#29827=VERTEX_POINT ( 'NONE', #30897 ) ;
#29841=ADVANCED_FACE ( 'NONE', ( #12526 ), #38228, .T. ) ;
#29846=FACE_OUTER_BOUND ( 'NONE', #2432, .T. ) ;
#29847=VERTEX_POINT ( 'NONE', #34296 ) ;
#29854=ORIENTED_EDGE ( 'NONE', *, *, #33498, .T. ) ;
#29861=ORIENTED_EDGE ( 'NONE', *, *, #46054, .F. ) ;
#29865=ORIENTED_EDGE ( 'NONE', *, *, #15737, .F. ) ;
#29867=ORIENTED_EDGE ( 'NONE', *, *, #5321, .T. ) ;
#29870=CIRCLE ( 'NONE', #43927, 42.00000000000000000 ) ;
#29877=DIRECTION ( 'NONE',  ( -1.000000000000000000, 0.000000000000000000, 0.000000000000000000 ) ) ;
#29882=VERTEX_POINT ( 'NONE', #26983 ) ;
#29888=CARTESIAN_POINT ( 'NONE',  ( 0.000000000000000000, 5.202137450156907761, -37.22597642581151689 ) ) ;
#29889=ORIENTED_EDGE ( 'NONE', *, *, #4240, .F. ) ;
#29893=DIRECTION ( 'NONE',  ( -1.000000000000000000, 0.000000000000000000, -0.000000000000000000 ) ) ;
#29897=LINE ( 'NONE', #19359, #20383 ) ;
#29898=CARTESIAN_POINT ( 'NONE',  ( 10.00000000000000000, -21.32104025579135964, 30.84782396557210760 ) ) ;
#29907=CARTESIAN_POINT ( 'NONE',  ( -3.000000000000000000, -20.55727247249748046, 16.78983467731285018 ) ) ;
#29919=VERTEX_POINT ( 'NONE', #19847 ) ;
#29955=DIRECTION ( 'NONE',  ( 1.000000000000000000, -0.000000000000000000, -0.000000000000000000 ) ) ;
#29960=LINE ( 'NONE', #14798, #37569 ) ;
#29964=CIRCLE ( 'NONE', #21319, 42.00000000000000000 ) ;
#29981=CARTESIAN_POINT ( 'NONE',  ( 10.00000000000000000, -36.88895765772637247, 6.736453364083436313 ) ) ;
#29986=ORIENTED_EDGE ( 'NONE', *, *, #39007, .F. ) ;
#29991=CYLINDRICAL_SURFACE ( 'NONE', #22646, 16.00000000000000000 ) ;
#29994=VECTOR ( 'NONE', #32579, 1000.000000000000000 ) ;
#30002=CARTESIAN_POINT ( 'NONE',  ( 10.00000000000000000, 35.47612816024523141, 22.48208911017513145 ) ) ;
#30010=DIRECTION ( 'NONE',  ( 0.000000000000000000, 0.3090169943749410120, 0.9510565162951557516 ) ) ;
#30012=ORIENTED_EDGE ( 'NONE', *, *, #17131, .T. ) ;
#30014=DIRECTION ( 'NONE',  ( 0.000000000000000000, 0.000000000000000000, 1.000000000000000000 ) ) ;
#30017=LINE ( 'NONE', #29533, #10548 ) ;
#30018=CARTESIAN_POINT ( 'NONE',  ( 10.00000000000000000, -40.98264845739743834, -9.188173127307738497 ) ) ;
#30024=AXIS2_PLACEMENT_3D ( 'NONE', #35706, #2175, #46961 ) ;
#30040=VECTOR ( 'NONE', #43047, 1000.000000000000000 ) ;
#30041=CIRCLE ( 'NONE', #6557, 37.49900000000000233 ) ;
#30052=ORIENTED_EDGE ( 'NONE', *, *, #14203, .T. ) ;
#30057=ORIENTED_EDGE ( 'NONE', *, *, #2570, .F. ) ;
#30060=LINE ( 'NONE', #23427, #39792 ) ;
#30066=PLANE ( 'NONE',  #25682 ) ;
#30077=EDGE_CURVE ( 'NONE', #7503, #44271, #21057, .T. ) ;
#30078=LINE ( 'NONE', #34214, #25938 ) ;
#30080=EDGE_CURVE ( 'NONE', #46139, #25303, #6383, .T. ) ;
#30081=DIRECTION ( 'NONE',  ( 0.000000000000000000, 0.8660254037844368202, 0.5000000000000029976 ) ) ;
#30089=ORIENTED_EDGE ( 'NONE', *, *, #30711, .T. ) ;
#30092=ORIENTED_EDGE ( 'NONE', *, *, #11228, .T. ) ;
#30093=DIRECTION ( 'NONE',  ( 0.000000000000000000, 0.000000000000000000, 1.000000000000000000 ) ) ;
#30106=DIRECTION ( 'NONE',  ( -1.000000000000000000, 0.000000000000000000, -0.000000000000000000 ) ) ;
#30112=CIRCLE ( 'NONE', #37122, 42.00000000000000000 ) ;
#30120=EDGE_CURVE ( 'NONE', #19539, #47351, #25446, .T. ) ;
#30127=ORIENTED_EDGE ( 'NONE', *, *, #17166, .F. ) ;
#30131=ADVANCED_FACE ( 'NONE', ( #7088 ), #44300, .T. ) ;
#30141=LINE ( 'NONE', #19343, #22862 ) ;
#30149=DIRECTION ( 'NONE',  ( 0.000000000000000000, 0.2079116908177664480, -0.9781476007338041345 ) ) ;
#30153=DIRECTION ( 'NONE',  ( 0.000000000000000000, -0.9781476007338070211, 0.2079116908177525425 ) ) ;
#30154=ORIENTED_EDGE ( 'NONE', *, *, #40078, .F. ) ;
#30157=DIRECTION ( 'NONE',  ( 0.000000000000000000, -0.9510565162951500895, -0.3090169943749583314 ) ) ;
#30161=AXIS2_PLACEMENT_3D ( 'NONE', #20372, #13777, #9361 ) ;
#30169=CARTESIAN_POINT ( 'NONE',  ( 10.00000000000000000, -12.42422080174663712, 35.38097989696507994 ) ) ;
#30184=ORIENTED_EDGE ( 'NONE', *, *, #5182, .T. ) ;
#30187=EDGE_CURVE ( 'NONE', #24216, #39388, #4158, .T. ) ;
#30191=AXIS2_PLACEMENT_3D ( 'NONE', #16011, #19653, #34583 ) ;
#30198=CARTESIAN_POINT ( 'NONE',  ( -3.000000000000000000, -26.23277895567251505, 4.042438405569750870 ) ) ;
#30208=CARTESIAN_POINT ( 'NONE',  ( 10.00000000000000000, -21.53537804866058991, -30.80686688397033635 ) ) ;
#30209=VERTEX_POINT ( 'NONE', #18596 ) ;
#30218=DIRECTION ( 'NONE',  ( 1.000000000000000000, 0.000000000000000000, -0.000000000000000000 ) ) ;
#30228=CARTESIAN_POINT ( 'NONE',  ( 0.000000000000000000, -23.29833615347104825, -3.418703333116803744 ) ) ;
#30236=CIRCLE ( 'NONE', #27908, 16.00000000000000000 ) ;
#30237=ADVANCED_FACE ( 'NONE', ( #44056 ), #10532, .T. ) ;
#30243=ADVANCED_FACE ( 'NONE', ( #38668 ), #23971, .T. ) ;
#30245=CARTESIAN_POINT ( 'NONE',  ( 4.999999999999999112, -3.925862922255855647, -41.81611651403866858 ) ) ;
#30246=ORIENTED_EDGE ( 'NONE', *, *, #22179, .F. ) ;
#30251=CARTESIAN_POINT ( 'NONE',  ( 10.00000000000000000, 0.000000000000000000, 0.000000000000000000 ) ) ;
#30253=ORIENTED_EDGE ( 'NONE', *, *, #17332, .T. ) ;
#30259=DIRECTION ( 'NONE',  ( 0.000000000000000000, -0.4999999999999913403, -0.8660254037844435926 ) ) ;
#30262=DIRECTION ( 'NONE',  ( -1.000000000000000000, 0.000000000000000000, 0.000000000000000000 ) ) ;
#30267=ORIENTED_EDGE ( 'NONE', *, *, #12479, .F. ) ;
#30271=DIRECTION ( 'NONE',  ( -1.000000000000000000, 0.000000000000000000, 0.000000000000000000 ) ) ;
#30275=LINE ( 'NONE', #18265, #11199 ) ;
#30284=DIRECTION ( 'NONE',  ( -1.000000000000000000, 0.000000000000000000, 0.000000000000000000 ) ) ;
#30288=FACE_OUTER_BOUND ( 'NONE', #46902, .T. ) ;
#30291=ORIENTED_EDGE ( 'NONE', *, *, #1505, .F. ) ;
#30300=EDGE_CURVE ( 'NONE', #27337, #9557, #42501, .T. ) ;
#30305=VERTEX_POINT ( 'NONE', #26914 ) ;
#30306=ORIENTED_EDGE ( 'NONE', *, *, #17618, .F. ) ;
#30309=ORIENTED_EDGE ( 'NONE', *, *, #6875, .T. ) ;
#30316=AXIS2_PLACEMENT_3D ( 'NONE', #47298, #25491, #36741 ) ;
#30321=VERTEX_POINT ( 'NONE', #31083 ) ;
#30324=LINE ( 'NONE', #8026, #18166 ) ;
#30328=CARTESIAN_POINT ( 'NONE',  ( 0.000000000000000000, -11.95096189432345390, 23.69967320028757385 ) ) ;
#30329=ADVANCED_FACE ( 'NONE', ( #8054 ), #46004, .T. ) ;
#30338=CARTESIAN_POINT ( 'NONE',  ( 0.000000000000000000, -33.79645857604501913, -16.45098606841161626 ) ) ;
#30344=FACE_OUTER_BOUND ( 'NONE', #44046, .T. ) ;
#30361=DIRECTION ( 'NONE',  ( 0.000000000000000000, -0.4539904997395352027, -0.8910065241883737830 ) ) ;
#30366=VERTEX_POINT ( 'NONE', #27161 ) ;
#30374=DIRECTION ( 'NONE',  ( 0.000000000000000000, 0.8090169943749504489, -0.5877852522924689183 ) ) ;
#30392=CARTESIAN_POINT ( 'NONE',  ( 0.000000000000000000, 16.61724383029390140, -20.69703378468904020 ) ) ;
#30393=DIRECTION ( 'NONE',  ( 0.000000000000000000, -0.7071067811865389130, -0.7071067811865563435 ) ) ;
#30394=EDGE_LOOP ( 'NONE', ( #43356, #20416, #16353, #23359 ) ) ;
#30408=CARTESIAN_POINT ( 'NONE',  ( 10.00000000000000000, -35.47612816024506088, -22.48208911017539435 ) ) ;
#30424=AXIS2_PLACEMENT_3D ( 'NONE', #21390, #3027, #36329 ) ;
#30429=ORIENTED_EDGE ( 'NONE', *, *, #15522, .F. ) ;
#30431=CARTESIAN_POINT ( 'NONE',  ( -3.000000000000000000, -22.32062822937469804, -14.36278369418829826 ) ) ;
#30432=EDGE_CURVE ( 'NONE', #46205, #44922, #6542, .T. ) ;
#30436=ADVANCED_FACE ( 'NONE', ( #32274 ), #36171, .T. ) ;
#30438=LINE ( 'NONE', #16243, #38890 ) ;
#30457=FACE_OUTER_BOUND ( 'NONE', #46525, .T. ) ;
#30460=CARTESIAN_POINT ( 'NONE',  ( -3.000000000000000000, 23.50000000000000000, 1.499999999999997780 ) ) ;
#30464=ORIENTED_EDGE ( 'NONE', *, *, #40304, .F. ) ;
#30473=EDGE_LOOP ( 'NONE', ( #8059, #2639, #39097, #1575 ) ) ;
#30481=VECTOR ( 'NONE', #11753, 1000.000000000000000 ) ;
#30485=VECTOR ( 'NONE', #14373, 1000.000000000000000 ) ;
#30488=ORIENTED_EDGE ( 'NONE', *, *, #39829, .T. ) ;
#30489=ORIENTED_EDGE ( 'NONE', *, *, #6612, .F. ) ;
#30495=CARTESIAN_POINT ( 'NONE',  ( 10.00000000000000000, 33.79645857604513992, 16.45098606841138178 ) ) ;
#30500=EDGE_CURVE ( 'NONE', #956, #28068, #1081, .T. ) ;
#30501=DIRECTION ( 'NONE',  ( -1.000000000000000000, 0.000000000000000000, -0.000000000000000000 ) ) ;
#30504=PLANE ( 'NONE',  #42567 ) ;
#30518=AXIS2_PLACEMENT_3D ( 'NONE', #45178, #16044, #4311 ) ;
#30538=DIRECTION ( 'NONE',  ( 0.000000000000000000, -0.9510565162951502005, -0.3090169943749581094 ) ) ;
#30540=DIRECTION ( 'NONE',  ( 0.000000000000000000, -0.2079116908177671419, 0.9781476007338040235 ) ) ;
#30545=ORIENTED_EDGE ( 'NONE', *, *, #16114, .F. ) ;
#30548=AXIS2_PLACEMENT_3D ( 'NONE', #33394, #48314, #44646 ) ;
#30553=ORIENTED_EDGE ( 'NONE', *, *, #2127, .F. ) ;
#30567=FACE_OUTER_BOUND ( 'NONE', #37575, .T. ) ;
#30578=ORIENTED_EDGE ( 'NONE', *, *, #19603, .F. ) ;
#30581=CIRCLE ( 'NONE', #32913, 37.49900000000000944 ) ;
#30596=ORIENTED_EDGE ( 'NONE', *, *, #8418, .F. ) ;
#30599=ORIENTED_EDGE ( 'NONE', *, *, #45150, .F. ) ;
#30603=LINE ( 'NONE', #31350, #22355 ) ;
#30615=DIRECTION ( 'NONE',  ( -1.000000000000000000, -0.000000000000000000, -0.000000000000000000 ) ) ;
#30627=EDGE_CURVE ( 'NONE', #20927, #28215, #19838, .T. ) ;
#30628=DIRECTION ( 'NONE',  ( 0.000000000000000000, 0.000000000000000000, -1.000000000000000000 ) ) ;
#30635=ORIENTED_EDGE ( 'NONE', *, *, #25627, .T. ) ;
#30641=CYLINDRICAL_SURFACE ( 'NONE', #32292, 16.00000000000000000 ) ;
#30648=VERTEX_POINT ( 'NONE', #14642 ) ;
#30651=DIRECTION ( 'NONE',  ( 0.000000000000000000, -6.938893903907228378E-15, 1.000000000000000000 ) ) ;
#30657=ORIENTED_EDGE ( 'NONE', *, *, #37072, .F. ) ;
#30660=CARTESIAN_POINT ( 'NONE',  ( 10.00000000000000000, 30.00120703465236716, -22.64427369931138756 ) ) ;
#30662=VERTEX_POINT ( 'NONE', #24089 ) ;
#30666=ADVANCED_FACE ( 'NONE', ( #5254 ), #9156, .T. ) ;
#30680=LINE ( 'NONE', #26529, #47285 ) ;
#30690=DIRECTION ( 'NONE',  ( -1.000000000000000000, 0.000000000000000000, 0.000000000000000000 ) ) ;
#30693=CARTESIAN_POINT ( 'NONE',  ( 10.00000000000000000, -33.17418723428294669, -17.67226234102862747 ) ) ;
#30696=CARTESIAN_POINT ( 'NONE',  ( 10.00000000000000000, 0.8828120875900632436, 37.48860685352291000 ) ) ;
#30704=VECTOR ( 'NONE', #39554, 1000.000000000000000 ) ;
#30711=EDGE_CURVE ( 'NONE', #35361, #14109, #42447, .T. ) ;
#30719=ORIENTED_EDGE ( 'NONE', *, *, #40716, .F. ) ;
#30736=ADVANCED_FACE ( 'NONE', ( #15370 ), #23593, .T. ) ;
#30739=AXIS2_PLACEMENT_3D ( 'NONE', #19650, #4276, #30948 ) ;
#30748=CARTESIAN_POINT ( 'NONE',  ( 10.00000000000000000, 0.000000000000000000, 0.000000000000000000 ) ) ;
#30750=CARTESIAN_POINT ( 'NONE',  ( -3.000000000000000000, -22.67460108101783334, 6.353146135317912169 ) ) ;
#30753=EDGE_CURVE ( 'NONE', #29847, #41101, #16712, .T. ) ;
#30756=EDGE_LOOP ( 'NONE', ( #6358, #39470, #10199, #24116 ) ) ;
#30759=CARTESIAN_POINT ( 'NONE',  ( 0.000000000000000000, -10.45096189432344147, 21.10159698893425784 ) ) ;
#30769=AXIS2_PLACEMENT_3D ( 'NONE', #7617, #45067, #33554 ) ;
#30771=ORIENTED_EDGE ( 'NONE', *, *, #36523, .T. ) ;
#30772=CIRCLE ( 'NONE', #9645, 15.99999999999999645 ) ;
#30776=ORIENTED_EDGE ( 'NONE', *, *, #19100, .F. ) ;
#30786=EDGE_CURVE ( 'NONE', #23469, #4226, #24573, .T. ) ;
#30788=VERTEX_POINT ( 'NONE', #17450 ) ;
#30789=CARTESIAN_POINT ( 'NONE',  ( 10.00000000000000000, 22.74946021919175720, -29.81001611430984255 ) ) ;
#30797=EDGE_LOOP ( 'NONE', ( #34745, #19437, #3682, #20964 ) ) ;
#30805=DIRECTION ( 'NONE',  ( 0.000000000000000000, 0.1045284632676570791, -0.9945218953682730678 ) ) ;
#30806=CIRCLE ( 'NONE', #310, 16.00000000000000000 ) ;
#30818=AXIS2_PLACEMENT_3D ( 'NONE', #32157, #24317, #25992 ) ;
#30842=EDGE_CURVE ( 'NONE', #12261, #42331, #36946, .T. ) ;
#30847=VECTOR ( 'NONE', #31138, 1000.000000000000000 ) ;
#30849=VECTOR ( 'NONE', #33460, 1000.000000000000000 ) ;
#30850=DIRECTION ( 'NONE',  ( 0.000000000000000000, 0.4539904997395412534, 0.8910065241883706744 ) ) ;
#30860=VERTEX_POINT ( 'NONE', #21847 ) ;
#30863=VERTEX_POINT ( 'NONE', #35825 ) ;
#30867=DIRECTION ( 'NONE',  ( -1.000000000000000000, 0.000000000000000000, 0.000000000000000000 ) ) ;
#30884=PLANE ( 'NONE',  #47766 ) ;
#30887=LINE ( 'NONE', #999, #6213 ) ;
#30888=CARTESIAN_POINT ( 'NONE',  ( 10.00000000000000000, 0.000000000000000000, 0.000000000000000000 ) ) ;
#30891=VECTOR ( 'NONE', #30106, 1000.000000000000000 ) ;
#30893=DIRECTION ( 'NONE',  ( 0.000000000000000000, -0.9510565162951543083, 0.3090169943749448977 ) ) ;
#30897=CARTESIAN_POINT ( 'NONE',  ( 10.00000000000000000, 41.81611651403861885, 3.925862922256313503 ) ) ;
#30903=EDGE_LOOP ( 'NONE', ( #23318, #44204, #9115, #7094 ) ) ;
#30904=EDGE_CURVE ( 'NONE', #27674, #9216, #7266, .T. ) ;
#30908=EDGE_CURVE ( 'NONE', #27887, #24885, #33045, .T. ) ;
#30912=VERTEX_POINT ( 'NONE', #22821 ) ;
#30920=VECTOR ( 'NONE', #2030, 1000.000000000000000 ) ;
#30922=CARTESIAN_POINT ( 'NONE',  ( 10.00000000000000000, -4.992566952384716927, -37.16516213103282951 ) ) ;
#30933=DIRECTION ( 'NONE',  ( -1.000000000000000000, 0.000000000000000000, 0.000000000000000000 ) ) ;
#30935=CARTESIAN_POINT ( 'NONE',  ( 0.000000000000000000, 37.01155633439059756, 6.555932627142549762 ) ) ;
#30937=CARTESIAN_POINT ( 'NONE',  ( 10.00000000000000000, 0.000000000000000000, 0.000000000000000000 ) ) ;
#30941=ORIENTED_EDGE ( 'NONE', *, *, #24212, .T. ) ;
#30946=ORIENTED_EDGE ( 'NONE', *, *, #24758, .T. ) ;
#30948=DIRECTION ( 'NONE',  ( 0.000000000000000000, 0.6691306063588563502, 0.7431448254773960205 ) ) ;
#30951=CIRCLE ( 'NONE', #39543, 16.00000000000000000 ) ;
#30956=CARTESIAN_POINT ( 'NONE',  ( 0.000000000000000000, -36.88895765772637247, 6.736453364083436313 ) ) ;
#30967=CARTESIAN_POINT ( 'NONE',  ( 10.00000000000000000, 0.000000000000000000, 0.000000000000000000 ) ) ;
#30975=ORIENTED_EDGE ( 'NONE', *, *, #47329, .F. ) ;
#30977=ORIENTED_EDGE ( 'NONE', *, *, #2422, .T. ) ;
#30979=AXIS2_PLACEMENT_3D ( 'NONE', #11136, #17502, #14810 ) ;
#30985=EDGE_CURVE ( 'NONE', #20241, #19341, #19378, .T. ) ;
#30995=ORIENTED_EDGE ( 'NONE', *, *, #28962, .F. ) ;
#30996=ORIENTED_EDGE ( 'NONE', *, *, #9280, .F. ) ;
#31005=DIRECTION ( 'NONE',  ( 0.000000000000000000, 0.9510565162951523099, 0.3090169943749517811 ) ) ;
#31013=AXIS2_PLACEMENT_3D ( 'NONE', #2961, #17890, #14228 ) ;
#31023=VECTOR ( 'NONE', #3851, 1000.000000000000000 ) ;
#31025=DIRECTION ( 'NONE',  ( -1.000000000000000000, 0.000000000000000000, 0.000000000000000000 ) ) ;
#31032=ORIENTED_EDGE ( 'NONE', *, *, #15647, .T. ) ;
#31034=ORIENTED_EDGE ( 'NONE', *, *, #9166, .T. ) ;
#31043=ORIENTED_EDGE ( 'NONE', *, *, #4104, .T. ) ;
#31050=CARTESIAN_POINT ( 'NONE',  ( 10.00000000000000000, -33.00180498840060039, 17.80606268964528027 ) ) ;
#31058=CYLINDRICAL_SURFACE ( 'NONE', #7239, 37.49900000000000233 ) ;
#31060=CARTESIAN_POINT ( 'NONE',  ( 10.00000000000000000, 6.736453364083557105, 36.88895765772635826 ) ) ;
#31066=AXIS2_PLACEMENT_3D ( 'NONE', #45352, #11598, #4262 ) ;
#31071=EDGE_CURVE ( 'NONE', #40610, #40065, #33826, .T. ) ;
#31083=CARTESIAN_POINT ( 'NONE',  ( 0.000000000000000000, -21.32104025579135964, 30.84782396557210760 ) ) ;
#31093=AXIS2_PLACEMENT_3D ( 'NONE', #26468, #26960, #33562 ) ;
#31097=ORIENTED_EDGE ( 'NONE', *, *, #20536, .F. ) ;
#31102=CIRCLE ( 'NONE', #24834, 37.49900000000000233 ) ;
#31104=FACE_OUTER_BOUND ( 'NONE', #5488, .T. ) ;
#31111=VERTEX_POINT ( 'NONE', #9332 ) ;
#31115=ORIENTED_EDGE ( 'NONE', *, *, #35146, .F. ) ;
#31119=CARTESIAN_POINT ( 'NONE',  ( 10.00000000000000000, 30.84782396557218931, 21.32104025579126017 ) ) ;
#31129=CARTESIAN_POINT ( 'NONE',  ( 0.000000000000000000, 17.67226234102874116, -33.17418723428288274 ) ) ;
#31138=DIRECTION ( 'NONE',  ( 0.000000000000000000, -0.2079116908177532363, -0.9781476007338069101 ) ) ;
#31148=SHAPE_DEFINITION_REPRESENTATION ( #19804, #12525 ) ;
#31154=CARTESIAN_POINT ( 'NONE',  ( 0.000000000000000000, -9.188173127307592836, 40.98264845739746676 ) ) ;
#31169=DIRECTION ( 'NONE',  ( 0.000000000000000000, 0.000000000000000000, 1.000000000000000000 ) ) ;
#31176=ORIENTED_EDGE ( 'NONE', *, *, #38017, .F. ) ;
#31177=EDGE_CURVE ( 'NONE', #35793, #24691, #12306, .T. ) ;
#31180=EDGE_CURVE ( 'NONE', #26444, #33012, #33084, .T. ) ;
#31184=ORIENTED_EDGE ( 'NONE', *, *, #38812, .F. ) ;
#31192=CARTESIAN_POINT ( 'NONE',  ( 0.000000000000000000, -13.04903810567647682, -19.60159698893442481 ) ) ;
#31196=CARTESIAN_POINT ( 'NONE',  ( -3.000000000000000000, 5.835314593368772229, -22.81335362449846826 ) ) ;
#31199=ORIENTED_EDGE ( 'NONE', *, *, #22325, .F. ) ;
#31201=EDGE_LOOP ( 'NONE', ( #24459, #5976, #19825, #21184 ) ) ;
#31213=AXIS2_PLACEMENT_3D ( 'NONE', #16434, #31873, #46788 ) ;
#31214=EDGE_CURVE ( 'NONE', #960, #21976, #43265, .T. ) ;
#31219=VERTEX_POINT ( 'NONE', #47270 ) ;
#31232=EDGE_CURVE ( 'NONE', #35055, #27526, #17636, .T. ) ;
#31241=DIRECTION ( 'NONE',  ( 0.000000000000000000, 0.000000000000000000, 1.000000000000000000 ) ) ;
#31242=ORIENTED_EDGE ( 'NONE', *, *, #37322, .T. ) ;
#31244=CYLINDRICAL_SURFACE ( 'NONE', #45737, 16.00000000000000000 ) ;
#31250=ADVANCED_FACE ( 'NONE', ( #29126 ), #39922, .F. ) ;
#31259=ORIENTED_EDGE ( 'NONE', *, *, #23250, .F. ) ;
#31264=ORIENTED_EDGE ( 'NONE', *, *, #23695, .F. ) ;
#31268=AXIS2_PLACEMENT_3D ( 'NONE', #31947, #16764, #31714 ) ;
#31278=ADVANCED_FACE ( 'NONE', ( #43822 ), #32794, .F. ) ;
#31279=ORIENTED_EDGE ( 'NONE', *, *, #953, .T. ) ;
#31289=EDGE_LOOP ( 'NONE', ( #9131, #13454, #237, #1638 ) ) ;
#31292=CARTESIAN_POINT ( 'NONE',  ( -3.000000000000000000, 23.59884966291521380, 12.14883922797262805 ) ) ;
#31295=LINE ( 'NONE', #46214, #7303 ) ;
#31299=EDGE_CURVE ( 'NONE', #38112, #28664, #21346, .T. ) ;
#31303=AXIS2_PLACEMENT_3D ( 'NONE', #6769, #21448, #33660 ) ;
#31322=CARTESIAN_POINT ( 'NONE',  ( 10.00000000000000000, 0.000000000000000000, 0.000000000000000000 ) ) ;
#31347=DIRECTION ( 'NONE',  ( -1.000000000000000000, -0.000000000000000000, -0.000000000000000000 ) ) ;
#31350=CARTESIAN_POINT ( 'NONE',  ( 5.000000000000000000, 35.47612816024556537, -22.48208911017461631 ) ) ;
#31356=DIRECTION ( 'NONE',  ( 0.000000000000000000, -0.8090169943749402348, -0.5877852522924830181 ) ) ;
#31357=EDGE_CURVE ( 'NONE', #43176, #33558, #22521, .T. ) ;
#31360=CYLINDRICAL_SURFACE ( 'NONE', #19558, 37.49900000000000233 ) ;
#31377=CARTESIAN_POINT ( 'NONE',  ( 0.000000000000000000, 30.00120703465205452, 22.64427369931179967 ) ) ;
#31378=CARTESIAN_POINT ( 'NONE',  ( 0.000000000000000000, -40.98264845739755202, 9.188173127307159405 ) ) ;
#31425=FACE_OUTER_BOUND ( 'NONE', #34555, .T. ) ;
#31432=DIRECTION ( 'NONE',  ( -0.000000000000000000, 0.7431448254773946882, -0.6691306063588577935 ) ) ;
#31443=DIRECTION ( 'NONE',  ( 0.000000000000000000, 1.000000000000000000, 3.491481338843133750E-15 ) ) ;
#31444=ORIENTED_EDGE ( 'NONE', *, *, #9055, .F. ) ;
#31455=EDGE_LOOP ( 'NONE', ( #47918, #26980, #17478, #6059 ) ) ;
#31477=DIRECTION ( 'NONE',  ( 1.000000000000000000, 0.000000000000000000, 0.000000000000000000 ) ) ;
#31483=CARTESIAN_POINT ( 'NONE',  ( -3.000000000000000000, 16.61724383029361718, 20.69703378468926402 ) ) ;
#31490=VERTEX_POINT ( 'NONE', #41860 ) ;
#31496=DIRECTION ( 'NONE',  ( 1.000000000000000000, 0.000000000000000000, -0.000000000000000000 ) ) ;
#31499=CARTESIAN_POINT ( 'NONE',  ( -3.000000000000000000, 20.85821328998756385, -10.92862929874494959 ) ) ;
#31504=VECTOR ( 'NONE', #38736, 1000.000000000000000 ) ;
#31526=ORIENTED_EDGE ( 'NONE', *, *, #39638, .F. ) ;
#31539=CARTESIAN_POINT ( 'NONE',  ( 0.000000000000000000, -31.52238457039619490, 27.75498641678731104 ) ) ;
#31548=VERTEX_POINT ( 'NONE', #46241 ) ;
#31552=AXIS2_PLACEMENT_3D ( 'NONE', #9008, #12685, #27610 ) ;
#31557=CIRCLE ( 'NONE', #29190, 16.00000000000000000 ) ;
#31561=FACE_OUTER_BOUND ( 'NONE', #40295, .T. ) ;
#31562=DIRECTION ( 'NONE',  ( -1.000000000000000000, 0.000000000000000000, 0.000000000000000000 ) ) ;
#31565=DIRECTION ( 'NONE',  ( 0.000000000000000000, 0.000000000000000000, 1.000000000000000000 ) ) ;
#31567=VERTEX_POINT ( 'NONE', #12710 ) ;
#31573=EDGE_CURVE ( 'NONE', #28097, #46278, #45503, .T. ) ;
#31579=LINE ( 'NONE', #8787, #6279 ) ;
#31580=AXIS2_PLACEMENT_3D ( 'NONE', #34391, #45671, #31005 ) ;
#31585=EDGE_LOOP ( 'NONE', ( #17878, #25358, #40592, #42318 ) ) ;
#31590=VERTEX_POINT ( 'NONE', #4082 ) ;
#31594=DIRECTION ( 'NONE',  ( -1.000000000000000000, -0.000000000000000000, 0.000000000000000000 ) ) ;
#31598=AXIS2_PLACEMENT_3D ( 'NONE', #18671, #2240, #38746 ) ;
#31601=ORIENTED_EDGE ( 'NONE', *, *, #38249, .T. ) ;
#31604=CARTESIAN_POINT ( 'NONE',  ( -3.000000000000000000, 24.81905959214261514, 9.408202855044825341 ) ) ;
#31616=CIRCLE ( 'NONE', #9679, 16.00000000000000000 ) ;
#31625=CARTESIAN_POINT ( 'NONE',  ( 0.000000000000000000, -22.74946021919153694, 29.81001611431000597 ) ) ;
#31626=AXIS2_PLACEMENT_3D ( 'NONE', #40192, #32128, #36502 ) ;
#31640=ORIENTED_EDGE ( 'NONE', *, *, #11006, .F. ) ;
#31647=ORIENTED_EDGE ( 'NONE', *, *, #27250, .T. ) ;
#31649=ADVANCED_FACE ( 'NONE', ( #37367 ), #30504, .F. ) ;
#31652=LINE ( 'NONE', #46079, #4725 ) ;
#31660=LINE ( 'NONE', #46325, #4388 ) ;
#31661=CARTESIAN_POINT ( 'NONE',  ( -3.000000000000000000, 0.000000000000000000, 0.000000000000000000 ) ) ;
#31670=CARTESIAN_POINT ( 'NONE',  ( 0.000000000000000000, -25.88420570971419821, 27.13269053701087330 ) ) ;
#31685=CARTESIAN_POINT ( 'NONE',  ( 0.000000000000000000, -19.89357724624987256, -12.59942793731086041 ) ) ;
#31688=EDGE_CURVE ( 'NONE', #44417, #46514, #21440, .T. ) ;
#31708=EDGE_LOOP ( 'NONE', ( #11760, #37482, #19035, #41224 ) ) ;
#31714=DIRECTION ( 'NONE',  ( 0.000000000000000000, 0.8090169943749487835, -0.5877852522924713607 ) ) ;
#31719=AXIS2_PLACEMENT_3D ( 'NONE', #13954, #10277, #36470 ) ;
#31730=FACE_BOUND ( 'NONE', #22118, .T. ) ;
#31734=DIRECTION ( 'NONE',  ( -0.000000000000000000, 0.8660254037844368202, 0.5000000000000031086 ) ) ;
#31736=DIRECTION ( 'NONE',  ( -1.000000000000000000, 0.000000000000000000, 0.000000000000000000 ) ) ;
#31740=CARTESIAN_POINT ( 'NONE',  ( 10.00000000000000000, -35.92658777277502935, -10.74501242461320594 ) ) ;
#31744=CARTESIAN_POINT ( 'NONE',  ( -3.000000000000000000, -23.29833615347109443, 3.418703333116492438 ) ) ;
#31765=CIRCLE ( 'NONE', #4394, 16.00000000000000000 ) ;
#31775=CARTESIAN_POINT ( 'NONE',  ( 0.000000000000000000, 27.13269053701096922, 25.88420570971410228 ) ) ;
#31777=AXIS2_PLACEMENT_3D ( 'NONE', #2273, #2054, #21104 ) ;
#31781=ORIENTED_EDGE ( 'NONE', *, *, #40707, .T. ) ;
#31790=VECTOR ( 'NONE', #35267, 1000.000000000000114 ) ;
#31800=EDGE_LOOP ( 'NONE', ( #7600, #8876, #46041, #42803 ) ) ;
#31803=EDGE_LOOP ( 'NONE', ( #18862, #25579, #46573, #19455 ) ) ;
#31812=DIRECTION ( 'NONE',  ( -1.000000000000000000, 0.000000000000000000, 0.000000000000000000 ) ) ;
#31818=ADVANCED_FACE ( 'NONE', ( #45927 ), #16540, .T. ) ;
#31822=ORIENTED_EDGE ( 'NONE', *, *, #12761, .T. ) ;
#31829=VECTOR ( 'NONE', #7030, 1000.000000000000000 ) ;
#31830=ORIENTED_EDGE ( 'NONE', *, *, #1764, .T. ) ;
#31832=DIRECTION ( 'NONE',  ( 1.000000000000000000, 0.000000000000000000, 0.000000000000000000 ) ) ;
#31834=VERTEX_POINT ( 'NONE', #27817 ) ;
#31843=DIRECTION ( 'NONE',  ( -0.000000000000000000, 0.5000000000000039968, -0.8660254037844363761 ) ) ;
#31849=CARTESIAN_POINT ( 'NONE',  ( -3.000000000000000000, -26.23277895567245821, -4.042438405570103477 ) ) ;
#31850=VECTOR ( 'NONE', #35814, 1000.000000000000000 ) ;
#31854=ADVANCED_FACE ( 'NONE', ( #27324 ), #19963, .T. ) ;
#31855=CARTESIAN_POINT ( 'NONE',  ( 5.000000000000000000, 15.48615015657581750, 39.04073710021349797 ) ) ;
#31857=ORIENTED_EDGE ( 'NONE', *, *, #12315, .T. ) ;
#31873=DIRECTION ( 'NONE',  ( -1.000000000000000000, -0.000000000000000000, 0.000000000000000000 ) ) ;
#31874=DIRECTION ( 'NONE',  ( -1.000000000000000000, 0.000000000000000000, 0.000000000000000000 ) ) ;
#31877=AXIS2_PLACEMENT_3D ( 'NONE', #24118, #39046, #35847 ) ;
#31880=ADVANCED_FACE ( 'NONE', ( #38582 ), #31244, .T. ) ;
#31884=EDGE_CURVE ( 'NONE', #38396, #33784, #16036, .T. ) ;
#31885=ORIENTED_EDGE ( 'NONE', *, *, #42715, .T. ) ;
#31906=DIRECTION ( 'NONE',  ( 0.000000000000000000, 0.7431448254773946882, -0.6691306063588577935 ) ) ;
#31915=DIRECTION ( 'NONE',  ( -1.000000000000000000, -0.000000000000000000, 0.000000000000000000 ) ) ;
#31921=EDGE_CURVE ( 'NONE', #45054, #24690, #20716, .T. ) ;
#31924=CYLINDRICAL_SURFACE ( 'NONE', #13503, 16.00000000000000000 ) ;
#31925=FACE_OUTER_BOUND ( 'NONE', #47505, .T. ) ;
#31927=CARTESIAN_POINT ( 'NONE',  ( 0.000000000000000000, -37.22597642581161637, 5.202137450156258502 ) ) ;
#31937=DIRECTION ( 'NONE',  ( -1.000000000000000000, -0.000000000000000000, -0.000000000000000000 ) ) ;
#31946=CARTESIAN_POINT ( 'NONE',  ( 0.000000000000000000, 4.992566952385522505, -37.16516213103271582 ) ) ;
#31947=CARTESIAN_POINT ( 'NONE',  ( 0.000000000000000000, 33.17418723428307459, 17.67226234102837878 ) ) ;
#31949=ADVANCED_FACE ( 'NONE', ( #6255 ), #20691, .T. ) ;
#31950=ORIENTED_EDGE ( 'NONE', *, *, #39527, .T. ) ;
#31963=FACE_BOUND ( 'NONE', #2075, .T. ) ;
#31968=LINE ( 'NONE', #36340, #47981 ) ;
#31970=EDGE_CURVE ( 'NONE', #8466, #36706, #8977, .T. ) ;
#31976=ORIENTED_EDGE ( 'NONE', *, *, #40173, .F. ) ;
#31980=CARTESIAN_POINT ( 'NONE',  ( 0.000000000000000000, 38.55633173627034438, -16.65560815589369881 ) ) ;
#31982=AXIS2_PLACEMENT_3D ( 'NONE', #10377, #25542, #40492 ) ;
#31996=DIRECTION ( 'NONE',  ( 0.000000000000000000, 0.7071067811865486830, -0.7071067811865463515 ) ) ;
#32005=VERTEX_POINT ( 'NONE', #24845 ) ;
#32024=( GEOMETRIC_REPRESENTATION_CONTEXT ( 3 ) GLOBAL_UNCERTAINTY_ASSIGNED_CONTEXT ( ( #29614 ) ) GLOBAL_UNIT_ASSIGNED_CONTEXT ( ( #14152, #18295, #40815 ) ) REPRESENTATION_CONTEXT ( 'NONE', 'WORKASPACE' ) );
#32030=ORIENTED_EDGE ( 'NONE', *, *, #20268, .F. ) ;
#32033=FACE_OUTER_BOUND ( 'NONE', #41959, .T. ) ;
#32037=ADVANCED_FACE ( 'NONE', ( #26098 ), #41517, .F. ) ;
#32041=CYLINDRICAL_SURFACE ( 'NONE', #21433, 16.00000000000000000 ) ;
#32042=AXIS2_PLACEMENT_3D ( 'NONE', #6286, #2589, #2840 ) ;
#32057=EDGE_LOOP ( 'NONE', ( #32892, #14645, #14523, #23987 ) ) ;
#32060=EDGE_CURVE ( 'NONE', #41101, #4382, #30017, .T. ) ;
#32066=DIRECTION ( 'NONE',  ( 0.000000000000000000, -0.8910065241883626808, -0.4539904997395570740 ) ) ;
#32068=EDGE_LOOP ( 'NONE', ( #26762, #6622, #26211, #3844 ) ) ;
#32070=CIRCLE ( 'NONE', #45328, 16.00000000000000000 ) ;
#32075=AXIS2_PLACEMENT_3D ( 'NONE', #25308, #40268, #37305 ) ;
#32080=EDGE_LOOP ( 'NONE', ( #30012, #35242, #43838, #10920 ) ) ;
#32081=DIRECTION ( 'NONE',  ( -1.000000000000000000, 0.000000000000000000, 0.000000000000000000 ) ) ;
#32084=CARTESIAN_POINT ( 'NONE',  ( -10.00000000000000000, 0.000000000000000000, 0.000000000000000000 ) ) ;
#32103=VECTOR ( 'NONE', #11096, 1000.000000000000000 ) ;
#32105=AXIS2_PLACEMENT_3D ( 'NONE', #28985, #36573, #10390 ) ;
#32107=ORIENTED_EDGE ( 'NONE', *, *, #11839, .T. ) ;
#32112=AXIS2_PLACEMENT_3D ( 'NONE', #14671, #10511, #40380 ) ;
#32113=ADVANCED_FACE ( 'NONE', ( #44457 ), #33444, .T. ) ;
#32128=DIRECTION ( 'NONE',  ( 0.000000000000000000, -0.6691306063588662312, 0.7431448254773870277 ) ) ;
#32129=CARTESIAN_POINT ( 'NONE',  ( -3.000000000000000000, 23.50000000000000000, 1.499999999999997780 ) ) ;
#32130=AXIS2_PLACEMENT_3D ( 'NONE', #13095, #24595, #20671 ) ;
#32135=LINE ( 'NONE', #27499, #32637 ) ;
#32142=DIRECTION ( 'NONE',  ( 0.000000000000000000, 0.000000000000000000, 1.000000000000000000 ) ) ;
#32155=DIRECTION ( 'NONE',  ( 0.000000000000000000, 0.2079116908177664758, -0.9781476007338042455 ) ) ;
#32157=CARTESIAN_POINT ( 'NONE',  ( 10.00000000000000000, 5.202137450156389953, 37.22597642581160216 ) ) ;
#32158=EDGE_LOOP ( 'NONE', ( #13613, #27234, #15664, #28729 ) ) ;
#32161=CARTESIAN_POINT ( 'NONE',  ( 0.000000000000000000, 0.000000000000000000, 0.000000000000000000 ) ) ;
#32170=ADVANCED_FACE ( 'NONE', ( #14849 ), #29764, .T. ) ;
#32171=ORIENTED_EDGE ( 'NONE', *, *, #7667, .T. ) ;
#32172=VECTOR ( 'NONE', #19295, 1000.000000000000000 ) ;
#32178=EDGE_CURVE ( 'NONE', #17758, #32256, #34886, .T. ) ;
#32181=CIRCLE ( 'NONE', #24337, 37.49900000000000233 ) ;
#32182=ORIENTED_EDGE ( 'NONE', *, *, #46680, .T. ) ;
#32185=VERTEX_POINT ( 'NONE', #1368 ) ;
#32195=CARTESIAN_POINT ( 'NONE',  ( 10.00000000000000000, 21.32104025579114648, 30.84782396557224970 ) ) ;
#32198=DIRECTION ( 'NONE',  ( 0.000000000000000000, 0.000000000000000000, 1.000000000000000000 ) ) ;
#32205=ORIENTED_EDGE ( 'NONE', *, *, #30842, .F. ) ;
#32207=ORIENTED_EDGE ( 'NONE', *, *, #17572, .T. ) ;
#32221=VERTEX_POINT ( 'NONE', #34386 ) ;
#32234=CARTESIAN_POINT ( 'NONE',  ( 10.00000000000000000, -30.84782396557201878, -21.32104025579148399 ) ) ;
#32242=EDGE_LOOP ( 'NONE', ( #40650, #11537, #43196, #2234 ) ) ;
#32244=EDGE_LOOP ( 'NONE', ( #34624, #36204, #84, #8030 ) ) ;
#32249=CARTESIAN_POINT ( 'NONE',  ( 0.000000000000000000, -22.67460108101774807, -6.353146135318215038 ) ) ;
#32255=DIRECTION ( 'NONE',  ( 0.000000000000000000, 0.000000000000000000, 1.000000000000000000 ) ) ;
#32256=VERTEX_POINT ( 'NONE', #45665 ) ;
#32260=DIRECTION ( 'NONE',  ( -1.000000000000000000, -0.000000000000000000, -0.000000000000000000 ) ) ;
#32265=LINE ( 'NONE', #27631, #38856 ) ;
#32269=DIRECTION ( 'NONE',  ( 0.000000000000000000, 0.7431448254773862505, 0.6691306063588671194 ) ) ;
#32270=DIRECTION ( 'NONE',  ( 0.000000000000000000, -1.156482317317870936E-15, -1.000000000000000000 ) ) ;
#32272=ADVANCED_FACE ( 'NONE', ( #5515 ), #45918, .T. ) ;
#32274=FACE_OUTER_BOUND ( 'NONE', #26334, .T. ) ;
#32281=CARTESIAN_POINT ( 'NONE',  ( 10.00000000000000000, 6.736453364084091788, -36.88895765772625879 ) ) ;
#32292=AXIS2_PLACEMENT_3D ( 'NONE', #20328, #15709, #35028 ) ;
#32293=EDGE_CURVE ( 'NONE', #5676, #293, #40016, .T. ) ;
#32296=CARTESIAN_POINT ( 'NONE',  ( 10.00000000000000000, 0.6853352020795618893, -37.58145647212453611 ) ) ;
#32314=ORIENTED_EDGE ( 'NONE', *, *, #12058, .T. ) ;
#32318=DIRECTION ( 'NONE',  ( 0.000000000000000000, -0.7071067811865536790, 0.7071067811865413555 ) ) ;
#32319=DIRECTION ( 'NONE',  ( 1.000000000000000000, 0.000000000000000000, 0.000000000000000000 ) ) ;
#32322=DIRECTION ( 'NONE',  ( -1.000000000000000000, -0.000000000000000000, 0.000000000000000000 ) ) ;
#32323=DIRECTION ( 'NONE',  ( 0.000000000000000000, 0.4539904997395477482, -0.8910065241883673437 ) ) ;
#32328=CARTESIAN_POINT ( 'NONE',  ( -3.000000000000000000, -20.55727247249726020, -16.78983467731313084 ) ) ;
#32333=EDGE_LOOP ( 'NONE', ( #32655, #4432, #10480, #9413 ) ) ;
#32344=DIRECTION ( 'NONE',  ( 0.000000000000000000, 0.000000000000000000, -1.000000000000000000 ) ) ;
#32345=ORIENTED_EDGE ( 'NONE', *, *, #16680, .F. ) ;
#32348=ADVANCED_FACE ( 'NONE', ( #17007, #47581, #6015, #2094, #35620, #36092, #31730, #13107, #28040, #9659, #35849, #28756, #24606, #13837, #42966, #9417, #31963 ), #5764, .F. ) ;
#32363=DIRECTION ( 'NONE',  ( 0.000000000000000000, 0.000000000000000000, 1.000000000000000000 ) ) ;
#32372=FACE_OUTER_BOUND ( 'NONE', #24163, .T. ) ;
#32373=EDGE_LOOP ( 'NONE', ( #35036, #31640, #6711, #21963 ) ) ;
#32379=DIRECTION ( 'NONE',  ( 0.000000000000000000, 0.3090169943749482839, -0.9510565162951533091 ) ) ;
#32397=CARTESIAN_POINT ( 'NONE',  ( 10.00000000000000178, 0.000000000000000000, 0.000000000000000000 ) ) ;
#32399=EDGE_CURVE ( 'NONE', #32891, #2211, #11601, .T. ) ;
#32406=DIRECTION ( 'NONE',  ( -1.000000000000000000, 0.000000000000000000, 0.000000000000000000 ) ) ;
#32410=CIRCLE ( 'NONE', #10531, 16.00000000000000000 ) ;
#32414=ORIENTED_EDGE ( 'NONE', *, *, #37524, .T. ) ;
#32416=AXIS2_PLACEMENT_3D ( 'NONE', #124, #44933, #29026 ) ;
#32417=CIRCLE ( 'NONE', #22243, 37.49900000000000944 ) ;
#32429=CARTESIAN_POINT ( 'NONE',  ( 5.000000000000000000, 26.79245525562714292, 32.34446384429980981 ) ) ;
#32432=ORIENTED_EDGE ( 'NONE', *, *, #23446, .F. ) ;
#32446=ORIENTED_EDGE ( 'NONE', *, *, #42437, .F. ) ;
#32449=AXIS2_PLACEMENT_3D ( 'NONE', #36571, #40499, #44644 ) ;
#32451=CARTESIAN_POINT ( 'NONE',  ( 4.999999999999999112, -41.81611651403864727, 3.925862922256025289 ) ) ;
#32471=CIRCLE ( 'NONE', #16862, 42.00000000000000000 ) ;
#32472=PLANE ( 'NONE',  #44519 ) ;
#32475=ORIENTED_EDGE ( 'NONE', *, *, #13480, .F. ) ;
#32479=ADVANCED_FACE ( 'NONE', ( #33145 ), #22122, .T. ) ;
#32484=ORIENTED_EDGE ( 'NONE', *, *, #21163, .F. ) ;
#32486=ORIENTED_EDGE ( 'NONE', *, *, #42777, .T. ) ;
#32499=DIRECTION ( 'NONE',  ( 1.000000000000000000, -0.000000000000000000, 0.000000000000000000 ) ) ;
#32502=DIRECTION ( 'NONE',  ( -0.000000000000000000, 0.000000000000000000, 1.000000000000000000 ) ) ;
#32511=LINE ( 'NONE', #39372, #11497 ) ;
#32520=ORIENTED_EDGE ( 'NONE', *, *, #14863, .T. ) ;
#32531=CIRCLE ( 'NONE', #33339, 16.00000000000000355 ) ;
#32540=PLANE ( 'NONE',  #12939 ) ;
#32543=EDGE_LOOP ( 'NONE', ( #22972, #38617, #4435, #7121 ) ) ;
#32547=CARTESIAN_POINT ( 'NONE',  ( 10.00000000000000000, -15.48615015657610883, 39.04073710021339139 ) ) ;
#32549=ORIENTED_EDGE ( 'NONE', *, *, #40656, .F. ) ;
#32552=DIRECTION ( 'NONE',  ( 0.000000000000000000, -0.8660254037844363761, -0.5000000000000039968 ) ) ;
#32555=LINE ( 'NONE', #25669, #12077 ) ;
#32562=PLANE ( 'NONE',  #16936 ) ;
#32567=LINE ( 'NONE', #13958, #48022 ) ;
#32579=DIRECTION ( 'NONE',  ( 1.000000000000000000, -0.000000000000000000, -0.000000000000000000 ) ) ;
#32582=ORIENTED_EDGE ( 'NONE', *, *, #25627, .F. ) ;
#32593=DIRECTION ( 'NONE',  ( 0.000000000000000000, -0.9135454576426056406, 0.4067366430757897722 ) ) ;
#32611=LINE ( 'NONE', #47536, #18697 ) ;
#32614=EDGE_CURVE ( 'NONE', #29381, #45887, #25448, .T. ) ;
#32620=DIRECTION ( 'NONE',  ( -1.000000000000000000, 0.000000000000000000, -0.000000000000000000 ) ) ;
#32623=DIRECTION ( 'NONE',  ( -1.000000000000000000, 0.000000000000000000, 0.000000000000000000 ) ) ;
#32624=CARTESIAN_POINT ( 'NONE',  ( 10.00000000000000000, 36.88895765772633695, 6.736453364083687667 ) ) ;
#32626=ADVANCED_FACE ( 'NONE', ( #31425 ), #46332, .T. ) ;
#32630=EDGE_LOOP ( 'NONE', ( #40539, #8428, #46019, #13209 ) ) ;
#32634=EDGE_CURVE ( 'NONE', #44307, #45913, #5231, .T. ) ;
#32637=VECTOR ( 'NONE', #9359, 1000.000000000000000 ) ;
#32644=EDGE_CURVE ( 'NONE', #19539, #26327, #1049, .T. ) ;
#32648=FACE_OUTER_BOUND ( 'NONE', #35848, .T. ) ;
#32649=PLANE ( 'NONE',  #30424 ) ;
#32654=VERTEX_POINT ( 'NONE', #31670 ) ;
#32655=ORIENTED_EDGE ( 'NONE', *, *, #22465, .T. ) ;
#32658=CARTESIAN_POINT ( 'NONE',  ( 10.00000000000000000, 37.01155633439059756, 6.555932627142549762 ) ) ;
#32659=FACE_OUTER_BOUND ( 'NONE', #26689, .T. ) ;
#32660=DIRECTION ( 'NONE',  ( -1.000000000000000000, -0.000000000000000000, -0.000000000000000000 ) ) ;
#32682=EDGE_CURVE ( 'NONE', #4718, #28097, #35796, .T. ) ;
#32699=DIRECTION ( 'NONE',  ( 0.000000000000000000, 0.000000000000000000, 1.000000000000000000 ) ) ;
#32708=ORIENTED_EDGE ( 'NONE', *, *, #43988, .T. ) ;
#32715=EDGE_CURVE ( 'NONE', #39388, #24628, #12972, .T. ) ;
#32716=VECTOR ( 'NONE', #27889, 1000.000000000000114 ) ;
#32723=PLANE ( 'NONE',  #47662 ) ;
#32733=LINE ( 'NONE', #9984, #39616 ) ;
#32734=CARTESIAN_POINT ( 'NONE',  ( -3.000000000000000000, -18.13022148937243472, -15.02647892043568767 ) ) ;
#32737=ORIENTED_EDGE ( 'NONE', *, *, #37861, .T. ) ;
#32741=ADVANCED_FACE ( 'NONE', ( #27988 ), #17672, .T. ) ;
#32744=CYLINDRICAL_SURFACE ( 'NONE', #9271, 42.00000000000000000 ) ;
#32747=VERTEX_POINT ( 'NONE', #21339 ) ;
#32759=DIRECTION ( 'NONE',  ( 0.000000000000000000, 0.000000000000000000, 1.000000000000000000 ) ) ;
#32764=ORIENTED_EDGE ( 'NONE', *, *, #28082, .T. ) ;
#32775=AXIS2_PLACEMENT_3D ( 'NONE', #39209, #843, #20348 ) ;
#32780=DIRECTION ( 'NONE',  ( -1.000000000000000000, -0.000000000000000000, 0.000000000000000000 ) ) ;
#32787=DIRECTION ( 'NONE',  ( 0.000000000000000000, 0.000000000000000000, 1.000000000000000000 ) ) ;
#32791=EDGE_LOOP ( 'NONE', ( #45588, #14761, #35967, #28020 ) ) ;
#32794=PLANE ( 'NONE',  #39347 ) ;
#32805=ORIENTED_EDGE ( 'NONE', *, *, #37402, .F. ) ;
#32810=ORIENTED_EDGE ( 'NONE', *, *, #4775, .F. ) ;
#32815=ORIENTED_EDGE ( 'NONE', *, *, #45259, .T. ) ;
#32816=DIRECTION ( 'NONE',  ( 0.000000000000000000, 0.000000000000000000, 1.000000000000000000 ) ) ;
#32818=CARTESIAN_POINT ( 'NONE',  ( 0.000000000000000000, 23.50000000000000000, 1.499999999999997780 ) ) ;
#32824=ORIENTED_EDGE ( 'NONE', *, *, #40304, .T. ) ;
#32828=ORIENTED_EDGE ( 'NONE', *, *, #32682, .T. ) ;
#32836=VERTEX_POINT ( 'NONE', #14974 ) ;
#32840=AXIS2_PLACEMENT_3D ( 'NONE', #21690, #47862, #32699 ) ;
#32846=VECTOR ( 'NONE', #29955, 1000.000000000000000 ) ;
#32853=VERTEX_POINT ( 'NONE', #33567 ) ;
#32860=CARTESIAN_POINT ( 'NONE',  ( 5.000000000000000000, 31.52238457039599595, 27.75498641678753842 ) ) ;
#32866=ORIENTED_EDGE ( 'NONE', *, *, #10310, .T. ) ;
#32871=CARTESIAN_POINT ( 'NONE',  ( 10.00000000000000000, -5.202137450156655518, 37.22597642581156663 ) ) ;
#32873=AXIS2_PLACEMENT_3D ( 'NONE', #3873, #4120, #1166 ) ;
#32876=FACE_OUTER_BOUND ( 'NONE', #23349, .T. ) ;
#32880=CARTESIAN_POINT ( 'NONE',  ( 0.000000000000000000, 37.58145647212455032, -0.6853352020786441789 ) ) ;
#32881=ORIENTED_EDGE ( 'NONE', *, *, #12291, .F. ) ;
#32885=CIRCLE ( 'NONE', #28220, 16.00000000000000000 ) ;
#32888=EDGE_LOOP ( 'NONE', ( #34760, #3944, #16101, #7612 ) ) ;
#32891=VERTEX_POINT ( 'NONE', #40922 ) ;
#32892=ORIENTED_EDGE ( 'NONE', *, *, #16625, .T. ) ;
#32894=DIRECTION ( 'NONE',  ( -1.000000000000000000, 0.000000000000000000, 0.000000000000000000 ) ) ;
#32901=CARTESIAN_POINT ( 'NONE',  ( 10.00000000000000000, -10.96151621346514382, 35.95386929396252640 ) ) ;
#32905=LINE ( 'NONE', #10159, #6826 ) ;
#32908=DIRECTION ( 'NONE',  ( 0.000000000000000000, 0.8090169943749486725, -0.5877852522924713607 ) ) ;
#32913=AXIS2_PLACEMENT_3D ( 'NONE', #45409, #7729, #4786 ) ;
#32925=EDGE_CURVE ( 'NONE', #26652, #15212, #12901, .T. ) ;
#32926=EDGE_CURVE ( 'NONE', #5723, #6467, #26982, .T. ) ;
#32946=CIRCLE ( 'NONE', #47039, 16.00000000000000000 ) ;
#32950=ORIENTED_EDGE ( 'NONE', *, *, #45035, .T. ) ;
#32955=ORIENTED_EDGE ( 'NONE', *, *, #5265, .F. ) ;
#32965=DIRECTION ( 'NONE',  ( 0.000000000000000000, 1.000000000000000000, 3.491481338843133750E-15 ) ) ;
#32966=ORIENTED_EDGE ( 'NONE', *, *, #15138, .T. ) ;
#32973=CARTESIAN_POINT ( 'NONE',  ( 10.00000000000000000, 12.42422080174639021, 35.38097989696516521 ) ) ;
#32977=DIRECTION ( 'NONE',  ( -1.000000000000000000, -0.000000000000000000, -0.000000000000000000 ) ) ;
#32978=EDGE_CURVE ( 'NONE', #5424, #17233, #529, .T. ) ;
#32981=CARTESIAN_POINT ( 'NONE',  ( -3.000000000000000000, -22.67460108101783334, 6.353146135317912169 ) ) ;
#32984=ORIENTED_EDGE ( 'NONE', *, *, #41255, .T. ) ;
#32992=VECTOR ( 'NONE', #29484, 1000.000000000000000 ) ;
#33004=DIRECTION ( 'NONE',  ( -1.000000000000000000, 0.000000000000000000, -0.000000000000000000 ) ) ;
#33011=ORIENTED_EDGE ( 'NONE', *, *, #46306, .F. ) ;
#33012=VERTEX_POINT ( 'NONE', #35014 ) ;
#33016=VECTOR ( 'NONE', #34449, 1000.000000000000000 ) ;
#33024=DIRECTION ( 'NONE',  ( 0.000000000000000000, 0.000000000000000000, 1.000000000000000000 ) ) ;
#33035=CARTESIAN_POINT ( 'NONE',  ( -3.000000000000000000, -0.9646360437375307573, 23.52805723605590060 ) ) ;
#33040=ORIENTED_EDGE ( 'NONE', *, *, #957, .T. ) ;
#33045=CIRCLE ( 'NONE', #36160, 16.00000000000000000 ) ;
#33056=CARTESIAN_POINT ( 'NONE',  ( -10.00000000000000000, 0.000000000000000000, 0.000000000000000000 ) ) ;
#33057=AXIS2_PLACEMENT_3D ( 'NONE', #16368, #937, #23457 ) ;
#33061=VERTEX_POINT ( 'NONE', #35251 ) ;
#33068=CYLINDRICAL_SURFACE ( 'NONE', #33095, 42.00000000000000000 ) ;
#33073=ORIENTED_EDGE ( 'NONE', *, *, #14432, .F. ) ;
#33074=FACE_OUTER_BOUND ( 'NONE', #27391, .T. ) ;
#33084=CIRCLE ( 'NONE', #47919, 16.00000000000000000 ) ;
#33088=AXIS2_PLACEMENT_3D ( 'NONE', #31322, #34472, #20041 ) ;
#33090=ORIENTED_EDGE ( 'NONE', *, *, #38451, .F. ) ;
#33095=AXIS2_PLACEMENT_3D ( 'NONE', #10808, #14483, #25715 ) ;
#33097=VECTOR ( 'NONE', #42008, 1000.000000000000000 ) ;
#33103=CARTESIAN_POINT ( 'NONE',  ( 10.00000000000000000, -12.26510123303234501, -35.53030884539098366 ) ) ;
#33118=ADVANCED_FACE ( 'NONE', ( #2210 ), #9538, .T. ) ;
#33129=VECTOR ( 'NONE', #44186, 1000.000000000000000 ) ;
#33133=CARTESIAN_POINT ( 'NONE',  ( 0.000000000000000000, 9.615535125378775305, 24.73947219025917121 ) ) ;
#33134=PLANE ( 'NONE',  #11663 ) ;
#33135=DIRECTION ( 'NONE',  ( -1.000000000000000000, -0.000000000000000000, 0.000000000000000000 ) ) ;
#33137=EDGE_CURVE ( 'NONE', #29574, #12245, #23852, .T. ) ;
#33138=VECTOR ( 'NONE', #36882, 1000.000000000000114 ) ;
#33140=ORIENTED_EDGE ( 'NONE', *, *, #1047, .T. ) ;
#33144=CIRCLE ( 'NONE', #22974, 16.00000000000000000 ) ;
#33145=FACE_OUTER_BOUND ( 'NONE', #1342, .T. ) ;
#33155=CARTESIAN_POINT ( 'NONE',  ( -3.000000000000000000, 6.762365576493310826, 25.66652317338401090 ) ) ;
#33157=DIRECTION ( 'NONE',  ( 0.000000000000000000, 0.4999999999999929501, 0.8660254037844427044 ) ) ;
#33163=LINE ( 'NONE', #48091, #34546 ) ;
#33164=CARTESIAN_POINT ( 'NONE',  ( -3.000000000000000000, 20.85821328998741109, 10.92862929874522315 ) ) ;
#33168=DIRECTION ( 'NONE',  ( 0.000000000000000000, 0.8910065241883688980, -0.4539904997395447506 ) ) ;
#33174=VECTOR ( 'NONE', #39719, 1000.000000000000000 ) ;
#33176=VERTEX_POINT ( 'NONE', #39675 ) ;
#33183=ORIENTED_EDGE ( 'NONE', *, *, #29787, .T. ) ;
#33186=CARTESIAN_POINT ( 'NONE',  ( 10.00000000000000000, -27.13269053701078448, -25.88420570971428702 ) ) ;
#33193=ORIENTED_EDGE ( 'NONE', *, *, #32399, .F. ) ;
#33198=FACE_OUTER_BOUND ( 'NONE', #16455, .T. ) ;
#33201=FACE_OUTER_BOUND ( 'NONE', #3784, .T. ) ;
#33202=ORIENTED_EDGE ( 'NONE', *, *, #13878, .T. ) ;
#33207=CARTESIAN_POINT ( 'NONE',  ( 0.000000000000000000, -10.74501242461307982, 35.92658777277507198 ) ) ;
#33209=CARTESIAN_POINT ( 'NONE',  ( -3.000000000000000000, 20.85821328998756385, -10.92862929874494959 ) ) ;
#33212=CARTESIAN_POINT ( 'NONE',  ( 0.000000000000000000, -16.45098606841102651, -33.79645857604531045 ) ) ;
#33214=DIRECTION ( 'NONE',  ( -1.000000000000000000, 0.000000000000000000, -0.000000000000000000 ) ) ;
#33216=VECTOR ( 'NONE', #46673, 999.9999999999998863 ) ;
#33229=DIRECTION ( 'NONE',  ( 0.000000000000000000, 1.000000000000000000, 7.228014483236689653E-16 ) ) ;
#33233=CARTESIAN_POINT ( 'NONE',  ( 10.00000000000000000, 16.45098606841126454, 33.79645857604518966 ) ) ;
#33243=EDGE_CURVE ( 'NONE', #27962, #33538, #37938, .T. ) ;
#33247=AXIS2_PLACEMENT_3D ( 'NONE', #17610, #32552, #47475 ) ;
#33248=ORIENTED_EDGE ( 'NONE', *, *, #36639, .T. ) ;
#33255=EDGE_CURVE ( 'NONE', #9753, #24727, #41065, .T. ) ;
#33256=DIRECTION ( 'NONE',  ( -1.000000000000000000, 0.000000000000000000, 0.000000000000000000 ) ) ;
#33271=DIRECTION ( 'NONE',  ( -1.000000000000000000, 0.000000000000000000, 0.000000000000000000 ) ) ;
#33296=VECTOR ( 'NONE', #28344, 1000.000000000000000 ) ;
#33298=EDGE_CURVE ( 'NONE', #45931, #17130, #6604, .T. ) ;
#33307=CIRCLE ( 'NONE', #20107, 16.00000000000000000 ) ;
#33315=CIRCLE ( 'NONE', #44258, 37.49900000000000233 ) ;
#33317=ADVANCED_FACE ( 'NONE', ( #40386 ), #38102, .F. ) ;
#33322=CARTESIAN_POINT ( 'NONE',  ( 10.00000000000000000, 0.000000000000000000, 0.000000000000000000 ) ) ;
#33325=CIRCLE ( 'NONE', #2853, 42.00000000000000000 ) ;
#33335=EDGE_CURVE ( 'NONE', #23424, #19153, #10265, .T. ) ;
#33339=AXIS2_PLACEMENT_3D ( 'NONE', #37712, #37230, #45296 ) ;
#33366=EDGE_LOOP ( 'NONE', ( #14272, #32866, #12712, #38669 ) ) ;
#33370=FACE_OUTER_BOUND ( 'NONE', #32543, .T. ) ;
#33381=CARTESIAN_POINT ( 'NONE',  ( 0.000000000000000000, 6.736453364084091788, -36.88895765772625879 ) ) ;
#33387=CARTESIAN_POINT ( 'NONE',  ( 0.000000000000000000, -22.67460108101783334, 6.353146135317912169 ) ) ;
#33389=EDGE_LOOP ( 'NONE', ( #1592, #17760, #13518, #32966 ) ) ;
#33391=CYLINDRICAL_SURFACE ( 'NONE', #20732, 16.00000000000000000 ) ;
#33394=CARTESIAN_POINT ( 'NONE',  ( 10.00000000000000000, -6.555932627142676772, 37.01155633439056203 ) ) ;
#33399=DIRECTION ( 'NONE',  ( 0.000000000000000000, -0.7071067811865389130, -0.7071067811865563435 ) ) ;
#33411=CARTESIAN_POINT ( 'NONE',  ( 0.000000000000000000, 0.000000000000000000, 0.000000000000000000 ) ) ;
#33427=DIRECTION ( 'NONE',  ( 0.000000000000000000, -0.5877852522924797984, 0.8090169943749426773 ) ) ;
#33430=VERTEX_POINT ( 'NONE', #1125 ) ;
#33435=EDGE_CURVE ( 'NONE', #41033, #23667, #27819, .T. ) ;
#33443=ORIENTED_EDGE ( 'NONE', *, *, #43976, .T. ) ;
#33444=CYLINDRICAL_SURFACE ( 'NONE', #21483, 16.00000000000000000 ) ;
#33455=CYLINDRICAL_SURFACE ( 'NONE', #14985, 16.00000000000000000 ) ;
#33458=CARTESIAN_POINT ( 'NONE',  ( -3.000000000000000000, -10.45096189432344147, 21.10159698893426494 ) ) ;
#33459=VECTOR ( 'NONE', #43880, 1000.000000000000000 ) ;
#33460=DIRECTION ( 'NONE',  ( 1.000000000000000000, -0.000000000000000000, 0.000000000000000000 ) ) ;
#33461=CARTESIAN_POINT ( 'NONE',  ( 4.999999999999999112, 21.40280677340371795, 36.13751322684426270 ) ) ;
#33465=DIRECTION ( 'NONE',  ( -1.000000000000000000, 0.000000000000000000, 0.000000000000000000 ) ) ;
#33471=AXIS2_PLACEMENT_3D ( 'NONE', #29045, #22437, #10447 ) ;
#33478=LINE ( 'NONE', #34430, #43692 ) ;
#33491=FACE_OUTER_BOUND ( 'NONE', #30394, .T. ) ;
#33498=EDGE_CURVE ( 'NONE', #7846, #29919, #12197, .T. ) ;
#33505=DIRECTION ( 'NONE',  ( -1.000000000000000000, 0.000000000000000000, -0.000000000000000000 ) ) ;
#33506=LINE ( 'NONE', #37186, #37925 ) ;
#33517=CYLINDRICAL_SURFACE ( 'NONE', #26933, 42.00000000000000000 ) ;
#33524=EDGE_CURVE ( 'NONE', #24727, #36078, #9923, .T. ) ;
#33528=DIRECTION ( 'NONE',  ( -1.000000000000000000, 0.000000000000000000, 0.000000000000000000 ) ) ;
#33534=EDGE_CURVE ( 'NONE', #17233, #19561, #2809, .T. ) ;
#33538=VERTEX_POINT ( 'NONE', #10653 ) ;
#33546=EDGE_CURVE ( 'NONE', #4028, #14988, #3551, .T. ) ;
#33554=DIRECTION ( 'NONE',  ( 0.000000000000000000, 0.000000000000000000, 1.000000000000000000 ) ) ;
#33558=VERTEX_POINT ( 'NONE', #40275 ) ;
#33561=ORIENTED_EDGE ( 'NONE', *, *, #9033, .T. ) ;
#33562=DIRECTION ( 'NONE',  ( 0.000000000000000000, 0.3090169943749482839, -0.9510565162951533091 ) ) ;
#33563=EDGE_LOOP ( 'NONE', ( #40276, #13739, #5139, #2940 ) ) ;
#33567=CARTESIAN_POINT ( 'NONE',  ( 0.000000000000000000, 6.762365576493310826, 25.66652317338401090 ) ) ;
#33569=PLANE ( 'NONE',  #24271 ) ;
#33576=CARTESIAN_POINT ( 'NONE',  ( 0.000000000000000000, -14.54903810567645372, -22.19967320028775504 ) ) ;
#33582=DIRECTION ( 'NONE',  ( -1.000000000000000000, 0.000000000000000000, 0.000000000000000000 ) ) ;
#33588=CIRCLE ( 'NONE', #32042, 15.99999999999999645 ) ;
#33598=EDGE_CURVE ( 'NONE', #20241, #21733, #43466, .T. ) ;
#33602=DIRECTION ( 'NONE',  ( 1.000000000000000000, 0.000000000000000000, -0.000000000000000000 ) ) ;
#33606=ORIENTED_EDGE ( 'NONE', *, *, #16700, .T. ) ;
#33621=ORIENTED_EDGE ( 'NONE', *, *, #21441, .F. ) ;
#33630=LINE ( 'NONE', #2383, #17576 ) ;
#33632=CARTESIAN_POINT ( 'NONE',  ( -3.000000000000000000, -3.948201729842348850, 23.21447184625293048 ) ) ;
#33652=VERTEX_POINT ( 'NONE', #15521 ) ;
#33660=DIRECTION ( 'NONE',  ( 0.000000000000000000, 0.000000000000000000, 1.000000000000000000 ) ) ;
#33662=ORIENTED_EDGE ( 'NONE', *, *, #22653, .F. ) ;
#33663=EDGE_LOOP ( 'NONE', ( #9458, #33671, #1353, #24223 ) ) ;
#33665=CARTESIAN_POINT ( 'NONE',  ( 5.000000000000000000, -16.65560815589439159, 38.55633173627004595 ) ) ;
#33671=ORIENTED_EDGE ( 'NONE', *, *, #27370, .F. ) ;
#33672=DIRECTION ( 'NONE',  ( -1.000000000000000000, -0.000000000000000000, 0.000000000000000000 ) ) ;
#33673=FACE_OUTER_BOUND ( 'NONE', #29291, .T. ) ;
#33676=DIRECTION ( 'NONE',  ( 0.000000000000000000, -0.7071067811865389130, -0.7071067811865561215 ) ) ;
#33683=EDGE_LOOP ( 'NONE', ( #2256, #40525, #6735, #43727 ) ) ;
#33687=EDGE_LOOP ( 'NONE', ( #46800, #45727, #2921, #27289 ) ) ;
#33691=VECTOR ( 'NONE', #45002, 1000.000000000000114 ) ;
#33706=EDGE_CURVE ( 'NONE', #11474, #35410, #29719, .T. ) ;
#33710=FACE_OUTER_BOUND ( 'NONE', #8431, .T. ) ;
#33725=CARTESIAN_POINT ( 'NONE',  ( -10.00000000000000000, 0.000000000000000000, 0.000000000000000000 ) ) ;
#33739=CARTESIAN_POINT ( 'NONE',  ( 0.000000000000000000, -10.96151621346461447, -35.95386929396268272 ) ) ;
#33744=LINE ( 'NONE', #26425, #179 ) ;
#33751=VERTEX_POINT ( 'NONE', #40995 ) ;
#33757=EDGE_CURVE ( 'NONE', #31567, #32256, #40508, .T. ) ;
#33765=EDGE_CURVE ( 'NONE', #19183, #14880, #47338, .T. ) ;
#33778=AXIS2_PLACEMENT_3D ( 'NONE', #28380, #36911, #7062 ) ;
#33781=CARTESIAN_POINT ( 'NONE',  ( 4.999999999999999112, -2.663952781846440576, 41.91543099594817789 ) ) ;
#33782=ORIENTED_EDGE ( 'NONE', *, *, #26246, .F. ) ;
#33784=VERTEX_POINT ( 'NONE', #23343 ) ;
#33789=DIRECTION ( 'NONE',  ( 1.000000000000000000, 0.000000000000000000, 0.000000000000000000 ) ) ;
#33801=EDGE_CURVE ( 'NONE', #28193, #13250, #35082, .T. ) ;
#33803=EDGE_CURVE ( 'NONE', #34159, #22253, #44994, .T. ) ;
#33806=LINE ( 'NONE', #48019, #1257 ) ;
#33813=AXIS2_PLACEMENT_3D ( 'NONE', #22501, #6845, #17847 ) ;
#33817=AXIS2_PLACEMENT_3D ( 'NONE', #43423, #6696, #18163 ) ;
#33820=AXIS2_PLACEMENT_3D ( 'NONE', #31196, #1328, #23841 ) ;
#33826=LINE ( 'NONE', #12535, #31504 ) ;
#33831=CIRCLE ( 'NONE', #11164, 16.00000000000000000 ) ;
#33835=AXIS2_PLACEMENT_3D ( 'NONE', #37810, #34358, #15537 ) ;
#33837=ORIENTED_EDGE ( 'NONE', *, *, #29501, .F. ) ;
#33838=EDGE_CURVE ( 'NONE', #29381, #41954, #12236, .T. ) ;
#33855=AXIS2_PLACEMENT_3D ( 'NONE', #36400, #40333, #39840 ) ;
#33861=DIRECTION ( 'NONE',  ( 0.000000000000000000, 0.9876883405951381034, -0.1564344650402276216 ) ) ;
#33865=CARTESIAN_POINT ( 'NONE',  ( 10.00000000000000000, 37.58145647212453611, 0.6853352020791767529 ) ) ;
#33873=EDGE_CURVE ( 'NONE', #6771, #33652, #5986, .T. ) ;
#33876=DIRECTION ( 'NONE',  ( 0.000000000000000000, 0.8660254037844359321, 0.5000000000000046629 ) ) ;
#33880=DIRECTION ( 'NONE',  ( -1.000000000000000000, 0.000000000000000000, -0.000000000000000000 ) ) ;
#33891=AXIS2_PLACEMENT_3D ( 'NONE', #27709, #42642, #9101 ) ;
#33896=CARTESIAN_POINT ( 'NONE',  ( -3.000000000000000000, 22.07842321921481243, 8.187992925817422218 ) ) ;
#33897=LINE ( 'NONE', #34610, #13301 ) ;
#33905=CARTESIAN_POINT ( 'NONE',  ( 10.00000000000000000, 30.80686688397041451, -21.53537804866048688 ) ) ;
#33909=ORIENTED_EDGE ( 'NONE', *, *, #32715, .T. ) ;
#33920=LINE ( 'NONE', #36633, #8433 ) ;
#33932=DIRECTION ( 'NONE',  ( -1.000000000000000000, -0.000000000000000000, 0.000000000000000000 ) ) ;
#33934=DIRECTION ( 'NONE',  ( -1.000000000000000000, 0.000000000000000000, 0.000000000000000000 ) ) ;
#33941=CARTESIAN_POINT ( 'NONE',  ( 10.00000000000000000, -35.38097989696503021, -12.42422080174676147 ) ) ;
#33947=ORIENTED_EDGE ( 'NONE', *, *, #28618, .F. ) ;
#33981=EDGE_CURVE ( 'NONE', #47549, #8466, #33315, .T. ) ;
#33983=ORIENTED_EDGE ( 'NONE', *, *, #42033, .T. ) ;
#33986=ORIENTED_EDGE ( 'NONE', *, *, #48049, .F. ) ;
#33991=LINE ( 'NONE', #22504, #1948 ) ;
#33994=DIRECTION ( 'NONE',  ( 0.000000000000000000, 0.3090169943749580539, -0.9510565162951500895 ) ) ;
#33999=CARTESIAN_POINT ( 'NONE',  ( -3.000000000000000000, -19.89357724624987256, -12.59942793731086041 ) ) ;
#34006=CIRCLE ( 'NONE', #9801, 15.99999999999999822 ) ;
#34011=CARTESIAN_POINT ( 'NONE',  ( 10.00000000000000000, 22.64427369931212297, -30.00120703465181293 ) ) ;
#34014=ADVANCED_FACE ( 'NONE', ( #31925 ), #13298, .T. ) ;
#34040=AXIS2_PLACEMENT_3D ( 'NONE', #1535, #13509, #5217 ) ;
#34041=AXIS2_PLACEMENT_3D ( 'NONE', #6894, #25488, #47748 ) ;
#34043=DIRECTION ( 'NONE',  ( -1.000000000000000000, 0.000000000000000000, 0.000000000000000000 ) ) ;
#34045=EDGE_LOOP ( 'NONE', ( #39013, #41270, #47820, #1300 ) ) ;
#34053=AXIS2_PLACEMENT_3D ( 'NONE', #26764, #34569, #27747 ) ;
#34058=DIRECTION ( 'NONE',  ( 0.000000000000000000, -0.9510565162951565288, 0.3090169943749383474 ) ) ;
#34079=CARTESIAN_POINT ( 'NONE',  ( -3.000000000000000000, -13.04903810567647682, -19.60159698893442481 ) ) ;
#34087=EDGE_CURVE ( 'NONE', #21133, #36907, #2814, .T. ) ;
#34090=ORIENTED_EDGE ( 'NONE', *, *, #34087, .F. ) ;
#34095=DIRECTION ( 'NONE',  ( 0.000000000000000000, 0.000000000000000000, 1.000000000000000000 ) ) ;
#34103=ORIENTED_EDGE ( 'NONE', *, *, #6752, .T. ) ;
#34119=CARTESIAN_POINT ( 'NONE',  ( 10.00000000000000178, 0.000000000000000000, 21.00000000000000000 ) ) ;
#34137=EDGE_CURVE ( 'NONE', #27337, #26404, #33806, .T. ) ;
#34138=ORIENTED_EDGE ( 'NONE', *, *, #2813, .T. ) ;
#34143=AXIS2_PLACEMENT_3D ( 'NONE', #27312, #38321, #37837 ) ;
#34152=DIRECTION ( 'NONE',  ( -1.000000000000000000, 0.000000000000000000, 0.000000000000000000 ) ) ;
#34159=VERTEX_POINT ( 'NONE', #279 ) ;
#34168=DIRECTION ( 'NONE',  ( 0.000000000000000000, -0.4999999999999913403, -0.8660254037844435926 ) ) ;
#34171=VERTEX_POINT ( 'NONE', #15235 ) ;
#34175=VERTEX_POINT ( 'NONE', #11559 ) ;
#34176=ORIENTED_EDGE ( 'NONE', *, *, #48208, .T. ) ;
#34186=DIRECTION ( 'NONE',  ( 0.000000000000000000, -0.5877852522924802425, 0.8090169943749422332 ) ) ;
#34191=VECTOR ( 'NONE', #11795, 1000.000000000000000 ) ;
#34195=ORIENTED_EDGE ( 'NONE', *, *, #25405, .T. ) ;
#34196=CARTESIAN_POINT ( 'NONE',  ( -10.00000000000000000, 0.000000000000000000, 0.000000000000000000 ) ) ;
#34198=CARTESIAN_POINT ( 'NONE',  ( -3.000000000000000000, 24.81905959214275370, -9.408202855044498492 ) ) ;
#34200=VECTOR ( 'NONE', #2007, 1000.000000000000000 ) ;
#34202=DIRECTION ( 'NONE',  ( -1.000000000000000000, 0.000000000000000000, -0.000000000000000000 ) ) ;
#34205=EDGE_LOOP ( 'NONE', ( #29418, #45472, #29591, #16416 ) ) ;
#34207=CARTESIAN_POINT ( 'NONE',  ( -3.000000000000000000, 8.688484142254221609, -21.88630264137359660 ) ) ;
#34210=VERTEX_POINT ( 'NONE', #12521 ) ;
#34214=CARTESIAN_POINT ( 'NONE',  ( 5.000000000000000000, 22.48208911017551870, -35.47612816024499693 ) ) ;
#34226=CARTESIAN_POINT ( 'NONE',  ( 0.000000000000000000, 37.58145647212453611, 16.68533520207917675 ) ) ;
#34229=CARTESIAN_POINT ( 'NONE',  ( 4.999999999999999112, 41.81611651403868990, -3.925862922255709542 ) ) ;
#34233=DIRECTION ( 'NONE',  ( 1.000000000000000000, 0.000000000000000000, 0.000000000000000000 ) ) ;
#34237=EDGE_CURVE ( 'NONE', #30209, #38886, #20040, .T. ) ;
#34238=DIRECTION ( 'NONE',  ( 0.000000000000000000, 0.000000000000000000, 1.000000000000000000 ) ) ;
#34241=ORIENTED_EDGE ( 'NONE', *, *, #33137, .F. ) ;
#34264=DIRECTION ( 'NONE',  ( -1.000000000000000000, 0.000000000000000000, 0.000000000000000000 ) ) ;
#34268=ORIENTED_EDGE ( 'NONE', *, *, #26607, .F. ) ;
#34278=DIRECTION ( 'NONE',  ( 0.000000000000000000, 0.000000000000000000, -1.000000000000000000 ) ) ;
#34291=LINE ( 'NONE', #4686, #2792 ) ;
#34296=CARTESIAN_POINT ( 'NONE',  ( 10.00000000000000000, -17.80606268964516659, -33.00180498840066434 ) ) ;
#34302=ORIENTED_EDGE ( 'NONE', *, *, #45252, .F. ) ;
#34308=EDGE_LOOP ( 'NONE', ( #28754, #13138, #10095, #26019 ) ) ;
#34311=CARTESIAN_POINT ( 'NONE',  ( 10.00000000000000000, -10.74501242461308159, 35.92658777277507909 ) ) ;
#34316=CARTESIAN_POINT ( 'NONE',  ( 10.00000000000000000, -17.80606268964516659, -33.00180498840066434 ) ) ;
#34320=EDGE_LOOP ( 'NONE', ( #28232, #43830, #42148, #12794 ) ) ;
#34324=CYLINDRICAL_SURFACE ( 'NONE', #3084, 16.00000000000000000 ) ;
#34331=CARTESIAN_POINT ( 'NONE',  ( -3.000000000000000000, -22.67460108101774807, -6.353146135318215038 ) ) ;
#34335=DIRECTION ( 'NONE',  ( -1.000000000000000000, 0.000000000000000000, 0.000000000000000000 ) ) ;
#34340=DIRECTION ( 'NONE',  ( 0.000000000000000000, 0.000000000000000000, -1.000000000000000000 ) ) ;
#34358=DIRECTION ( 'NONE',  ( -1.000000000000000000, 0.000000000000000000, 0.000000000000000000 ) ) ;
#34362=ADVANCED_FACE ( 'NONE', ( #35262 ), #17619, .T. ) ;
#34369=DIRECTION ( 'NONE',  ( 0.000000000000000000, -0.4067366430758010409, 0.9135454576426005335 ) ) ;
#34372=DIRECTION ( 'NONE',  ( 0.000000000000000000, 0.000000000000000000, -1.000000000000000000 ) ) ;
#34373=CIRCLE ( 'NONE', #10180, 16.00000000000000000 ) ;
#34386=CARTESIAN_POINT ( 'NONE',  ( 0.000000000000000000, 16.83928648764945279, -16.46020748918028076 ) ) ;
#34389=CARTESIAN_POINT ( 'NONE',  ( 0.000000000000000000, 0.8828120875905820508, -37.48860685352290290 ) ) ;
#34391=CARTESIAN_POINT ( 'NONE',  ( 0.000000000000000000, 5.202137450156389953, 37.22597642581160216 ) ) ;
#34392=CARTESIAN_POINT ( 'NONE',  ( 10.00000000000000000, 25.88420570971438650, -27.13269053701069566 ) ) ;
#34403=EDGE_CURVE ( 'NONE', #36833, #24283, #24491, .T. ) ;
#34406=CARTESIAN_POINT ( 'NONE',  ( 10.00000000000000000, -26.08949754953005495, -27.05870788708258701 ) ) ;
#34408=CIRCLE ( 'NONE', #42254, 16.00000000000000000 ) ;
#34413=CIRCLE ( 'NONE', #32105, 16.00000000000000000 ) ;
#34419=ADVANCED_FACE ( 'NONE', ( #28652 ), #32562, .F. ) ;
#34427=EDGE_LOOP ( 'NONE', ( #11427, #6837, #1701, #394 ) ) ;
#34429=EDGE_CURVE ( 'NONE', #31590, #34673, #1994, .T. ) ;
#34430=CARTESIAN_POINT ( 'NONE',  ( 10.00000000000000000, -33.80338159004273280, -16.23288003029533044 ) ) ;
#34431=ORIENTED_EDGE ( 'NONE', *, *, #11715, .T. ) ;
#34448=CYLINDRICAL_SURFACE ( 'NONE', #40100, 37.49900000000000233 ) ;
#34449=DIRECTION ( 'NONE',  ( 1.000000000000000000, -0.000000000000000000, -0.000000000000000000 ) ) ;
#34453=AXIS2_PLACEMENT_3D ( 'NONE', #18338, #25670, #472 ) ;
#34459=ADVANCED_FACE ( 'NONE', ( #18089 ), #36467, .F. ) ;
#34461=EDGE_LOOP ( 'NONE', ( #2294, #29693, #29738, #10437 ) ) ;
#34470=CARTESIAN_POINT ( 'NONE',  ( 10.00000000000000000, 0.000000000000000000, 0.000000000000000000 ) ) ;
#34472=DIRECTION ( 'NONE',  ( -1.000000000000000000, -0.000000000000000000, -0.000000000000000000 ) ) ;
#34477=AXIS2_PLACEMENT_3D ( 'NONE', #5708, #13530, #20631 ) ;
#34481=ORIENTED_EDGE ( 'NONE', *, *, #13861, .T. ) ;
#34485=LINE ( 'NONE', #7595, #23741 ) ;
#34489=AXIS2_PLACEMENT_3D ( 'NONE', #335, #27025, #15513 ) ;
#34493=EDGE_LOOP ( 'NONE', ( #31242, #34565, #41145, #19864 ) ) ;
#34495=VERTEX_POINT ( 'NONE', #3661 ) ;
#34502=DIRECTION ( 'NONE',  ( 0.000000000000000000, 0.000000000000000000, 1.000000000000000000 ) ) ;
#34511=CIRCLE ( 'NONE', #36104, 16.00000000000000355 ) ;
#34514=ORIENTED_EDGE ( 'NONE', *, *, #46306, .T. ) ;
#34520=CARTESIAN_POINT ( 'NONE',  ( -3.000000000000000000, 24.81905959214261514, 9.408202855044825341 ) ) ;
#34526=FACE_OUTER_BOUND ( 'NONE', #14644, .T. ) ;
#34530=CARTESIAN_POINT ( 'NONE',  ( -3.000000000000000000, 8.688484142253939169, 21.88630264137371029 ) ) ;
#34534=AXIS2_PLACEMENT_3D ( 'NONE', #43022, #38380, #39104 ) ;
#34542=ORIENTED_EDGE ( 'NONE', *, *, #25950, .T. ) ;
#34546=VECTOR ( 'NONE', #17974, 1000.000000000000000 ) ;
#34547=AXIS2_PLACEMENT_3D ( 'NONE', #27929, #1975, #13457 ) ;
#34555=EDGE_LOOP ( 'NONE', ( #43223, #32107, #8565, #15678 ) ) ;
#34558=ORIENTED_EDGE ( 'NONE', *, *, #19161, .F. ) ;
#34565=ORIENTED_EDGE ( 'NONE', *, *, #46940, .F. ) ;
#34567=ORIENTED_EDGE ( 'NONE', *, *, #20268, .T. ) ;
#34569=DIRECTION ( 'NONE',  ( 1.000000000000000000, 0.000000000000000000, 0.000000000000000000 ) ) ;
#34583=DIRECTION ( 'NONE',  ( 0.000000000000000000, -0.7071067811865535679, 0.7071067811865413555 ) ) ;
#34590=DIRECTION ( 'NONE',  ( -1.000000000000000000, 0.000000000000000000, 0.000000000000000000 ) ) ;
#34607=AXIS2_PLACEMENT_3D ( 'NONE', #4913, #4676, #34278 ) ;
#34608=ADVANCED_FACE ( 'NONE', ( #30344 ), #26429, .T. ) ;
#34610=CARTESIAN_POINT ( 'NONE',  ( 0.000000000000000000, 26.50000000000000000, -1.500000000000001332 ) ) ;
#34624=ORIENTED_EDGE ( 'NONE', *, *, #36484, .F. ) ;
#34630=DIRECTION ( 'NONE',  ( -1.000000000000000000, 0.000000000000000000, 0.000000000000000000 ) ) ;
#34632=DIRECTION ( 'NONE',  ( 0.000000000000000000, -0.4539904997395542430, 0.8910065241883641241 ) ) ;
#34638=LINE ( 'NONE', #34392, #47872 ) ;
#34642=DIRECTION ( 'NONE',  ( 0.000000000000000000, 0.000000000000000000, 1.000000000000000000 ) ) ;
#34646=VERTEX_POINT ( 'NONE', #7811 ) ;
#34653=CARTESIAN_POINT ( 'NONE',  ( 0.000000000000000000, -30.80686688396994910, -21.53537804866113703 ) ) ;
#34656=ORIENTED_EDGE ( 'NONE', *, *, #27077, .T. ) ;
#34671=ORIENTED_EDGE ( 'NONE', *, *, #22816, .F. ) ;
#34673=VERTEX_POINT ( 'NONE', #42080 ) ;
#34694=DIRECTION ( 'NONE',  ( 0.000000000000000000, 0.000000000000000000, 1.000000000000000000 ) ) ;
#34697=DIRECTION ( 'NONE',  ( 0.000000000000000000, 0.000000000000000000, 1.000000000000000000 ) ) ;
#34698=CARTESIAN_POINT ( 'NONE',  ( 10.00000000000000000, 0.000000000000000000, 0.000000000000000000 ) ) ;
#34702=EDGE_CURVE ( 'NONE', #6878, #21795, #23708, .T. ) ;
#34706=CIRCLE ( 'NONE', #30818, 16.00000000000000000 ) ;
#34707=EDGE_LOOP ( 'NONE', ( #5403, #34542, #32984, #45187 ) ) ;
#34713=DIRECTION ( 'NONE',  ( -1.000000000000000000, -0.000000000000000000, -0.000000000000000000 ) ) ;
#34719=EDGE_CURVE ( 'NONE', #41352, #43656, #15888, .T. ) ;
#34720=DIRECTION ( 'NONE',  ( -0.000000000000000000, 0.8090169943749504489, -0.5877852522924689183 ) ) ;
#34734=EDGE_LOOP ( 'NONE', ( #15845, #15656, #43793, #3509 ) ) ;
#34742=EDGE_CURVE ( 'NONE', #28319, #12709, #34923, .T. ) ;
#34745=ORIENTED_EDGE ( 'NONE', *, *, #13504, .T. ) ;
#34750=ORIENTED_EDGE ( 'NONE', *, *, #18933, .T. ) ;
#34760=ORIENTED_EDGE ( 'NONE', *, *, #41955, .F. ) ;
#34769=CIRCLE ( 'NONE', #18379, 15.99999999999999822 ) ;
#34776=LINE ( 'NONE', #42625, #43849 ) ;
#34782=LINE ( 'NONE', #5657, #3689 ) ;
#34784=VECTOR ( 'NONE', #16793, 1000.000000000000000 ) ;
#34791=ORIENTED_EDGE ( 'NONE', *, *, #21977, .F. ) ;
#34800=EDGE_CURVE ( 'NONE', #35770, #1468, #41204, .T. ) ;
#34806=ORIENTED_EDGE ( 'NONE', *, *, #48287, .T. ) ;
#34808=VECTOR ( 'NONE', #40254, 1000.000000000000000 ) ;
#34810=EDGE_CURVE ( 'NONE', #10117, #39461, #14641, .T. ) ;
#34811=CARTESIAN_POINT ( 'NONE',  ( -3.000000000000000000, 16.83928648764923253, 16.46020748918050458 ) ) ;
#34818=DIRECTION ( 'NONE',  ( -1.000000000000000000, 0.000000000000000000, 0.000000000000000000 ) ) ;
#34820=AXIS2_PLACEMENT_3D ( 'NONE', #41882, #19566, #34502 ) ;
#34821=FACE_OUTER_BOUND ( 'NONE', #41378, .T. ) ;
#34824=DIRECTION ( 'NONE',  ( 0.000000000000000000, 0.000000000000000000, 1.000000000000000000 ) ) ;
#34829=CARTESIAN_POINT ( 'NONE',  ( 0.000000000000000000, -14.54903810567645195, -22.19967320028775504 ) ) ;
#34831=DIRECTION ( 'NONE',  ( 0.000000000000000000, -0.8090169943749403458, -0.5877852522924830181 ) ) ;
#34842=AXIS2_PLACEMENT_3D ( 'NONE', #2447, #12522, #32323 ) ;
#34843=CARTESIAN_POINT ( 'NONE',  ( 10.00000000000000000, 21.32104025579158701, -30.84782396557194772 ) ) ;
#34846=PLANE ( 'NONE',  #33820 ) ;
#34850=CARTESIAN_POINT ( 'NONE',  ( 0.000000000000000000, -16.65560815589383381, -38.55633173627028754 ) ) ;
#34857=CARTESIAN_POINT ( 'NONE',  ( 0.000000000000000000, 5.835314593368477354, 22.81335362449854642 ) ) ;
#34858=VECTOR ( 'NONE', #38266, 1000.000000000000000 ) ;
#34865=AXIS2_PLACEMENT_3D ( 'NONE', #2967, #9586, #39720 ) ;
#34866=ORIENTED_EDGE ( 'NONE', *, *, #35532, .T. ) ;
#34868=EDGE_CURVE ( 'NONE', #1357, #31567, #32511, .T. ) ;
#34870=CARTESIAN_POINT ( 'NONE',  ( 10.00000000000000000, 35.92658777277511462, 10.74501242461295014 ) ) ;
#34872=DIRECTION ( 'NONE',  ( 0.000000000000000000, -1.000000000000000000, -1.040834085586084257E-14 ) ) ;
#34873=ORIENTED_EDGE ( 'NONE', *, *, #14421, .F. ) ;
#34875=EDGE_CURVE ( 'NONE', #33538, #33012, #32265, .T. ) ;
#34877=ORIENTED_EDGE ( 'NONE', *, *, #6339, .F. ) ;
#34884=DIRECTION ( 'NONE',  ( 1.000000000000000000, -0.000000000000000000, -0.000000000000000000 ) ) ;
#34886=LINE ( 'NONE', #27806, #13734 ) ;
#34896=CARTESIAN_POINT ( 'NONE',  ( 0.000000000000000000, 0.000000000000000000, 0.000000000000000000 ) ) ;
#34899=EDGE_LOOP ( 'NONE', ( #15087, #14232, #6746, #24874 ) ) ;
#34900=VERTEX_POINT ( 'NONE', #47189 ) ;
#34906=CIRCLE ( 'NONE', #35684, 16.00000000000000000 ) ;
#34913=LINE ( 'NONE', #38345, #26385 ) ;
#34922=EDGE_CURVE ( 'NONE', #28193, #38831, #16247, .T. ) ;
#34923=CIRCLE ( 'NONE', #13838, 16.00000000000000000 ) ;
#34938=AXIS2_PLACEMENT_3D ( 'NONE', #2571, #17978, #29255 ) ;
#34941=CARTESIAN_POINT ( 'NONE',  ( 10.00000000000000000, 37.16516213103277977, 4.992566952385115719 ) ) ;
#34947=CARTESIAN_POINT ( 'NONE',  ( 10.00000000000000000, 0.000000000000000000, 0.000000000000000000 ) ) ;
#34954=CIRCLE ( 'NONE', #31877, 16.00000000000000000 ) ;
#34960=CARTESIAN_POINT ( 'NONE',  ( 10.00000000000000000, -17.80606268964563554, 33.00180498840040855 ) ) ;
#34964=DIRECTION ( 'NONE',  ( -1.000000000000000000, -0.000000000000000000, 0.000000000000000000 ) ) ;
#34970=ORIENTED_EDGE ( 'NONE', *, *, #43381, .T. ) ;
#34977=VERTEX_POINT ( 'NONE', #32973 ) ;
#34980=DIRECTION ( 'NONE',  ( 0.000000000000000000, -0.4539904997395351471, -0.8910065241883737830 ) ) ;
#34996=ORIENTED_EDGE ( 'NONE', *, *, #14758, .T. ) ;
#35000=CARTESIAN_POINT ( 'NONE',  ( 0.000000000000000000, 16.65560815589411092, 38.55633173627015253 ) ) ;
#35001=LINE ( 'NONE', #47229, #19976 ) ;
#35014=CARTESIAN_POINT ( 'NONE',  ( 0.000000000000000000, -32.34446384429989507, 26.79245525562703278 ) ) ;
#35027=EDGE_CURVE ( 'NONE', #40610, #20645, #46721, .T. ) ;
#35028=DIRECTION ( 'NONE',  ( 0.000000000000000000, 0.000000000000000000, 1.000000000000000000 ) ) ;
#35029=CARTESIAN_POINT ( 'NONE',  ( 0.000000000000000000, 35.92658777277510040, 10.74501242461294659 ) ) ;
#35030=CARTESIAN_POINT ( 'NONE',  ( 0.000000000000000000, 0.000000000000000000, 0.000000000000000000 ) ) ;
#35032=CARTESIAN_POINT ( 'NONE',  ( -3.000000000000000000, 16.83928648764923253, 16.46020748918050458 ) ) ;
#35036=ORIENTED_EDGE ( 'NONE', *, *, #9546, .T. ) ;
#35047=ORIENTED_EDGE ( 'NONE', *, *, #38770, .T. ) ;
#35052=ORIENTED_EDGE ( 'NONE', *, *, #30500, .T. ) ;
#35053=CARTESIAN_POINT ( 'NONE',  ( -3.000000000000000000, -13.04903810567675038, 19.60159698893425428 ) ) ;
#35055=VERTEX_POINT ( 'NONE', #38342 ) ;
#35057=VECTOR ( 'NONE', #46945, 1000.000000000000000 ) ;
#35062=FACE_OUTER_BOUND ( 'NONE', #34427, .T. ) ;
#35064=DIRECTION ( 'NONE',  ( 0.000000000000000000, -0.6691306063588577935, -0.7431448254773946882 ) ) ;
#35069=ORIENTED_EDGE ( 'NONE', *, *, #39638, .T. ) ;
#35073=CARTESIAN_POINT ( 'NONE',  ( 10.00000000000000000, 30.80686688397010542, 21.53537804866092387 ) ) ;
#35075=ORIENTED_EDGE ( 'NONE', *, *, #23956, .F. ) ;
#35082=LINE ( 'NONE', #34843, #11399 ) ;
#35107=ORIENTED_EDGE ( 'NONE', *, *, #9608, .F. ) ;
#35118=CARTESIAN_POINT ( 'NONE',  ( 10.00000000000000000, -17.67226234102801286, -33.17418723428327354 ) ) ;
#35119=ORIENTED_EDGE ( 'NONE', *, *, #4240, .T. ) ;
#35128=ORIENTED_EDGE ( 'NONE', *, *, #29570, .T. ) ;
#35131=DIRECTION ( 'NONE',  ( -1.000000000000000000, 0.000000000000000000, 0.000000000000000000 ) ) ;
#35143=CARTESIAN_POINT ( 'NONE',  ( 10.00000000000000000, -30.00120703465222149, 22.64427369931158296 ) ) ;
#35146=EDGE_CURVE ( 'NONE', #14490, #28940, #42805, .T. ) ;
#35148=EDGE_CURVE ( 'NONE', #1345, #41033, #25584, .T. ) ;
#35154=ORIENTED_EDGE ( 'NONE', *, *, #17131, .F. ) ;
#35155=VECTOR ( 'NONE', #40965, 1000.000000000000000 ) ;
#35176=ORIENTED_EDGE ( 'NONE', *, *, #1035, .F. ) ;
#35186=ORIENTED_EDGE ( 'NONE', *, *, #36586, .F. ) ;
#35189=VECTOR ( 'NONE', #4542, 1000.000000000000114 ) ;
#35196=AXIS2_PLACEMENT_3D ( 'NONE', #11034, #14717, #8080 ) ;
#35206=CARTESIAN_POINT ( 'NONE',  ( 10.00000000000000000, 40.98264845739763018, -9.188173127306866306 ) ) ;
#35215=ORIENTED_EDGE ( 'NONE', *, *, #42033, .F. ) ;
#35216=DIRECTION ( 'NONE',  ( -1.000000000000000000, 0.000000000000000000, -0.000000000000000000 ) ) ;
#35218=ORIENTED_EDGE ( 'NONE', *, *, #22820, .F. ) ;
#35226=ORIENTED_EDGE ( 'NONE', *, *, #26869, .F. ) ;
#35228=CIRCLE ( 'NONE', #24305, 16.00000000000000000 ) ;
#35239=DIRECTION ( 'NONE',  ( 0.000000000000000000, 0.1045284632676448111, 0.9945218953682742891 ) ) ;
#35242=ORIENTED_EDGE ( 'NONE', *, *, #162, .F. ) ;
#35244=VERTEX_POINT ( 'NONE', #20703 ) ;
#35246=DIRECTION ( 'NONE',  ( 0.000000000000000000, 0.000000000000000000, 1.000000000000000000 ) ) ;
#35248=ORIENTED_EDGE ( 'NONE', *, *, #30627, .F. ) ;
#35249=ORIENTED_EDGE ( 'NONE', *, *, #26798, .F. ) ;
#35250=CARTESIAN_POINT ( 'NONE',  ( 0.000000000000000000, -4.261787119644969479, -26.19803753235780519 ) ) ;
#35251=CARTESIAN_POINT ( 'NONE',  ( 0.000000000000000000, -0.8828120875903202602, 37.48860685352291000 ) ) ;
#35255=DIRECTION ( 'NONE',  ( 1.000000000000000000, 0.000000000000000000, 0.000000000000000000 ) ) ;
#35262=FACE_OUTER_BOUND ( 'NONE', #22069, .T. ) ;
#35267=DIRECTION ( 'NONE',  ( 0.000000000000000000, -0.1045284632676429099, -0.9945218953682744001 ) ) ;
#35268=CIRCLE ( 'NONE', #42293, 42.00000000000000000 ) ;
#35276=EDGE_CURVE ( 'NONE', #32891, #38425, #13360, .T. ) ;
#35277=DIRECTION ( 'NONE',  ( 0.000000000000000000, 0.000000000000000000, 1.000000000000000000 ) ) ;
#35298=EDGE_CURVE ( 'NONE', #20236, #11961, #612, .T. ) ;
#35302=LINE ( 'NONE', #38256, #41779 ) ;
#35303=DIRECTION ( 'NONE',  ( 0.000000000000000000, 0.000000000000000000, 1.000000000000000000 ) ) ;
#35304=DIRECTION ( 'NONE',  ( 1.000000000000000000, 0.000000000000000000, 0.000000000000000000 ) ) ;
#35309=ORIENTED_EDGE ( 'NONE', *, *, #3242, .T. ) ;
#35320=EDGE_CURVE ( 'NONE', #24209, #39037, #27830, .T. ) ;
#35330=AXIS2_PLACEMENT_3D ( 'NONE', #36107, #21892, #43471 ) ;
#35334=ORIENTED_EDGE ( 'NONE', *, *, #21441, .T. ) ;
#35338=AXIS2_PLACEMENT_3D ( 'NONE', #3534, #22132, #33399 ) ;
#35342=CARTESIAN_POINT ( 'NONE',  ( 0.000000000000000000, 8.688484142253939169, 21.88630264137371029 ) ) ;
#35343=VERTEX_POINT ( 'NONE', #44844 ) ;
#35344=ORIENTED_EDGE ( 'NONE', *, *, #23362, .F. ) ;
#35346=ADVANCED_FACE ( 'NONE', ( #45322 ), #14516, .F. ) ;
#35355=DIRECTION ( 'NONE',  ( 0.000000000000000000, -0.3090169943749349057, -0.9510565162951577500 ) ) ;
#35361=VERTEX_POINT ( 'NONE', #30408 ) ;
#35362=CARTESIAN_POINT ( 'NONE',  ( 10.00000000000000000, 0.000000000000000000, 0.000000000000000000 ) ) ;
#35363=ORIENTED_EDGE ( 'NONE', *, *, #43280, .F. ) ;
#35365=CIRCLE ( 'NONE', #33778, 42.00000000000000000 ) ;
#35366=DIRECTION ( 'NONE',  ( -1.000000000000000000, 0.000000000000000000, -0.000000000000000000 ) ) ;
#35382=CARTESIAN_POINT ( 'NONE',  ( 0.000000000000000000, -1.278221433540145613, -26.51162292216073979 ) ) ;
#35388=CARTESIAN_POINT ( 'NONE',  ( 4.999999999999999112, 40.98264845739763018, -9.188173127306860977 ) ) ;
#35399=CIRCLE ( 'NONE', #15070, 42.00000000000000000 ) ;
#35405=EDGE_CURVE ( 'NONE', #47865, #30860, #28744, .T. ) ;
#35408=CYLINDRICAL_SURFACE ( 'NONE', #9728, 42.00000000000000000 ) ;
#35410=VERTEX_POINT ( 'NONE', #18155 ) ;
#35413=DIRECTION ( 'NONE',  ( -1.000000000000000000, 0.000000000000000000, 0.000000000000000000 ) ) ;
#35414=DIRECTION ( 'NONE',  ( 0.000000000000000000, -0.5877852522924789103, 0.8090169943749432324 ) ) ;
#35420=ORIENTED_EDGE ( 'NONE', *, *, #29501, .T. ) ;
#35421=EDGE_LOOP ( 'NONE', ( #34996, #12679, #30975, #10113 ) ) ;
#35422=EDGE_CURVE ( 'NONE', #15212, #28487, #41193, .T. ) ;
#35430=ORIENTED_EDGE ( 'NONE', *, *, #21099, .T. ) ;
#35431=ORIENTED_EDGE ( 'NONE', *, *, #24978, .T. ) ;
#35437=ORIENTED_EDGE ( 'NONE', *, *, #34719, .F. ) ;
#35450=VECTOR ( 'NONE', #3186, 1000.000000000000000 ) ;
#35451=VECTOR ( 'NONE', #40280, 1000.000000000000227 ) ;
#35454=CYLINDRICAL_SURFACE ( 'NONE', #27024, 16.00000000000000000 ) ;
#35469=VECTOR ( 'NONE', #10165, 1000.000000000000000 ) ;
#35470=EDGE_LOOP ( 'NONE', ( #32182, #5031, #128, #45232 ) ) ;
#35472=EDGE_LOOP ( 'NONE', ( #15027, #40997, #46754, #35047 ) ) ;
#35479=ORIENTED_EDGE ( 'NONE', *, *, #43667, .T. ) ;
#35486=FACE_OUTER_BOUND ( 'NONE', #9845, .T. ) ;
#35495=CARTESIAN_POINT ( 'NONE',  ( 10.00000000000000000, -33.80338159004296017, 16.23288003029484727 ) ) ;
#35496=CARTESIAN_POINT ( 'NONE',  ( 10.00000000000000000, 35.53030884539084866, 12.26510123303271982 ) ) ;
#35503=DIRECTION ( 'NONE',  ( 0.000000000000000000, 0.000000000000000000, 1.000000000000000000 ) ) ;
#35504=DIRECTION ( 'NONE',  ( 0.000000000000000000, -0.4067366430758010409, 0.9135454576426005335 ) ) ;
#35508=DIRECTION ( 'NONE',  ( 0.000000000000000000, 0.2079116908177543743, 0.9781476007338066880 ) ) ;
#35515=DIRECTION ( 'NONE',  ( -1.000000000000000000, -0.000000000000000000, 0.000000000000000000 ) ) ;
#35516=VECTOR ( 'NONE', #2252, 1000.000000000000000 ) ;
#35521=EDGE_CURVE ( 'NONE', #26069, #16291, #23296, .T. ) ;
#35525=CYLINDRICAL_SURFACE ( 'NONE', #27654, 37.49900000000000233 ) ;
#35532=EDGE_CURVE ( 'NONE', #44403, #37347, #23776, .T. ) ;
#35547=AXIS2_PLACEMENT_3D ( 'NONE', #24122, #31477, #46882 ) ;
#35550=ORIENTED_EDGE ( 'NONE', *, *, #25502, .F. ) ;
#35551=ORIENTED_EDGE ( 'NONE', *, *, #4104, .F. ) ;
#35552=LINE ( 'NONE', #5447, #11865 ) ;
#35553=LINE ( 'NONE', #24777, #35516 ) ;
#35564=CARTESIAN_POINT ( 'NONE',  ( 10.00000000000000000, -33.00180498840060039, 17.80606268964528027 ) ) ;
#35565=AXIS2_PLACEMENT_3D ( 'NONE', #23281, #7860, #30393 ) ;
#35567=DIRECTION ( 'NONE',  ( 0.000000000000000000, -0.3090169943749349057, -0.9510565162951576390 ) ) ;
#35582=ORIENTED_EDGE ( 'NONE', *, *, #13970, .T. ) ;
#35601=EDGE_CURVE ( 'NONE', #17031, #14290, #19599, .T. ) ;
#35604=CARTESIAN_POINT ( 'NONE',  ( 0.000000000000000000, 14.60985201121729737, -18.46759930825688301 ) ) ;
#35609=ORIENTED_EDGE ( 'NONE', *, *, #39937, .T. ) ;
#35616=ORIENTED_EDGE ( 'NONE', *, *, #6147, .T. ) ;
#35620=FACE_BOUND ( 'NONE', #18318, .T. ) ;
#35621=DIRECTION ( 'NONE',  ( 1.000000000000000000, 0.000000000000000000, -0.000000000000000000 ) ) ;
#35628=CARTESIAN_POINT ( 'NONE',  ( 0.000000000000000000, 0.000000000000000000, 0.000000000000000000 ) ) ;
#35631=AXIS2_PLACEMENT_3D ( 'NONE', #17115, #28851, #13453 ) ;
#35633=DIRECTION ( 'NONE',  ( 0.000000000000000000, -0.9781476007338070211, 0.2079116908177525425 ) ) ;
#35640=LINE ( 'NONE', #5536, #19316 ) ;
#35641=CARTESIAN_POINT ( 'NONE',  ( -3.000000000000000000, 23.59884966291538078, -12.14883922797231541 ) ) ;
#35670=VERTEX_POINT ( 'NONE', #32328 ) ;
#35680=FACE_OUTER_BOUND ( 'NONE', #41348, .T. ) ;
#35684=AXIS2_PLACEMENT_3D ( 'NONE', #47291, #13768, #2729 ) ;
#35689=FACE_OUTER_BOUND ( 'NONE', #20077, .T. ) ;
#35690=ORIENTED_EDGE ( 'NONE', *, *, #45630, .F. ) ;
#35692=EDGE_LOOP ( 'NONE', ( #35430, #20791, #45102, #16073 ) ) ;
#35697=CARTESIAN_POINT ( 'NONE',  ( 0.000000000000000000, -16.45098606841149902, 33.79645857604508308 ) ) ;
#35706=CARTESIAN_POINT ( 'NONE',  ( 10.00000000000000000, 0.000000000000000000, 0.000000000000000000 ) ) ;
#35709=ORIENTED_EDGE ( 'NONE', *, *, #18290, .T. ) ;
#35724=ORIENTED_EDGE ( 'NONE', *, *, #38407, .T. ) ;
#35727=DIRECTION ( 'NONE',  ( -1.000000000000000000, 0.000000000000000000, 0.000000000000000000 ) ) ;
#35737=CARTESIAN_POINT ( 'NONE',  ( 10.00000000000000000, 21.40280677340421533, -36.13751322684397138 ) ) ;
#35742=ORIENTED_EDGE ( 'NONE', *, *, #25757, .F. ) ;
#35752=DIRECTION ( 'NONE',  ( 0.000000000000000000, 0.000000000000000000, 1.000000000000000000 ) ) ;
#35761=ADVANCED_FACE ( 'NONE', ( #23440 ), #42059, .T. ) ;
#35770=VERTEX_POINT ( 'NONE', #19753 ) ;
#35791=EDGE_CURVE ( 'NONE', #20853, #43486, #45975, .T. ) ;
#35793=VERTEX_POINT ( 'NONE', #31292 ) ;
#35796=LINE ( 'NONE', #39487, #39566 ) ;
#35797=ORIENTED_EDGE ( 'NONE', *, *, #38053, .T. ) ;
#35802=DIRECTION ( 'NONE',  ( -1.000000000000000000, 0.000000000000000000, 0.000000000000000000 ) ) ;
#35806=ADVANCED_FACE ( 'NONE', ( #13161 ), #46210, .F. ) ;
#35807=CARTESIAN_POINT ( 'NONE',  ( 10.00000000000000000, 10.74501242461282757, 35.92658777277515014 ) ) ;
#35813=( NAMED_UNIT ( * ) SI_UNIT ( $, .STERADIAN. ) SOLID_ANGLE_UNIT ( ) );
#35814=DIRECTION ( 'NONE',  ( -1.000000000000000000, 0.000000000000000000, 0.000000000000000000 ) ) ;
#35818=PRODUCT_DEFINITION_FORMATION_WITH_SPECIFIED_SOURCE ( 'ANY', '', #13210, .NOT_KNOWN. ) ;
#35823=DIRECTION ( 'NONE',  ( -1.000000000000000000, 0.000000000000000000, 0.000000000000000000 ) ) ;
#35825=CARTESIAN_POINT ( 'NONE',  ( -3.000000000000000000, 18.84667830672579925, 18.68964196561269020 ) ) ;
#35829=CARTESIAN_POINT ( 'NONE',  ( 10.00000000000000000, 36.13751322684419165, 21.40280677340384230 ) ) ;
#35832=AXIS2_PLACEMENT_3D ( 'NONE', #6235, #48066, #17229 ) ;
#35842=CARTESIAN_POINT ( 'NONE',  ( 10.00000000000000000, -41.91543099594816368, -2.663952781846588014 ) ) ;
#35844=AXIS2_PLACEMENT_3D ( 'NONE', #37994, #27460, #19139 ) ;
#35845=ADVANCED_FACE ( 'NONE', ( #43261 ), #46934, .T. ) ;
#35847=DIRECTION ( 'NONE',  ( 0.000000000000000000, 0.8910065241883657894, 0.4539904997395509678 ) ) ;
#35848=EDGE_LOOP ( 'NONE', ( #46927, #21818, #5503, #20735 ) ) ;
#35849=FACE_BOUND ( 'NONE', #5733, .T. ) ;
#35851=CARTESIAN_POINT ( 'NONE',  ( 0.000000000000000000, -22.32062822937469804, -14.36278369418829826 ) ) ;
#35852=DIRECTION ( 'NONE',  ( 0.000000000000000000, 0.000000000000000000, 1.000000000000000000 ) ) ;
#35861=ORIENTED_EDGE ( 'NONE', *, *, #27008, .F. ) ;
#35868=EDGE_CURVE ( 'NONE', #45324, #15496, #19394, .T. ) ;
#35874=EDGE_CURVE ( 'NONE', #33652, #29574, #36145, .T. ) ;
#35876=DIRECTION ( 'NONE',  ( -1.000000000000000000, -0.000000000000000000, -0.000000000000000000 ) ) ;
#35879=ORIENTED_EDGE ( 'NONE', *, *, #2159, .T. ) ;
#35882=EDGE_CURVE ( 'NONE', #41559, #29480, #10202, .T. ) ;
#35890=ORIENTED_EDGE ( 'NONE', *, *, #3756, .F. ) ;
#35898=ORIENTED_EDGE ( 'NONE', *, *, #46665, .F. ) ;
#35903=CARTESIAN_POINT ( 'NONE',  ( -3.000000000000000000, 0.000000000000000000, 0.000000000000000000 ) ) ;
#35904=DIRECTION ( 'NONE',  ( 1.000000000000000000, 0.000000000000000000, -0.000000000000000000 ) ) ;
#35908=DIRECTION ( 'NONE',  ( -1.000000000000000000, -0.000000000000000000, -0.000000000000000000 ) ) ;
#35915=EDGE_CURVE ( 'NONE', #894, #15085, #23356, .T. ) ;
#35921=DIRECTION ( 'NONE',  ( -1.000000000000000000, 0.000000000000000000, -0.000000000000000000 ) ) ;
#35933=AXIS2_PLACEMENT_3D ( 'NONE', #21568, #10293, #29134 ) ;
#35936=ORIENTED_EDGE ( 'NONE', *, *, #33838, .T. ) ;
#35944=ORIENTED_EDGE ( 'NONE', *, *, #12888, .T. ) ;
#35954=AXIS2_PLACEMENT_3D ( 'NONE', #38305, #5742, #16281 ) ;
#35967=ORIENTED_EDGE ( 'NONE', *, *, #37072, .T. ) ;
#35969=DIRECTION ( 'NONE',  ( -1.000000000000000000, 0.000000000000000000, 0.000000000000000000 ) ) ;
#35977=ORIENTED_EDGE ( 'NONE', *, *, #26275, .F. ) ;
#35982=DIRECTION ( 'NONE',  ( -1.000000000000000000, -0.000000000000000000, 0.000000000000000000 ) ) ;
#35985=DIRECTION ( 'NONE',  ( -0.000000000000000000, -0.6691306063588569053, -0.7431448254773954654 ) ) ;
#35988=DIRECTION ( 'NONE',  ( -0.000000000000000000, -0.6691306063588569053, -0.7431448254773954654 ) ) ;
#35989=LINE ( 'NONE', #829, #34200 ) ;
#35994=VECTOR ( 'NONE', #35802, 1000.000000000000000 ) ;
#35997=DIRECTION ( 'NONE',  ( -1.000000000000000000, -0.000000000000000000, -0.000000000000000000 ) ) ;
#36000=VECTOR ( 'NONE', #6191, 1000.000000000000000 ) ;
#36003=DIRECTION ( 'NONE',  ( 0.000000000000000000, -0.4539904997395541320, 0.8910065241883640130 ) ) ;
#36008=CARTESIAN_POINT ( 'NONE',  ( 10.00000000000000000, 15.48615015657638239, -39.04073710021328480 ) ) ;
#36023=ORIENTED_EDGE ( 'NONE', *, *, #40682, .F. ) ;
#36036=FACE_OUTER_BOUND ( 'NONE', #21066, .T. ) ;
#36037=VERTEX_POINT ( 'NONE', #46012 ) ;
#36048=CARTESIAN_POINT ( 'NONE',  ( 0.000000000000000000, -11.95096189432345390, 23.69967320028757385 ) ) ;
#36057=DIRECTION ( 'NONE',  ( -1.000000000000000000, 0.000000000000000000, 0.000000000000000000 ) ) ;
#36070=EDGE_CURVE ( 'NONE', #2611, #28645, #39794, .T. ) ;
#36074=AXIS2_PLACEMENT_3D ( 'NONE', #19181, #584, #26293 ) ;
#36076=DIRECTION ( 'NONE',  ( 0.000000000000000000, -6.938893903907228378E-15, 1.000000000000000000 ) ) ;
#36078=VERTEX_POINT ( 'NONE', #27907 ) ;
#36084=EDGE_CURVE ( 'NONE', #5383, #29067, #27286, .T. ) ;
#36089=DIRECTION ( 'NONE',  ( 0.000000000000000000, 0.000000000000000000, 1.000000000000000000 ) ) ;
#36092=FACE_BOUND ( 'NONE', #3618, .T. ) ;
#36098=LINE ( 'NONE', #13588, #15666 ) ;
#36102=CARTESIAN_POINT ( 'NONE',  ( -3.000000000000000000, -23.29833615347104825, -3.418703333116803744 ) ) ;
#36103=ORIENTED_EDGE ( 'NONE', *, *, #48043, .T. ) ;
#36104=AXIS2_PLACEMENT_3D ( 'NONE', #47573, #33135, #17722 ) ;
#36107=CARTESIAN_POINT ( 'NONE',  ( 10.00000000000000000, 0.000000000000000000, 0.000000000000000000 ) ) ;
#36118=ORIENTED_EDGE ( 'NONE', *, *, #1670, .T. ) ;
#36122=ADVANCED_FACE ( 'NONE', ( #14649 ), #43540, .F. ) ;
#36126=ORIENTED_EDGE ( 'NONE', *, *, #24210, .T. ) ;
#36127=AXIS2_PLACEMENT_3D ( 'NONE', #40743, #45376, #37319 ) ;
#36129=AXIS2_PLACEMENT_3D ( 'NONE', #47932, #33004, #10752 ) ;
#36130=DIRECTION ( 'NONE',  ( -1.000000000000000000, -0.000000000000000000, -0.000000000000000000 ) ) ;
#36135=EDGE_CURVE ( 'NONE', #29511, #8888, #3120, .T. ) ;
#36145=LINE ( 'NONE', #47877, #2221 ) ;
#36152=DIRECTION ( 'NONE',  ( 0.000000000000000000, -6.982962677686267499E-15, 1.000000000000000000 ) ) ;
#36153=ORIENTED_EDGE ( 'NONE', *, *, #38405, .T. ) ;
#36154=DIRECTION ( 'NONE',  ( -1.000000000000000000, 0.000000000000000000, -0.000000000000000000 ) ) ;
#36156=VECTOR ( 'NONE', #3393, 1000.000000000000000 ) ;
#36159=DIRECTION ( 'NONE',  ( -1.000000000000000000, 0.000000000000000000, -0.000000000000000000 ) ) ;
#36160=AXIS2_PLACEMENT_3D ( 'NONE', #6217, #36057, #6447 ) ;
#36161=DIRECTION ( 'NONE',  ( 0.000000000000000000, 0.000000000000000000, -1.000000000000000000 ) ) ;
#36166=DIRECTION ( 'NONE',  ( -1.000000000000000000, 0.000000000000000000, -0.000000000000000000 ) ) ;
#36167=LINE ( 'NONE', #47194, #1063 ) ;
#36171=CYLINDRICAL_SURFACE ( 'NONE', #43268, 37.49900000000000233 ) ;
#36178=ADVANCED_FACE ( 'NONE', ( #43770 ), #36658, .T. ) ;
#36180=CARTESIAN_POINT ( 'NONE',  ( 0.000000000000000000, 37.48860685352291000, -0.8828120875901940279 ) ) ;
#36199=CIRCLE ( 'NONE', #47143, 37.49900000000000944 ) ;
#36204=ORIENTED_EDGE ( 'NONE', *, *, #12118, .F. ) ;
#36208=ADVANCED_FACE ( 'NONE', ( #17815 ), #32744, .T. ) ;
#36211=ORIENTED_EDGE ( 'NONE', *, *, #28133, .F. ) ;
#36212=EDGE_LOOP ( 'NONE', ( #25202, #13385, #11159, #36406 ) ) ;
#36217=AXIS2_PLACEMENT_3D ( 'NONE', #46559, #35997, #9818 ) ;
#36226=DIRECTION ( 'NONE',  ( 0.000000000000000000, 0.000000000000000000, 1.000000000000000000 ) ) ;
#36249=DIRECTION ( 'NONE',  ( -1.000000000000000000, -0.000000000000000000, -0.000000000000000000 ) ) ;
#36272=ORIENTED_EDGE ( 'NONE', *, *, #43560, .F. ) ;
#36281=ORIENTED_EDGE ( 'NONE', *, *, #22761, .T. ) ;
#36284=EDGE_CURVE ( 'NONE', #47549, #18104, #19491, .T. ) ;
#36290=AXIS2_PLACEMENT_3D ( 'NONE', #29322, #26128, #22464 ) ;
#36294=DIRECTION ( 'NONE',  ( 0.000000000000000000, 0.6691306063588675634, -0.7431448254773856954 ) ) ;
#36296=VECTOR ( 'NONE', #38659, 1000.000000000000000 ) ;
#36298=CARTESIAN_POINT ( 'NONE',  ( 10.00000000000000000, -39.04073710021333454, -15.48615015657624738 ) ) ;
#36299=DIRECTION ( 'NONE',  ( 0.000000000000000000, -0.1564344650402382242, 0.9876883405951366601 ) ) ;
#36303=ADVANCED_FACE ( 'NONE', ( #15378 ), #23187, .T. ) ;
#36310=ADVANCED_FACE ( 'NONE', ( #33710 ), #26620, .T. ) ;
#36313=FACE_OUTER_BOUND ( 'NONE', #6906, .T. ) ;
#36321=VECTOR ( 'NONE', #25764, 1000.000000000000000 ) ;
#36322=LINE ( 'NONE', #17716, #3505 ) ;
#36326=EDGE_LOOP ( 'NONE', ( #18251, #28902, #40759, #19084 ) ) ;
#36329=DIRECTION ( 'NONE',  ( 0.000000000000000000, 0.2079116908177532363, 0.9781476007338069101 ) ) ;
#36340=CARTESIAN_POINT ( 'NONE',  ( 10.00000000000000000, -21.32104025579091910, -30.84782396557241313 ) ) ;
#36354=CARTESIAN_POINT ( 'NONE',  ( 0.000000000000000000, 0.000000000000000000, 0.000000000000000000 ) ) ;
#36356=VECTOR ( 'NONE', #10666, 1000.000000000000000 ) ;
#36357=DIRECTION ( 'NONE',  ( -1.000000000000000000, 0.000000000000000000, -0.000000000000000000 ) ) ;
#36358=LINE ( 'NONE', #106, #35469 ) ;
#36366=CIRCLE ( 'NONE', #34820, 42.00000000000000000 ) ;
#36382=ORIENTED_EDGE ( 'NONE', *, *, #43324, .F. ) ;
#36400=CARTESIAN_POINT ( 'NONE',  ( 10.00000000000000000, 21.53537804866126137, -30.80686688396986028 ) ) ;
#36402=PLANE ( 'NONE',  #13439 ) ;
#36406=ORIENTED_EDGE ( 'NONE', *, *, #7800, .T. ) ;
#36408=FACE_BOUND ( 'NONE', #6815, .T. ) ;
#36419=DIRECTION ( 'NONE',  ( 0.000000000000000000, 0.000000000000000000, 1.000000000000000000 ) ) ;
#36430=CARTESIAN_POINT ( 'NONE',  ( 10.00000000000000000, 16.45098606841126454, 33.79645857604518966 ) ) ;
#36438=ORIENTED_EDGE ( 'NONE', *, *, #32926, .T. ) ;
#36452=DIRECTION ( 'NONE',  ( -1.000000000000000000, 0.000000000000000000, -0.000000000000000000 ) ) ;
#36467=PLANE ( 'NONE',  #37224 ) ;
#36470=DIRECTION ( 'NONE',  ( 0.000000000000000000, 0.000000000000000000, 1.000000000000000000 ) ) ;
#36472=CARTESIAN_POINT ( 'NONE',  ( 10.00000000000000000, 37.58145647212455032, -0.6853352020786441789 ) ) ;
#36484=EDGE_CURVE ( 'NONE', #5281, #26444, #15564, .T. ) ;
#36494=CARTESIAN_POINT ( 'NONE',  ( 0.000000000000000000, -26.79245525562690844, -32.34446384430000876 ) ) ;
#36498=CARTESIAN_POINT ( 'NONE',  ( 0.000000000000000000, 29.81001611431009479, 22.74946021919143391 ) ) ;
#36500=DIRECTION ( 'NONE',  ( -1.000000000000000000, 0.000000000000000000, -0.000000000000000000 ) ) ;
#36501=ORIENTED_EDGE ( 'NONE', *, *, #12184, .F. ) ;
#36502=DIRECTION ( 'NONE',  ( 0.000000000000000000, -0.7431448254773870277, -0.6691306063588662312 ) ) ;
#36508=ORIENTED_EDGE ( 'NONE', *, *, #22634, .T. ) ;
#36512=CARTESIAN_POINT ( 'NONE',  ( 10.00000000000000000, -32.34446384429951138, -26.79245525562750530 ) ) ;
#36516=LINE ( 'NONE', #28925, #36000 ) ;
#36523=EDGE_CURVE ( 'NONE', #34646, #16565, #2287, .T. ) ;
#36526=EDGE_LOOP ( 'NONE', ( #13318, #35069, #19046, #28733 ) ) ;
#36531=CARTESIAN_POINT ( 'NONE',  ( 0.000000000000000000, 16.83928648764945279, -16.46020748918028076 ) ) ;
#36539=ORIENTED_EDGE ( 'NONE', *, *, #30432, .F. ) ;
#36542=ORIENTED_EDGE ( 'NONE', *, *, #18718, .F. ) ;
#36557=ORIENTED_EDGE ( 'NONE', *, *, #5021, .F. ) ;
#36561=LINE ( 'NONE', #33133, #678 ) ;
#36562=DIRECTION ( 'NONE',  ( 0.000000000000000000, -0.1045284632676436454, -0.9945218953682744001 ) ) ;
#36571=CARTESIAN_POINT ( 'NONE',  ( -10.00000000000000000, 0.000000000000000000, 0.000000000000000000 ) ) ;
#36572=FACE_OUTER_BOUND ( 'NONE', #26141, .T. ) ;
#36573=DIRECTION ( 'NONE',  ( -1.000000000000000000, -0.000000000000000000, 0.000000000000000000 ) ) ;
#36584=ORIENTED_EDGE ( 'NONE', *, *, #27250, .F. ) ;
#36585=DIRECTION ( 'NONE',  ( 1.000000000000000000, 0.000000000000000000, 0.000000000000000000 ) ) ;
#36586=EDGE_CURVE ( 'NONE', #3154, #22090, #21681, .T. ) ;
#36633=CARTESIAN_POINT ( 'NONE',  ( 0.000000000000000000, 23.50000000000000000, -1.500000000000001332 ) ) ;
#36639=EDGE_CURVE ( 'NONE', #12152, #46530, #29019, .T. ) ;
#36640=VERTEX_POINT ( 'NONE', #43238 ) ;
#36642=ADVANCED_FACE ( 'NONE', ( #24637 ), #13869, .T. ) ;
#36647=LINE ( 'NONE', #6324, #29457 ) ;
#36652=ORIENTED_EDGE ( 'NONE', *, *, #13036, .T. ) ;
#36655=ORIENTED_EDGE ( 'NONE', *, *, #39348, .F. ) ;
#36658=CYLINDRICAL_SURFACE ( 'NONE', #41323, 16.00000000000000000 ) ;
#36661=ORIENTED_EDGE ( 'NONE', *, *, #19379, .T. ) ;
#36676=EDGE_CURVE ( 'NONE', #5880, #12261, #7711, .T. ) ;
#36678=ORIENTED_EDGE ( 'NONE', *, *, #46257, .F. ) ;
#36681=EDGE_LOOP ( 'NONE', ( #26396, #20535, #24402, #20478 ) ) ;
#36684=EDGE_LOOP ( 'NONE', ( #47097, #40373, #5578, #12129 ) ) ;
#36685=AXIS2_PLACEMENT_3D ( 'NONE', #44443, #39820, #17526 ) ;
#36689=ORIENTED_EDGE ( 'NONE', *, *, #33534, .F. ) ;
#36692=LINE ( 'NONE', #24732, #16792 ) ;
#36693=CARTESIAN_POINT ( 'NONE',  ( 0.000000000000000000, -35.53030884539077050, -12.26510123303296851 ) ) ;
#36694=DIRECTION ( 'NONE',  ( 0.000000000000000000, 0.000000000000000000, 1.000000000000000000 ) ) ;
#36703=DIRECTION ( 'NONE',  ( -1.000000000000000000, 0.000000000000000000, 0.000000000000000000 ) ) ;
#36706=VERTEX_POINT ( 'NONE', #29509 ) ;
#36709=CARTESIAN_POINT ( 'NONE',  ( 10.00000000000000000, 0.000000000000000000, 0.000000000000000000 ) ) ;
#36714=EDGE_CURVE ( 'NONE', #20645, #7437, #48343, .T. ) ;
#36717=ORIENTED_EDGE ( 'NONE', *, *, #44541, .F. ) ;
#36724=ADVANCED_FACE ( 'NONE', ( #44675 ), #29991, .T. ) ;
#36731=DIRECTION ( 'NONE',  ( 0.000000000000000000, -0.9510565162951500895, -0.3090169943749583314 ) ) ;
#36732=FACE_OUTER_BOUND ( 'NONE', #35472, .T. ) ;
#36734=EDGE_CURVE ( 'NONE', #43358, #16571, #5437, .T. ) ;
#36735=FACE_OUTER_BOUND ( 'NONE', #23544, .T. ) ;
#36737=EDGE_CURVE ( 'NONE', #33784, #26631, #10914, .T. ) ;
#36741=DIRECTION ( 'NONE',  ( 0.000000000000000000, 0.000000000000000000, 1.000000000000000000 ) ) ;
#36755=AXIS2_PLACEMENT_3D ( 'NONE', #380, #19938, #18963 ) ;
#36758=CARTESIAN_POINT ( 'NONE',  ( 0.000000000000000000, -27.75498641678720446, -31.52238457039628727 ) ) ;
#36761=CARTESIAN_POINT ( 'NONE',  ( 10.00000000000000000, 6.736453364083557105, 36.88895765772635826 ) ) ;
#36771=DIRECTION ( 'NONE',  ( 0.000000000000000000, 0.000000000000000000, -1.000000000000000000 ) ) ;
#36777=ORIENTED_EDGE ( 'NONE', *, *, #43004, .T. ) ;
#36793=ORIENTED_EDGE ( 'NONE', *, *, #4576, .T. ) ;
#36796=CARTESIAN_POINT ( 'NONE',  ( 10.00000000000000000, -29.81001611430991360, -22.74946021919165418 ) ) ;
#36797=ADVANCED_FACE ( 'NONE', ( #24515 ), #5435, .T. ) ;
#36799=CARTESIAN_POINT ( 'NONE',  ( 10.00000000000000000, -35.92658777277502935, -10.74501242461320594 ) ) ;
#36802=VECTOR ( 'NONE', #42069, 1000.000000000000000 ) ;
#36812=CARTESIAN_POINT ( 'NONE',  ( 0.000000000000000000, 0.000000000000000000, 0.000000000000000000 ) ) ;
#36818=EDGE_LOOP ( 'NONE', ( #19883, #41527, #39547, #20309 ) ) ;
#36831=CIRCLE ( 'NONE', #46244, 15.99999999999999822 ) ;
#36833=VERTEX_POINT ( 'NONE', #43122 ) ;
#36836=EDGE_CURVE ( 'NONE', #45945, #15085, #46881, .T. ) ;
#36837=CIRCLE ( 'NONE', #2461, 16.00000000000000000 ) ;
#36839=DIRECTION ( 'NONE',  ( -1.000000000000000000, 0.000000000000000000, -0.000000000000000000 ) ) ;
#36861=VERTEX_POINT ( 'NONE', #6160 ) ;
#36871=CARTESIAN_POINT ( 'NONE',  ( 0.000000000000000000, 14.60985201121729737, -18.46759930825687945 ) ) ;
#36872=DIRECTION ( 'NONE',  ( 0.000000000000000000, 0.000000000000000000, 1.000000000000000000 ) ) ;
#36882=DIRECTION ( 'NONE',  ( -0.000000000000000000, -0.3090169943749448977, -0.9510565162951543083 ) ) ;
#36888=AXIS2_PLACEMENT_3D ( 'NONE', #7928, #33876, #45151 ) ;
#36894=DIRECTION ( 'NONE',  ( -1.000000000000000000, 0.000000000000000000, 0.000000000000000000 ) ) ;
#36896=AXIS2_PLACEMENT_3D ( 'NONE', #21409, #33157, #93 ) ;
#36902=EDGE_CURVE ( 'NONE', #32256, #35410, #24043, .T. ) ;
#36904=DIRECTION ( 'NONE',  ( -1.000000000000000000, -0.000000000000000000, -0.000000000000000000 ) ) ;
#36907=VERTEX_POINT ( 'NONE', #20593 ) ;
#36908=EDGE_LOOP ( 'NONE', ( #27574, #44098, #17782, #3074 ) ) ;
#36911=DIRECTION ( 'NONE',  ( -1.000000000000000000, -0.000000000000000000, -0.000000000000000000 ) ) ;
#36913=VERTEX_POINT ( 'NONE', #44552 ) ;
#36920=CARTESIAN_POINT ( 'NONE',  ( -3.000000000000000000, -0.9646360437372163421, -23.52805723605591126 ) ) ;
#36924=CARTESIAN_POINT ( 'NONE',  ( 0.000000000000000000, 20.85821328998741109, 10.92862929874522315 ) ) ;
#36932=EDGE_CURVE ( 'NONE', #1711, #27887, #29682, .T. ) ;
#36933=VECTOR ( 'NONE', #34168, 1000.000000000000227 ) ;
#36946=CIRCLE ( 'NONE', #33817, 16.00000000000000355 ) ;
#36960=ORIENTED_EDGE ( 'NONE', *, *, #23422, .T. ) ;
#36973=ORIENTED_EDGE ( 'NONE', *, *, #42156, .T. ) ;
#37007=EDGE_CURVE ( 'NONE', #11522, #32747, #2948, .T. ) ;
#37011=DIRECTION ( 'NONE',  ( -1.000000000000000000, 0.000000000000000000, 0.000000000000000000 ) ) ;
#37012=EDGE_CURVE ( 'NONE', #43777, #26532, #6395, .T. ) ;
#37014=ORIENTED_EDGE ( 'NONE', *, *, #36737, .T. ) ;
#37026=ORIENTED_EDGE ( 'NONE', *, *, #41488, .F. ) ;
#37037=AXIS2_PLACEMENT_3D ( 'NONE', #1318, #34335, #46338 ) ;
#37060=DIRECTION ( 'NONE',  ( -1.000000000000000000, -0.000000000000000000, 0.000000000000000000 ) ) ;
#37063=DIRECTION ( 'NONE',  ( 1.000000000000000000, -0.000000000000000000, -0.000000000000000000 ) ) ;
#37072=EDGE_CURVE ( 'NONE', #18858, #44417, #28142, .T. ) ;
#37085=EDGE_CURVE ( 'NONE', #42163, #3180, #11521, .T. ) ;
#37086=CIRCLE ( 'NONE', #16802, 16.00000000000000000 ) ;
#37106=DIRECTION ( 'NONE',  ( 0.000000000000000000, 0.000000000000000000, 1.000000000000000000 ) ) ;
#37122=AXIS2_PLACEMENT_3D ( 'NONE', #38808, #9398, #24336 ) ;
#37129=AXIS2_PLACEMENT_3D ( 'NONE', #8233, #33271, #10761 ) ;
#37132=CARTESIAN_POINT ( 'NONE',  ( -3.000000000000000000, -18.13022148937263012, 15.02647892043544608 ) ) ;
#37138=EDGE_CURVE ( 'NONE', #9789, #1027, #32070, .T. ) ;
#37142=DIRECTION ( 'NONE',  ( 0.000000000000000000, 0.000000000000000000, 1.000000000000000000 ) ) ;
#37143=ADVANCED_FACE ( 'NONE', ( #7829 ), #22764, .T. ) ;
#37144=VECTOR ( 'NONE', #218, 1000.000000000000000 ) ;
#37166=ORIENTED_EDGE ( 'NONE', *, *, #24758, .F. ) ;
#37171=CARTESIAN_POINT ( 'NONE',  ( -3.000000000000000000, 23.50000000000000000, -1.500000000000001332 ) ) ;
#37173=ORIENTED_EDGE ( 'NONE', *, *, #23530, .F. ) ;
#37186=CARTESIAN_POINT ( 'NONE',  ( 10.00000000000000000, -21.32104025579135964, 30.84782396557210760 ) ) ;
#37198=DIRECTION ( 'NONE',  ( -1.000000000000000000, 0.000000000000000000, -0.000000000000000000 ) ) ;
#37202=ORIENTED_EDGE ( 'NONE', *, *, #46708, .T. ) ;
#37205=VECTOR ( 'NONE', #37, 1000.000000000000114 ) ;
#37212=ORIENTED_EDGE ( 'NONE', *, *, #29570, .F. ) ;
#37222=EDGE_CURVE ( 'NONE', #28893, #22498, #34373, .T. ) ;
#37223=EDGE_LOOP ( 'NONE', ( #45053, #34877, #30429, #18974 ) ) ;
#37224=AXIS2_PLACEMENT_3D ( 'NONE', #17856, #25438, #33024 ) ;
#37230=DIRECTION ( 'NONE',  ( -1.000000000000000000, 0.000000000000000000, -0.000000000000000000 ) ) ;
#37231=ORIENTED_EDGE ( 'NONE', *, *, #1495, .T. ) ;
#37247=EDGE_CURVE ( 'NONE', #13778, #8400, #13306, .T. ) ;
#37253=AXIS2_PLACEMENT_3D ( 'NONE', #29321, #29554, #6558 ) ;
#37255=DIRECTION ( 'NONE',  ( -0.000000000000000000, -0.9135454576426059736, 0.4067366430757887730 ) ) ;
#37257=DIRECTION ( 'NONE',  ( 0.000000000000000000, -1.000000000000000000, -1.047444401652940007E-14 ) ) ;
#37261=PLANE ( 'NONE',  #2580 ) ;
#37263=CARTESIAN_POINT ( 'NONE',  ( -3.000000000000000000, 8.688484142253939169, 21.88630264137371029 ) ) ;
#37265=VERTEX_POINT ( 'NONE', #5871 ) ;
#37268=VECTOR ( 'NONE', #34884, 1000.000000000000000 ) ;
#37270=EDGE_LOOP ( 'NONE', ( #565, #36023, #44996, #15669 ) ) ;
#37282=EDGE_CURVE ( 'NONE', #22651, #41559, #31579, .T. ) ;
#37291=ORIENTED_EDGE ( 'NONE', *, *, #5698, .T. ) ;
#37296=CIRCLE ( 'NONE', #16212, 37.49900000000000944 ) ;
#37302=DIRECTION ( 'NONE',  ( -0.000000000000000000, 0.1045284632676436315, 0.9945218953682742891 ) ) ;
#37305=DIRECTION ( 'NONE',  ( 0.000000000000000000, 0.000000000000000000, 1.000000000000000000 ) ) ;
#37309=FACE_OUTER_BOUND ( 'NONE', #9228, .T. ) ;
#37311=EDGE_CURVE ( 'NONE', #10700, #38800, #2406, .T. ) ;
#37312=DIRECTION ( 'NONE',  ( -1.000000000000000000, 0.000000000000000000, 0.000000000000000000 ) ) ;
#37319=DIRECTION ( 'NONE',  ( 0.000000000000000000, 0.000000000000000000, -1.000000000000000000 ) ) ;
#37322=EDGE_CURVE ( 'NONE', #13859, #32853, #5143, .T. ) ;
#37328=CARTESIAN_POINT ( 'NONE',  ( 10.00000000000000000, -37.48860685352290290, -0.8828120875904512665 ) ) ;
#37346=EDGE_CURVE ( 'NONE', #34171, #44060, #9514, .T. ) ;
#37347=VERTEX_POINT ( 'NONE', #28843 ) ;
#37349=CARTESIAN_POINT ( 'NONE',  ( 10.00000000000000000, -37.22597642581153821, -5.202137450156795850 ) ) ;
#37361=DIRECTION ( 'NONE',  ( -1.000000000000000000, -0.000000000000000000, 0.000000000000000000 ) ) ;
#37367=FACE_OUTER_BOUND ( 'NONE', #37468, .T. ) ;
#37369=AXIS2_PLACEMENT_3D ( 'NONE', #42612, #19826, #2205 ) ;
#37376=ORIENTED_EDGE ( 'NONE', *, *, #6821, .F. ) ;
#37389=VERTEX_POINT ( 'NONE', #48172 ) ;
#37402=EDGE_CURVE ( 'NONE', #36037, #27530, #24158, .T. ) ;
#37410=ORIENTED_EDGE ( 'NONE', *, *, #23369, .T. ) ;
#37411=CARTESIAN_POINT ( 'NONE',  ( -3.000000000000000000, -26.23277895567245821, -4.042438405570103477 ) ) ;
#37426=ORIENTED_EDGE ( 'NONE', *, *, #16272, .F. ) ;
#37428=DIRECTION ( 'NONE',  ( -1.000000000000000000, 0.000000000000000000, 0.000000000000000000 ) ) ;
#37436=VECTOR ( 'NONE', #1705, 1000.000000000000000 ) ;
#37438=ORIENTED_EDGE ( 'NONE', *, *, #5997, .F. ) ;
#37440=DIRECTION ( 'NONE',  ( 0.000000000000000000, 0.000000000000000000, 1.000000000000000000 ) ) ;
#37454=ORIENTED_EDGE ( 'NONE', *, *, #13923, .T. ) ;
#37468=EDGE_LOOP ( 'NONE', ( #45516, #42309, #30291, #42054 ) ) ;
#37472=CARTESIAN_POINT ( 'NONE',  ( 10.00000000000000000, -40.68715046381937128, 10.41901085202062660 ) ) ;
#37473=LINE ( 'NONE', #33781, #10305 ) ;
#37477=CYLINDRICAL_SURFACE ( 'NONE', #15364, 16.00000000000000000 ) ;
#37480=ORIENTED_EDGE ( 'NONE', *, *, #3177, .F. ) ;
#37482=ORIENTED_EDGE ( 'NONE', *, *, #5182, .F. ) ;
#37495=CARTESIAN_POINT ( 'NONE',  ( 0.000000000000000000, 22.74946021919175720, -29.81001611430984255 ) ) ;
#37496=DIRECTION ( 'NONE',  ( 0.000000000000000000, 0.4067366430758009854, -0.9135454576426004225 ) ) ;
#37498=LINE ( 'NONE', #18877, #37205 ) ;
#37503=ORIENTED_EDGE ( 'NONE', *, *, #3993, .F. ) ;
#37518=ADVANCED_FACE ( 'NONE', ( #41322 ), #19026, .F. ) ;
#37523=VERTEX_POINT ( 'NONE', #26623 ) ;
#37524=EDGE_CURVE ( 'NONE', #47099, #45945, #42044, .T. ) ;
#37538=AXIS2_PLACEMENT_3D ( 'NONE', #7840, #4654, #11762 ) ;
#37539=EDGE_CURVE ( 'NONE', #44846, #21976, #30060, .T. ) ;
#37544=CARTESIAN_POINT ( 'NONE',  ( 5.000000000000000000, -27.75498641678720446, -31.52238457039628727 ) ) ;
#37567=ORIENTED_EDGE ( 'NONE', *, *, #37539, .T. ) ;
#37569=VECTOR ( 'NONE', #37063, 1000.000000000000000 ) ;
#37570=AXIS2_PLACEMENT_3D ( 'NONE', #20602, #21574, #6647 ) ;
#37575=EDGE_LOOP ( 'NONE', ( #18774, #11845, #38797, #22425 ) ) ;
#37585=CARTESIAN_POINT ( 'NONE',  ( -3.000000000000000000, 6.762365576493643893, -25.66652317338391853 ) ) ;
#37590=DIRECTION ( 'NONE',  ( 0.000000000000000000, -0.4999999999999920064, -0.8660254037844432595 ) ) ;
#37592=EDGE_LOOP ( 'NONE', ( #41672, #41293, #14911, #19128 ) ) ;
#37605=DIRECTION ( 'NONE',  ( -1.000000000000000000, 0.000000000000000000, 0.000000000000000000 ) ) ;
#37607=AXIS2_PLACEMENT_3D ( 'NONE', #1262, #4683, #27689 ) ;
#37613=CIRCLE ( 'NONE', #16507, 37.49900000000000233 ) ;
#37618=AXIS2_PLACEMENT_3D ( 'NONE', #13711, #14907, #48424 ) ;
#37619=AXIS2_PLACEMENT_3D ( 'NONE', #36693, #5901, #32318 ) ;
#37622=EDGE_CURVE ( 'NONE', #38863, #960, #33478, .T. ) ;
#37625=CARTESIAN_POINT ( 'NONE',  ( -3.000000000000000000, 23.50000000000000000, -1.500000000000001332 ) ) ;
#37632=AXIS2_PLACEMENT_3D ( 'NONE', #24911, #9261, #46953 ) ;
#37634=VERTEX_POINT ( 'NONE', #12195 ) ;
#37637=ORIENTED_EDGE ( 'NONE', *, *, #41725, .F. ) ;
#37649=VERTEX_POINT ( 'NONE', #8732 ) ;
#37651=ORIENTED_EDGE ( 'NONE', *, *, #965, .T. ) ;
#37664=ORIENTED_EDGE ( 'NONE', *, *, #34742, .F. ) ;
#37669=ORIENTED_EDGE ( 'NONE', *, *, #14149, .T. ) ;
#37672=DIRECTION ( 'NONE',  ( -1.000000000000000000, 0.000000000000000000, 0.000000000000000000 ) ) ;
#37678=CARTESIAN_POINT ( 'NONE',  ( -3.000000000000000000, 14.60985201121704513, 18.46759930825707841 ) ) ;
#37694=CARTESIAN_POINT ( 'NONE',  ( -10.00000000000000000, 0.000000000000000000, 0.000000000000000000 ) ) ;
#37698=AXIS2_PLACEMENT_3D ( 'NONE', #23347, #38282, #1070 ) ;
#37712=CARTESIAN_POINT ( 'NONE',  ( 0.000000000000000000, 37.22597642581158084, -5.202137450156524068 ) ) ;
#37723=DIRECTION ( 'NONE',  ( 0.000000000000000000, -0.8660254037844363761, -0.5000000000000039968 ) ) ;
#37729=CARTESIAN_POINT ( 'NONE',  ( 4.999999999999999112, 9.188173127307898369, -40.98264845739739570 ) ) ;
#37733=CARTESIAN_POINT ( 'NONE',  ( -3.000000000000000000, 0.000000000000000000, 0.000000000000000000 ) ) ;
#37739=LINE ( 'NONE', #11567, #15839 ) ;
#37743=FACE_OUTER_BOUND ( 'NONE', #31708, .T. ) ;
#37756=ORIENTED_EDGE ( 'NONE', *, *, #109, .T. ) ;
#37760=EDGE_LOOP ( 'NONE', ( #20394, #6243, #20165, #1529 ) ) ;
#37766=ORIENTED_EDGE ( 'NONE', *, *, #12447, .F. ) ;
#37767=VECTOR ( 'NONE', #27227, 1000.000000000000000 ) ;
#37769=DIRECTION ( 'NONE',  ( 0.000000000000000000, 0.000000000000000000, 1.000000000000000000 ) ) ;
#37776=ORIENTED_EDGE ( 'NONE', *, *, #24577, .F. ) ;
#37793=CARTESIAN_POINT ( 'NONE',  ( 10.00000000000000000, 0.000000000000000000, 0.000000000000000000 ) ) ;
#37805=DIRECTION ( 'NONE',  ( -1.000000000000000000, 0.000000000000000000, -0.000000000000000000 ) ) ;
#37810=CARTESIAN_POINT ( 'NONE',  ( 10.00000000000000000, -37.58145647212455032, 0.6853352020789044152 ) ) ;
#37817=DIRECTION ( 'NONE',  ( -1.000000000000000000, 0.000000000000000000, 0.000000000000000000 ) ) ;
#37819=AXIS2_PLACEMENT_3D ( 'NONE', #2394, #9266, #32270 ) ;
#37832=DIRECTION ( 'NONE',  ( -1.000000000000000000, 0.000000000000000000, 0.000000000000000000 ) ) ;
#37835=ORIENTED_EDGE ( 'NONE', *, *, #22217, .F. ) ;
#37837=DIRECTION ( 'NONE',  ( 0.000000000000000000, 0.000000000000000000, 1.000000000000000000 ) ) ;
#37856=DIRECTION ( 'NONE',  ( -1.000000000000000000, 0.000000000000000000, 0.000000000000000000 ) ) ;
#37861=EDGE_CURVE ( 'NONE', #38863, #44846, #17928, .T. ) ;
#37862=EDGE_CURVE ( 'NONE', #30321, #26404, #33588, .T. ) ;
#37890=ADVANCED_FACE ( 'NONE', ( #28559 ), #32472, .F. ) ;
#37893=DIRECTION ( 'NONE',  ( -1.000000000000000000, 0.000000000000000000, 0.000000000000000000 ) ) ;
#37901=VECTOR ( 'NONE', #32155, 999.9999999999998863 ) ;
#37908=AXIS2_PLACEMENT_3D ( 'NONE', #24613, #46889, #28272 ) ;
#37912=LINE ( 'NONE', #928, #32172 ) ;
#37915=VERTEX_POINT ( 'NONE', #26565 ) ;
#37925=VECTOR ( 'NONE', #4620, 1000.000000000000000 ) ;
#37927=DIRECTION ( 'NONE',  ( 0.000000000000000000, 0.000000000000000000, 1.000000000000000000 ) ) ;
#37934=CIRCLE ( 'NONE', #11354, 21.00000000000000000 ) ;
#37938=CIRCLE ( 'NONE', #37129, 16.00000000000000000 ) ;
#37942=ORIENTED_EDGE ( 'NONE', *, *, #40914, .T. ) ;
#37951=DIRECTION ( 'NONE',  ( -1.000000000000000000, -0.000000000000000000, 0.000000000000000000 ) ) ;
#37955=CARTESIAN_POINT ( 'NONE',  ( 5.000000000000000000, 35.47612816024523852, 22.48208911017513145 ) ) ;
#37971=CARTESIAN_POINT ( 'NONE',  ( 10.00000000000000000, 0.000000000000000000, 0.000000000000000000 ) ) ;
#37975=VECTOR ( 'NONE', #29247, 1000.000000000000000 ) ;
#37994=CARTESIAN_POINT ( 'NONE',  ( -3.000000000000000000, 5.835314593368772229, -22.81335362449846826 ) ) ;
#38007=VECTOR ( 'NONE', #21461, 1000.000000000000000 ) ;
#38017=EDGE_CURVE ( 'NONE', #8792, #34171, #849, .T. ) ;
#38019=CIRCLE ( 'NONE', #1302, 16.00000000000000000 ) ;
#38020=ADVANCED_FACE ( 'NONE', ( #29751 ), #45648, .T. ) ;
#38027=DIRECTION ( 'NONE',  ( -1.000000000000000000, 0.000000000000000000, -0.000000000000000000 ) ) ;
#38033=EDGE_CURVE ( 'NONE', #45751, #31219, #33897, .T. ) ;
#38035=LINE ( 'NONE', #34331, #26184 ) ;
#38051=CARTESIAN_POINT ( 'NONE',  ( 10.00000000000000000, -22.64427369931191336, 30.00120703465197280 ) ) ;
#38053=EDGE_CURVE ( 'NONE', #22253, #5635, #12533, .T. ) ;
#38058=EDGE_LOOP ( 'NONE', ( #37567, #15357, #27130, #32737 ) ) ;
#38063=EDGE_CURVE ( 'NONE', #3614, #46270, #27380, .T. ) ;
#38076=CARTESIAN_POINT ( 'NONE',  ( 0.000000000000000000, -18.13022148937263012, 15.02647892043544608 ) ) ;
#38080=EDGE_LOOP ( 'NONE', ( #39226, #29861, #20581, #13366 ) ) ;
#38084=ORIENTED_EDGE ( 'NONE', *, *, #2827, .T. ) ;
#38098=DIRECTION ( 'NONE',  ( 0.000000000000000000, 0.6691306063588676745, -0.7431448254773856954 ) ) ;
#38102=PLANE ( 'NONE',  #33247 ) ;
#38104=VERTEX_POINT ( 'NONE', #28023 ) ;
#38112=VERTEX_POINT ( 'NONE', #42214 ) ;
#38113=LINE ( 'NONE', #22463, #31023 ) ;
#38122=DIRECTION ( 'NONE',  ( -1.000000000000000000, -0.000000000000000000, -0.000000000000000000 ) ) ;
#38131=EDGE_CURVE ( 'NONE', #32654, #29523, #776, .T. ) ;
#38135=CARTESIAN_POINT ( 'NONE',  ( 10.00000000000000000, 0.000000000000000000, 0.000000000000000000 ) ) ;
#38136=ORIENTED_EDGE ( 'NONE', *, *, #36523, .F. ) ;
#38144=AXIS2_PLACEMENT_3D ( 'NONE', #10345, #16316, #46173 ) ;
#38154=DIRECTION ( 'NONE',  ( 0.000000000000000000, -0.7431448254773954654, 0.6691306063588569053 ) ) ;
#38158=DIRECTION ( 'NONE',  ( 0.000000000000000000, -0.2079116908177532363, -0.9781476007338070211 ) ) ;
#38165=CARTESIAN_POINT ( 'NONE',  ( 10.00000000000000000, 10.96151621346540317, -35.95386929396244113 ) ) ;
#38171=ORIENTED_EDGE ( 'NONE', *, *, #36070, .F. ) ;
#38178=VECTOR ( 'NONE', #10446, 1000.000000000000000 ) ;
#38182=EDGE_CURVE ( 'NONE', #25221, #41422, #25023, .T. ) ;
#38183=VERTEX_POINT ( 'NONE', #35604 ) ;
#38195=CARTESIAN_POINT ( 'NONE',  ( 10.00000000000000000, 36.88895765772642932, -6.736453364083163642 ) ) ;
#38197=LINE ( 'NONE', #37955, #41576 ) ;
#38201=ORIENTED_EDGE ( 'NONE', *, *, #23250, .T. ) ;
#38203=ORIENTED_EDGE ( 'NONE', *, *, #23990, .T. ) ;
#38207=FACE_OUTER_BOUND ( 'NONE', #27184, .T. ) ;
#38228=CYLINDRICAL_SURFACE ( 'NONE', #43232, 16.00000000000000000 ) ;
#38237=VERTEX_POINT ( 'NONE', #17715 ) ;
#38246=AXIS2_PLACEMENT_3D ( 'NONE', #23917, #42272, #38614 ) ;
#38249=EDGE_CURVE ( 'NONE', #28893, #21133, #14056, .T. ) ;
#38256=CARTESIAN_POINT ( 'NONE',  ( 4.999999999999999112, -41.91543099594816368, -2.663952781846588014 ) ) ;
#38257=CYLINDRICAL_SURFACE ( 'NONE', #41106, 15.99999999999999645 ) ;
#38260=FACE_OUTER_BOUND ( 'NONE', #38809, .T. ) ;
#38266=DIRECTION ( 'NONE',  ( -0.000000000000000000, -0.8660254037844427044, 0.4999999999999929501 ) ) ;
#38278=CARTESIAN_POINT ( 'NONE',  ( 10.00000000000000000, 0.000000000000000000, 0.000000000000000000 ) ) ;
#38280=DIRECTION ( 'NONE',  ( 0.000000000000000000, -0.9876883405951393247, 0.1564344650402205161 ) ) ;
#38282=DIRECTION ( 'NONE',  ( -1.000000000000000000, -0.000000000000000000, -0.000000000000000000 ) ) ;
#38288=CIRCLE ( 'NONE', #17142, 16.00000000000000711 ) ;
#38293=CARTESIAN_POINT ( 'NONE',  ( -3.000000000000000000, 18.84667830672605859, -18.68964196561243796 ) ) ;
#38305=CARTESIAN_POINT ( 'NONE',  ( 10.00000000000000000, -16.45098606841102651, -33.79645857604531045 ) ) ;
#38315=FACE_OUTER_BOUND ( 'NONE', #37223, .T. ) ;
#38321=DIRECTION ( 'NONE',  ( -1.000000000000000000, -0.000000000000000000, -0.000000000000000000 ) ) ;
#38330=LINE ( 'NONE', #27816, #43041 ) ;
#38333=CARTESIAN_POINT ( 'NONE',  ( 10.00000000000000000, 0.8828120875900632436, 37.48860685352291000 ) ) ;
#38340=DIRECTION ( 'NONE',  ( -1.000000000000000000, 0.000000000000000000, 0.000000000000000000 ) ) ;
#38341=CARTESIAN_POINT ( 'NONE',  ( -3.000000000000000000, -20.55727247249748046, 16.78983467731285018 ) ) ;
#38342=CARTESIAN_POINT ( 'NONE',  ( 10.00000000000000000, -35.38097989696520074, 12.42422080174625520 ) ) ;
#38344=DIRECTION ( 'NONE',  ( 1.000000000000000000, -0.000000000000000000, -0.000000000000000000 ) ) ;
#38345=CARTESIAN_POINT ( 'NONE',  ( 10.00000000000000000, -10.74501242461308159, 35.92658777277507909 ) ) ;
#38352=VERTEX_POINT ( 'NONE', #26017 ) ;
#38364=EDGE_LOOP ( 'NONE', ( #33606, #30309, #6500, #32486 ) ) ;
#38377=LINE ( 'NONE', #5336, #20810 ) ;
#38380=DIRECTION ( 'NONE',  ( -1.000000000000000000, 0.000000000000000000, -0.000000000000000000 ) ) ;
#38385=LINE ( 'NONE', #7374, #4941 ) ;
#38396=VERTEX_POINT ( 'NONE', #48056 ) ;
#38405=EDGE_CURVE ( 'NONE', #32185, #44060, #14775, .T. ) ;
#38407=EDGE_CURVE ( 'NONE', #17279, #7503, #44869, .T. ) ;
#38425=VERTEX_POINT ( 'NONE', #4246 ) ;
#38440=DIRECTION ( 'NONE',  ( 0.000000000000000000, 0.5877852522924741363, -0.8090169943749465631 ) ) ;
#38445=DIRECTION ( 'NONE',  ( 0.000000000000000000, 0.000000000000000000, -1.000000000000000000 ) ) ;
#38451=EDGE_CURVE ( 'NONE', #12245, #6771, #3999, .T. ) ;
#38456=EDGE_CURVE ( 'NONE', #29827, #11046, #10977, .T. ) ;
#38463=DIRECTION ( 'NONE',  ( 1.000000000000000000, -0.000000000000000000, -0.000000000000000000 ) ) ;
#38474=ORIENTED_EDGE ( 'NONE', *, *, #4162, .T. ) ;
#38475=DIRECTION ( 'NONE',  ( 0.000000000000000000, 0.5877852522924685852, 0.8090169943749508930 ) ) ;
#38479=CARTESIAN_POINT ( 'NONE',  ( 10.00000000000000000, -33.79645857604501913, -16.45098606841161626 ) ) ;
#38491=CYLINDRICAL_SURFACE ( 'NONE', #28569, 42.00000000000000000 ) ;
#38500=CARTESIAN_POINT ( 'NONE',  ( 10.00000000000000000, -37.22597642581153821, -5.202137450156795850 ) ) ;
#38512=DIRECTION ( 'NONE',  ( -0.000000000000000000, 0.9945218953682731788, 0.1045284632676559550 ) ) ;
#38516=ADVANCED_FACE ( 'NONE', ( #38748 ), #1030, .T. ) ;
#38522=AXIS2_PLACEMENT_3D ( 'NONE', #37971, #8817, #23510 ) ;
#38526=LINE ( 'NONE', #38783, #27158 ) ;
#38532=ADVANCED_FACE ( 'NONE', ( #46318 ), #5215, .T. ) ;
#38533=ORIENTED_EDGE ( 'NONE', *, *, #36932, .F. ) ;
#38539=DIRECTION ( 'NONE',  ( 0.000000000000000000, 0.000000000000000000, 1.000000000000000000 ) ) ;
#38540=VECTOR ( 'NONE', #29202, 1000.000000000000000 ) ;
#38552=CIRCLE ( 'NONE', #44793, 42.00000000000000000 ) ;
#38564=VECTOR ( 'NONE', #14281, 1000.000000000000000 ) ;
#38566=ORIENTED_EDGE ( 'NONE', *, *, #29243, .T. ) ;
#38571=EDGE_CURVE ( 'NONE', #37634, #1618, #31652, .T. ) ;
#38572=CARTESIAN_POINT ( 'NONE',  ( -3.000000000000000000, 22.07842321921492612, -8.187992925817130896 ) ) ;
#38582=FACE_OUTER_BOUND ( 'NONE', #35470, .T. ) ;
#38583=FACE_OUTER_BOUND ( 'NONE', #12411, .T. ) ;
#38588=CARTESIAN_POINT ( 'NONE',  ( -3.000000000000000000, -23.29833615347104825, -3.418703333116803744 ) ) ;
#38590=CARTESIAN_POINT ( 'NONE',  ( 0.000000000000000000, 0.000000000000000000, 0.000000000000000000 ) ) ;
#38595=DIRECTION ( 'NONE',  ( 0.000000000000000000, -0.7071067811865389130, -0.7071067811865561215 ) ) ;
#38597=EDGE_CURVE ( 'NONE', #22836, #1330, #1297, .T. ) ;
#38609=EDGE_LOOP ( 'NONE', ( #37166, #42201, #40233, #18196 ) ) ;
#38614=DIRECTION ( 'NONE',  ( 0.000000000000000000, 0.5877852522924684742, 0.8090169943749506709 ) ) ;
#38617=ORIENTED_EDGE ( 'NONE', *, *, #17913, .T. ) ;
#38620=ORIENTED_EDGE ( 'NONE', *, *, #629, .F. ) ;
#38623=DIRECTION ( 'NONE',  ( -1.000000000000000000, -0.000000000000000000, 0.000000000000000000 ) ) ;
#38628=VERTEX_POINT ( 'NONE', #34811 ) ;
#38640=LINE ( 'NONE', #6072, #42438 ) ;
#38643=ADVANCED_FACE ( 'NONE', ( #10564 ), #28905, .T. ) ;
#38644=ORIENTED_EDGE ( 'NONE', *, *, #38033, .T. ) ;
#38659=DIRECTION ( 'NONE',  ( 1.000000000000000000, -0.000000000000000000, 0.000000000000000000 ) ) ;
#38668=FACE_OUTER_BOUND ( 'NONE', #5291, .T. ) ;
#38669=ORIENTED_EDGE ( 'NONE', *, *, #27712, .F. ) ;
#38686=ORIENTED_EDGE ( 'NONE', *, *, #6454, .F. ) ;
#38688=EDGE_LOOP ( 'NONE', ( #23682, #37766, #38201, #38848 ) ) ;
#38696=CARTESIAN_POINT ( 'NONE',  ( -10.00000000000000000, 0.000000000000000000, 0.000000000000000000 ) ) ;
#38701=CARTESIAN_POINT ( 'NONE',  ( 10.00000000000000000, 30.84782396557248418, -21.32104025579081252 ) ) ;
#38706=VERTEX_POINT ( 'NONE', #36494 ) ;
#38707=FACE_OUTER_BOUND ( 'NONE', #23551, .T. ) ;
#38723=LINE ( 'NONE', #5184, #25589 ) ;
#38736=DIRECTION ( 'NONE',  ( -1.000000000000000000, 0.000000000000000000, -0.000000000000000000 ) ) ;
#38739=CARTESIAN_POINT ( 'NONE',  ( 10.00000000000000000, 37.58145647212455032, -0.6853352020786441789 ) ) ;
#38742=ORIENTED_EDGE ( 'NONE', *, *, #42011, .F. ) ;
#38745=AXIS2_PLACEMENT_3D ( 'NONE', #10134, #48299, #43671 ) ;
#38746=DIRECTION ( 'NONE',  ( 0.000000000000000000, 0.4539904997395479702, -0.8910065241883673437 ) ) ;
#38747=VERTEX_POINT ( 'NONE', #6403 ) ;
#38748=FACE_OUTER_BOUND ( 'NONE', #29562, .T. ) ;
#38749=ORIENTED_EDGE ( 'NONE', *, *, #23369, .F. ) ;
#38754=CARTESIAN_POINT ( 'NONE',  ( 0.000000000000000000, -17.80606268964516659, -33.00180498840066434 ) ) ;
#38768=DIRECTION ( 'NONE',  ( 1.000000000000000000, -0.000000000000000000, 0.000000000000000000 ) ) ;
#38770=EDGE_CURVE ( 'NONE', #22704, #13285, #24263, .T. ) ;
#38775=VECTOR ( 'NONE', #2819, 1000.000000000000000 ) ;
#38783=CARTESIAN_POINT ( 'NONE',  ( 0.000000000000000000, -10.45096189432344147, 21.10159698893426494 ) ) ;
#38785=DIRECTION ( 'NONE',  ( -1.000000000000000000, -0.000000000000000000, 0.000000000000000000 ) ) ;
#38797=ORIENTED_EDGE ( 'NONE', *, *, #26364, .F. ) ;
#38800=VERTEX_POINT ( 'NONE', #45964 ) ;
#38801=AXIS2_PLACEMENT_3D ( 'NONE', #2253, #28442, #17172 ) ;
#38808=CARTESIAN_POINT ( 'NONE',  ( 0.000000000000000000, 0.000000000000000000, 0.000000000000000000 ) ) ;
#38809=EDGE_LOOP ( 'NONE', ( #41811, #40643, #11870, #18675 ) ) ;
#38810=FACE_OUTER_BOUND ( 'NONE', #36684, .T. ) ;
#38812=EDGE_CURVE ( 'NONE', #3154, #41890, #11949, .T. ) ;
#38819=ORIENTED_EDGE ( 'NONE', *, *, #27180, .F. ) ;
#38827=CARTESIAN_POINT ( 'NONE',  ( 10.00000000000000000, -37.01155633439063308, 6.555932627142289526 ) ) ;
#38828=LINE ( 'NONE', #8946, #10982 ) ;
#38831=VERTEX_POINT ( 'NONE', #907 ) ;
#38832=CARTESIAN_POINT ( 'NONE',  ( 0.000000000000000000, -13.04903810567675038, 19.60159698893425428 ) ) ;
#38841=DIRECTION ( 'NONE',  ( 0.000000000000000000, 0.9876883405951372152, 0.1564344650402347547 ) ) ;
#38848=ORIENTED_EDGE ( 'NONE', *, *, #22823, .T. ) ;
#38854=VERTEX_POINT ( 'NONE', #11701 ) ;
#38856=VECTOR ( 'NONE', #31812, 1000.000000000000000 ) ;
#38863=VERTEX_POINT ( 'NONE', #45000 ) ;
#38867=EDGE_CURVE ( 'NONE', #30648, #36833, #44624, .T. ) ;
#38868=EDGE_CURVE ( 'NONE', #11582, #12094, #3998, .T. ) ;
#38870=DIRECTION ( 'NONE',  ( -0.000000000000000000, -0.5877852522924789103, 0.8090169943749432324 ) ) ;
#38874=ORIENTED_EDGE ( 'NONE', *, *, #37007, .F. ) ;
#38878=EDGE_LOOP ( 'NONE', ( #37637, #47393, #24910, #32824 ) ) ;
#38881=EDGE_LOOP ( 'NONE', ( #7283, #29867, #28064, #35944 ) ) ;
#38886=VERTEX_POINT ( 'NONE', #19743 ) ;
#38890=VECTOR ( 'NONE', #15995, 1000.000000000000000 ) ;
#38898=CARTESIAN_POINT ( 'NONE',  ( -3.000000000000000000, -23.29833615347104825, -3.418703333116803744 ) ) ;
#38918=ADVANCED_FACE ( 'NONE', ( #15390 ), #4375, .F. ) ;
#38921=AXIS2_PLACEMENT_3D ( 'NONE', #20738, #35413, #12672 ) ;
#38923=ORIENTED_EDGE ( 'NONE', *, *, #16762, .F. ) ;
#38941=ADVANCED_FACE ( 'NONE', ( #20739 ), #9708, .F. ) ;
#38950=CARTESIAN_POINT ( 'NONE',  ( -3.000000000000000000, 22.07842321921481243, 8.187992925817422218 ) ) ;
#38952=DIRECTION ( 'NONE',  ( 0.000000000000000000, 0.000000000000000000, 1.000000000000000000 ) ) ;
#38966=ORIENTED_EDGE ( 'NONE', *, *, #44310, .F. ) ;
#39002=CARTESIAN_POINT ( 'NONE',  ( 10.00000000000000000, 0.000000000000000000, 0.000000000000000000 ) ) ;
#39004=CARTESIAN_POINT ( 'NONE',  ( 10.00000000000000000, 21.32104025579158701, -30.84782396557194772 ) ) ;
#39007=EDGE_CURVE ( 'NONE', #35670, #7892, #20973, .T. ) ;
#39013=ORIENTED_EDGE ( 'NONE', *, *, #1455, .F. ) ;
#39016=VECTOR ( 'NONE', #39148, 1000.000000000000114 ) ;
#39037=VERTEX_POINT ( 'NONE', #5331 ) ;
#39046=DIRECTION ( 'NONE',  ( -1.000000000000000000, 0.000000000000000000, 0.000000000000000000 ) ) ;
#39050=DIRECTION ( 'NONE',  ( 0.000000000000000000, -0.8090169943749504489, 0.5877852522924689183 ) ) ;
#39066=DIRECTION ( 'NONE',  ( -1.000000000000000000, 0.000000000000000000, 0.000000000000000000 ) ) ;
#39067=DIRECTION ( 'NONE',  ( -1.000000000000000000, -0.000000000000000000, -0.000000000000000000 ) ) ;
#39080=ORIENTED_EDGE ( 'NONE', *, *, #39259, .T. ) ;
#39084=VECTOR ( 'NONE', #7354, 1000.000000000000000 ) ;
#39088=EDGE_LOOP ( 'NONE', ( #47724, #25342, #29986, #14955 ) ) ;
#39097=ORIENTED_EDGE ( 'NONE', *, *, #41350, .F. ) ;
#39101=LINE ( 'NONE', #28090, #16144 ) ;
#39104=DIRECTION ( 'NONE',  ( 0.000000000000000000, 0.9510565162951544194, -0.3090169943749447867 ) ) ;
#39108=DIRECTION ( 'NONE',  ( -1.000000000000000000, -0.000000000000000000, 0.000000000000000000 ) ) ;
#39120=CIRCLE ( 'NONE', #17221, 16.00000000000000000 ) ;
#39122=DIRECTION ( 'NONE',  ( -1.000000000000000000, -0.000000000000000000, 0.000000000000000000 ) ) ;
#39127=AXIS2_PLACEMENT_3D ( 'NONE', #33056, #48235, #43836 ) ;
#39128=DIRECTION ( 'NONE',  ( 0.000000000000000000, 0.000000000000000000, -1.000000000000000000 ) ) ;
#39133=CARTESIAN_POINT ( 'NONE',  ( 10.00000000000000000, -16.23288003029473359, -33.80338159004301701 ) ) ;
#39141=ORIENTED_EDGE ( 'NONE', *, *, #45479, .T. ) ;
#39144=ORIENTED_EDGE ( 'NONE', *, *, #21905, .F. ) ;
#39148=DIRECTION ( 'NONE',  ( 0.000000000000000000, 0.3090169943749442316, 0.9510565162951545304 ) ) ;
#39153=ORIENTED_EDGE ( 'NONE', *, *, #30908, .T. ) ;
#39155=CARTESIAN_POINT ( 'NONE',  ( 10.00000000000000000, 0.000000000000000000, 0.000000000000000000 ) ) ;
#39162=DIRECTION ( 'NONE',  ( 0.000000000000000000, 0.000000000000000000, 1.000000000000000000 ) ) ;
#39166=CARTESIAN_POINT ( 'NONE',  ( 0.000000000000000000, -32.34446384429951138, -26.79245525562750530 ) ) ;
#39169=ORIENTED_EDGE ( 'NONE', *, *, #2220, .F. ) ;
#39188=CARTESIAN_POINT ( 'NONE',  ( 0.000000000000000000, -0.9646360437372163421, -23.52805723605591126 ) ) ;
#39190=AXIS2_PLACEMENT_3D ( 'NONE', #14115, #47632, #20741 ) ;
#39195=CARTESIAN_POINT ( 'NONE',  ( 0.000000000000000000, 14.60985201121704513, 18.46759930825707841 ) ) ;
#39209=CARTESIAN_POINT ( 'NONE',  ( -10.00000000000000000, 0.000000000000000000, 0.000000000000000000 ) ) ;
#39215=CARTESIAN_POINT ( 'NONE',  ( -3.000000000000000000, -14.54903810567645195, -22.19967320028775504 ) ) ;
#39225=FACE_OUTER_BOUND ( 'NONE', #9990, .T. ) ;
#39226=ORIENTED_EDGE ( 'NONE', *, *, #45630, .T. ) ;
#39231=DIRECTION ( 'NONE',  ( 0.000000000000000000, 0.000000000000000000, 1.000000000000000000 ) ) ;
#39235=DIRECTION ( 'NONE',  ( -1.000000000000000000, 0.000000000000000000, 0.000000000000000000 ) ) ;
#39236=DIRECTION ( 'NONE',  ( 0.000000000000000000, -0.3090169943749349057, -0.9510565162951577500 ) ) ;
#39240=ADVANCED_FACE ( 'NONE', ( #38315 ), #4314, .F. ) ;
#39255=VECTOR ( 'NONE', #12266, 1000.000000000000000 ) ;
#39257=CIRCLE ( 'NONE', #8738, 16.00000000000000000 ) ;
#39259=EDGE_CURVE ( 'NONE', #34495, #30209, #30581, .T. ) ;
#39262=EDGE_CURVE ( 'NONE', #25211, #40387, #627, .T. ) ;
#39271=PLANE ( 'NONE',  #32130 ) ;
#39276=CIRCLE ( 'NONE', #19726, 15.99999999999999822 ) ;
#39286=DIRECTION ( 'NONE',  ( 0.000000000000000000, 0.5877852522924685852, 0.8090169943749508930 ) ) ;
#39288=ADVANCED_FACE ( 'NONE', ( #15801 ), #130, .T. ) ;
#39290=CIRCLE ( 'NONE', #15051, 15.99999999999999645 ) ;
#39292=DIRECTION ( 'NONE',  ( 0.000000000000000000, 0.000000000000000000, 1.000000000000000000 ) ) ;
#39294=LINE ( 'NONE', #9425, #25934 ) ;
#39296=VERTEX_POINT ( 'NONE', #44685 ) ;
#39301=AXIS2_PLACEMENT_3D ( 'NONE', #12359, #8193, #16028 ) ;
#39304=LINE ( 'NONE', #32451, #18242 ) ;
#39309=ORIENTED_EDGE ( 'NONE', *, *, #30786, .T. ) ;
#39312=AXIS2_PLACEMENT_3D ( 'NONE', #32161, #13551, #47080 ) ;
#39331=ORIENTED_EDGE ( 'NONE', *, *, #40417, .T. ) ;
#39339=ORIENTED_EDGE ( 'NONE', *, *, #9558, .T. ) ;
#39345=CARTESIAN_POINT ( 'NONE',  ( 0.000000000000000000, 27.75498641678786527, -31.52238457039571173 ) ) ;
#39347=AXIS2_PLACEMENT_3D ( 'NONE', #39450, #6870, #13488 ) ;
#39348=EDGE_CURVE ( 'NONE', #390, #37389, #19622, .T. ) ;
#39349=CARTESIAN_POINT ( 'NONE',  ( 0.000000000000000000, -37.48860685352291711, 0.8828120875899322373 ) ) ;
#39350=VERTEX_POINT ( 'NONE', #26340 ) ;
#39365=CIRCLE ( 'NONE', #5749, 42.00000000000000000 ) ;
#39367=CARTESIAN_POINT ( 'NONE',  ( 10.00000000000000000, -30.00120703465222149, 22.64427369931158296 ) ) ;
#39372=CARTESIAN_POINT ( 'NONE',  ( -3.000000000000000000, -0.9646360437375307573, 23.52805723605590060 ) ) ;
#39387=DIRECTION ( 'NONE',  ( -1.000000000000000000, -0.000000000000000000, 0.000000000000000000 ) ) ;
#39388=VERTEX_POINT ( 'NONE', #23870 ) ;
#39389=AXIS2_PLACEMENT_3D ( 'NONE', #45894, #23847, #12358 ) ;
#39403=VECTOR ( 'NONE', #29069, 999.9999999999998863 ) ;
#39409=AXIS2_PLACEMENT_3D ( 'NONE', #14214, #29617, #32344 ) ;
#39410=AXIS2_PLACEMENT_3D ( 'NONE', #20436, #13113, #43206 ) ;
#39411=LINE ( 'NONE', #28143, #27785 ) ;
#39416=DIRECTION ( 'NONE',  ( -1.000000000000000000, -0.000000000000000000, -0.000000000000000000 ) ) ;
#39417=EDGE_CURVE ( 'NONE', #28664, #47099, #21971, .T. ) ;
#39425=DIRECTION ( 'NONE',  ( 0.000000000000000000, 0.000000000000000000, 1.000000000000000000 ) ) ;
#39433=AXIS2_PLACEMENT_3D ( 'NONE', #7575, #4145, #11972 ) ;
#39435=LINE ( 'NONE', #20101, #3628 ) ;
#39445=ORIENTED_EDGE ( 'NONE', *, *, #5310, .F. ) ;
#39450=CARTESIAN_POINT ( 'NONE',  ( -3.000000000000000000, -0.9646360437372163421, -23.52805723605591126 ) ) ;
#39454=EDGE_LOOP ( 'NONE', ( #45564, #44825, #6898, #16705 ) ) ;
#39459=CARTESIAN_POINT ( 'NONE',  ( 10.00000000000000000, -27.05870788708250885, 26.08949754953014022 ) ) ;
#39461=VERTEX_POINT ( 'NONE', #13101 ) ;
#39462=DIRECTION ( 'NONE',  ( 1.000000000000000000, -0.000000000000000000, -0.000000000000000000 ) ) ;
#39467=ORIENTED_EDGE ( 'NONE', *, *, #2422, .F. ) ;
#39470=ORIENTED_EDGE ( 'NONE', *, *, #27801, .F. ) ;
#39472=ORIENTED_EDGE ( 'NONE', *, *, #5826, .T. ) ;
#39487=CARTESIAN_POINT ( 'NONE',  ( -3.000000000000000000, 20.85821328998756385, -10.92862929874494959 ) ) ;
#39492=DIRECTION ( 'NONE',  ( 1.000000000000000000, 0.000000000000000000, 0.000000000000000000 ) ) ;
#39503=AXIS2_PLACEMENT_3D ( 'NONE', #17143, #25444, #36226 ) ;
#39520=ORIENTED_EDGE ( 'NONE', *, *, #41461, .F. ) ;
#39525=EDGE_CURVE ( 'NONE', #5144, #41422, #10378, .T. ) ;
#39527=EDGE_CURVE ( 'NONE', #39726, #22743, #13394, .T. ) ;
#39536=AXIS2_PLACEMENT_3D ( 'NONE', #13907, #17809, #36419 ) ;
#39541=EDGE_CURVE ( 'NONE', #21082, #35343, #10636, .T. ) ;
#39543=AXIS2_PLACEMENT_3D ( 'NONE', #19130, #8586, #34058 ) ;
#39545=ORIENTED_EDGE ( 'NONE', *, *, #44199, .T. ) ;
#39547=ORIENTED_EDGE ( 'NONE', *, *, #46732, .F. ) ;
#39552=DIRECTION ( 'NONE',  ( -1.000000000000000000, -0.000000000000000000, -0.000000000000000000 ) ) ;
#39554=DIRECTION ( 'NONE',  ( 1.000000000000000000, -0.000000000000000000, -0.000000000000000000 ) ) ;
#39557=CARTESIAN_POINT ( 'NONE',  ( 0.000000000000000000, 12.42422080174638310, 35.38097989696515810 ) ) ;
#39566=VECTOR ( 'NONE', #43625, 1000.000000000000000 ) ;
#39581=CIRCLE ( 'NONE', #2832, 42.00000000000000000 ) ;
#39593=ORIENTED_EDGE ( 'NONE', *, *, #42204, .F. ) ;
#39597=CYLINDRICAL_SURFACE ( 'NONE', #38921, 16.00000000000000000 ) ;
#39608=CARTESIAN_POINT ( 'NONE',  ( 10.00000000000000000, -22.48208911017474065, -35.47612816024548721 ) ) ;
#39616=VECTOR ( 'NONE', #36166, 1000.000000000000000 ) ;
#39619=CARTESIAN_POINT ( 'NONE',  ( 0.000000000000000000, -29.81001611430991360, -22.74946021919165418 ) ) ;
#39623=DIRECTION ( 'NONE',  ( -1.000000000000000000, 0.000000000000000000, 0.000000000000000000 ) ) ;
#39627=AXIS2_PLACEMENT_3D ( 'NONE', #17235, #42728, #36089 ) ;
#39629=CARTESIAN_POINT ( 'NONE',  ( 0.000000000000000000, -18.13022148937263012, 15.02647892043544608 ) ) ;
#39638=EDGE_CURVE ( 'NONE', #13990, #29283, #34511, .T. ) ;
#39639=CIRCLE ( 'NONE', #13849, 37.49900000000000944 ) ;
#39656=CIRCLE ( 'NONE', #18538, 42.00000000000000000 ) ;
#39675=CARTESIAN_POINT ( 'NONE',  ( 0.000000000000000000, -31.52238457039579345, -27.75498641678775158 ) ) ;
#39677=DIRECTION ( 'NONE',  ( 0.000000000000000000, 0.9876883405951382144, -0.1564344650402276493 ) ) ;
#39712=LINE ( 'NONE', #2475, #12567 ) ;
#39714=ORIENTED_EDGE ( 'NONE', *, *, #497, .F. ) ;
#39719=DIRECTION ( 'NONE',  ( 1.000000000000000000, -0.000000000000000000, -0.000000000000000000 ) ) ;
#39720=DIRECTION ( 'NONE',  ( 0.000000000000000000, 0.4539904997395479702, -0.8910065241883673437 ) ) ;
#39726=VERTEX_POINT ( 'NONE', #7674 ) ;
#39729=VECTOR ( 'NONE', #31496, 1000.000000000000000 ) ;
#39735=VECTOR ( 'NONE', #9707, 1000.000000000000000 ) ;
#39756=CARTESIAN_POINT ( 'NONE',  ( 10.00000000000000000, 41.81611651403867569, -3.925862922255714871 ) ) ;
#39758=EDGE_CURVE ( 'NONE', #28940, #47865, #797, .T. ) ;
#39763=AXIS2_PLACEMENT_3D ( 'NONE', #24597, #28512, #37769 ) ;
#39767=DIRECTION ( 'NONE',  ( 0.000000000000000000, -0.3090169943749549453, 0.9510565162951511997 ) ) ;
#39786=DIRECTION ( 'NONE',  ( 0.000000000000000000, 0.000000000000000000, 1.000000000000000000 ) ) ;
#39789=DIRECTION ( 'NONE',  ( 1.000000000000000000, 0.000000000000000000, 0.000000000000000000 ) ) ;
#39792=VECTOR ( 'NONE', #29805, 1000.000000000000000 ) ;
#39794=CIRCLE ( 'NONE', #21011, 16.00000000000000355 ) ;
#39801=LINE ( 'NONE', #21172, #38775 ) ;
#39809=ORIENTED_EDGE ( 'NONE', *, *, #42494, .T. ) ;
#39816=ORIENTED_EDGE ( 'NONE', *, *, #27474, .T. ) ;
#39820=DIRECTION ( 'NONE',  ( -1.000000000000000000, 0.000000000000000000, 0.000000000000000000 ) ) ;
#39824=VERTEX_POINT ( 'NONE', #8621 ) ;
#39829=EDGE_CURVE ( 'NONE', #26069, #40081, #32946, .T. ) ;
#39833=CIRCLE ( 'NONE', #24206, 16.00000000000000000 ) ;
#39837=DIRECTION ( 'NONE',  ( 0.000000000000000000, 0.000000000000000000, 1.000000000000000000 ) ) ;
#39840=DIRECTION ( 'NONE',  ( 0.000000000000000000, 0.000000000000000000, 1.000000000000000000 ) ) ;
#39848=ADVANCED_FACE ( 'NONE', ( #12558 ), #20363, .F. ) ;
#39854=AXIS2_PLACEMENT_3D ( 'NONE', #17854, #32780, #40393 ) ;
#39860=VECTOR ( 'NONE', #6989, 1000.000000000000000 ) ;
#39879=AXIS2_PLACEMENT_3D ( 'NONE', #24335, #27788, #23609 ) ;
#39880=ORIENTED_EDGE ( 'NONE', *, *, #38868, .T. ) ;
#39884=VECTOR ( 'NONE', #47502, 1000.000000000000114 ) ;
#39892=DIRECTION ( 'NONE',  ( 0.000000000000000000, 0.8660254037844363761, 0.5000000000000039968 ) ) ;
#39895=AXIS2_PLACEMENT_3D ( 'NONE', #45070, #30615, #26956 ) ;
#39898=CARTESIAN_POINT ( 'NONE',  ( 5.000000000000000000, 3.925862922256160736, 41.81611651403863306 ) ) ;
#39903=DIRECTION ( 'NONE',  ( 1.000000000000000000, 0.000000000000000000, 0.000000000000000000 ) ) ;
#39904=CARTESIAN_POINT ( 'NONE',  ( -3.000000000000000000, 0.000000000000000000, 0.000000000000000000 ) ) ;
#39906=ADVANCED_FACE ( 'NONE', ( #8543 ), #19321, .F. ) ;
#39909=DIRECTION ( 'NONE',  ( -1.000000000000000000, 0.000000000000000000, -0.000000000000000000 ) ) ;
#39922=PLANE ( 'NONE',  #18998 ) ;
#39927=ORIENTED_EDGE ( 'NONE', *, *, #1900, .T. ) ;
#39937=EDGE_CURVE ( 'NONE', #7735, #1412, #26867, .T. ) ;
#39945=ORIENTED_EDGE ( 'NONE', *, *, #12231, .F. ) ;
#39946=DIRECTION ( 'NONE',  ( 0.000000000000000000, 0.000000000000000000, -1.000000000000000000 ) ) ;
#39966=CARTESIAN_POINT ( 'NONE',  ( 10.00000000000000000, -27.13269053701114331, 25.88420570971391754 ) ) ;
#39983=DIRECTION ( 'NONE',  ( -1.000000000000000000, 0.000000000000000000, -0.000000000000000000 ) ) ;
#39990=ORIENTED_EDGE ( 'NONE', *, *, #17977, .T. ) ;
#39992=AXIS2_PLACEMENT_3D ( 'NONE', #37349, #15080, #30010 ) ;
#39997=EDGE_CURVE ( 'NONE', #7892, #10144, #3675, .T. ) ;
#40016=LINE ( 'NONE', #25069, #5915 ) ;
#40027=VERTEX_POINT ( 'NONE', #34870 ) ;
#40030=CARTESIAN_POINT ( 'NONE',  ( 0.000000000000000000, 22.64427369931169309, 30.00120703465213623 ) ) ;
#40052=EDGE_CURVE ( 'NONE', #2104, #18905, #10438, .T. ) ;
#40065=VERTEX_POINT ( 'NONE', #31946 ) ;
#40078=EDGE_CURVE ( 'NONE', #46205, #45324, #13325, .T. ) ;
#40080=CARTESIAN_POINT ( 'NONE',  ( 10.00000000000000000, 21.53537804866081373, 30.80686688397018358 ) ) ;
#40081=VERTEX_POINT ( 'NONE', #24586 ) ;
#40100=AXIS2_PLACEMENT_3D ( 'NONE', #19756, #26162, #34697 ) ;
#40104=VERTEX_POINT ( 'NONE', #5267 ) ;
#40115=ORIENTED_EDGE ( 'NONE', *, *, #13963, .F. ) ;
#40130=FACE_OUTER_BOUND ( 'NONE', #22724, .T. ) ;
#40141=ADVANCED_FACE ( 'NONE', ( #33370 ), #48053, .T. ) ;
#40146=CIRCLE ( 'NONE', #26862, 42.00000000000000000 ) ;
#40149=PLANE ( 'NONE',  #12018 ) ;
#40150=FACE_OUTER_BOUND ( 'NONE', #47333, .T. ) ;
#40159=CARTESIAN_POINT ( 'NONE',  ( 10.00000000000000000, -6.736453364083817341, 36.88895765772630142 ) ) ;
#40167=AXIS2_PLACEMENT_3D ( 'NONE', #32981, #25634, #26133 ) ;
#40173=EDGE_CURVE ( 'NONE', #6771, #35343, #28399, .T. ) ;
#40175=VECTOR ( 'NONE', #25692, 1000.000000000000000 ) ;
#40192=CARTESIAN_POINT ( 'NONE',  ( -3.000000000000000000, 16.61724383029390140, -20.69703378468903665 ) ) ;
#40199=DIRECTION ( 'NONE',  ( 0.000000000000000000, 0.000000000000000000, 1.000000000000000000 ) ) ;
#40202=CARTESIAN_POINT ( 'NONE',  ( -3.000000000000000000, 16.83928648764945279, -16.46020748918028076 ) ) ;
#40210=AXIS2_PLACEMENT_3D ( 'NONE', #2036, #43846, #24531 ) ;
#40227=EDGE_LOOP ( 'NONE', ( #14403, #16777, #44983, #27027 ) ) ;
#40233=ORIENTED_EDGE ( 'NONE', *, *, #12711, .F. ) ;
#40235=VERTEX_POINT ( 'NONE', #10130 ) ;
#40236=AXIS2_PLACEMENT_3D ( 'NONE', #32084, #13468, #35503 ) ;
#40238=VECTOR ( 'NONE', #18243, 1000.000000000000000 ) ;
#40241=ORIENTED_EDGE ( 'NONE', *, *, #45523, .F. ) ;
#40246=DIRECTION ( 'NONE',  ( -1.000000000000000000, 0.000000000000000000, 0.000000000000000000 ) ) ;
#40254=DIRECTION ( 'NONE',  ( -1.000000000000000000, 0.000000000000000000, -0.000000000000000000 ) ) ;
#40260=DIRECTION ( 'NONE',  ( -1.000000000000000000, -0.000000000000000000, 0.000000000000000000 ) ) ;
#40268=DIRECTION ( 'NONE',  ( -1.000000000000000000, -0.000000000000000000, 0.000000000000000000 ) ) ;
#40275=CARTESIAN_POINT ( 'NONE',  ( 0.000000000000000000, -33.00180498840035170, -17.80606268964575278 ) ) ;
#40276=ORIENTED_EDGE ( 'NONE', *, *, #34875, .T. ) ;
#40280=DIRECTION ( 'NONE',  ( 0.000000000000000000, 0.9135454576426003115, 0.4067366430758017071 ) ) ;
#40281=CARTESIAN_POINT ( 'NONE',  ( 10.00000000000000000, -21.53537804866058991, -30.80686688397033635 ) ) ;
#40282=ADVANCED_FACE ( 'NONE', ( #28738 ), #29211, .F. ) ;
#40287=VERTEX_POINT ( 'NONE', #22103 ) ;
#40295=EDGE_LOOP ( 'NONE', ( #17153, #16997, #18656, #25771 ) ) ;
#40304=EDGE_CURVE ( 'NONE', #29847, #41768, #308, .T. ) ;
#40307=DIRECTION ( 'NONE',  ( 0.000000000000000000, 0.9135454576426063067, -0.4067366430757881068 ) ) ;
#40327=DIRECTION ( 'NONE',  ( -1.000000000000000000, -0.000000000000000000, -0.000000000000000000 ) ) ;
#40333=DIRECTION ( 'NONE',  ( -1.000000000000000000, 0.000000000000000000, -0.000000000000000000 ) ) ;
#40335=CARTESIAN_POINT ( 'NONE',  ( 0.000000000000000000, -35.92658777277517856, 10.74501242461269257 ) ) ;
#40356=AXIS2_PLACEMENT_3D ( 'NONE', #2906, #2194, #13929 ) ;
#40365=DIRECTION ( 'NONE',  ( 0.000000000000000000, -0.5877852522924624790, -0.8090169943749550008 ) ) ;
#40367=VERTEX_POINT ( 'NONE', #11584 ) ;
#40373=ORIENTED_EDGE ( 'NONE', *, *, #8183, .F. ) ;
#40380=DIRECTION ( 'NONE',  ( 0.000000000000000000, 0.000000000000000000, 1.000000000000000000 ) ) ;
#40385=DIRECTION ( 'NONE',  ( -1.000000000000000000, 0.000000000000000000, -0.000000000000000000 ) ) ;
#40386=FACE_OUTER_BOUND ( 'NONE', #1922, .T. ) ;
#40387=VERTEX_POINT ( 'NONE', #1029 ) ;
#40392=FACE_OUTER_BOUND ( 'NONE', #2907, .T. ) ;
#40393=DIRECTION ( 'NONE',  ( 0.000000000000000000, 0.000000000000000000, 1.000000000000000000 ) ) ;
#40410=EDGE_CURVE ( 'NONE', #42331, #45054, #15978, .T. ) ;
#40417=EDGE_CURVE ( 'NONE', #12661, #43656, #6564, .T. ) ;
#40418=CARTESIAN_POINT ( 'NONE',  ( 10.00000000000000000, 0.000000000000000000, 0.000000000000000000 ) ) ;
#40422=ORIENTED_EDGE ( 'NONE', *, *, #9196, .F. ) ;
#40429=CARTESIAN_POINT ( 'NONE',  ( 10.00000000000000000, 0.000000000000000000, 0.000000000000000000 ) ) ;
#40432=CARTESIAN_POINT ( 'NONE',  ( -10.00000000000000000, 0.000000000000000000, 0.000000000000000000 ) ) ;
#40441=CYLINDRICAL_SURFACE ( 'NONE', #30316, 37.49900000000000233 ) ;
#40446=ORIENTED_EDGE ( 'NONE', *, *, #3239, .F. ) ;
#40453=DIRECTION ( 'NONE',  ( 0.000000000000000000, 0.9510565162951544194, -0.3090169943749447867 ) ) ;
#40470=CARTESIAN_POINT ( 'NONE',  ( 10.00000000000000000, 33.80338159004283938, 16.23288003029508886 ) ) ;
#40472=ORIENTED_EDGE ( 'NONE', *, *, #33598, .T. ) ;
#40482=DIRECTION ( 'NONE',  ( 0.000000000000000000, 0.000000000000000000, 1.000000000000000000 ) ) ;
#40489=AXIS2_PLACEMENT_3D ( 'NONE', #21926, #18008, #21694 ) ;
#40492=DIRECTION ( 'NONE',  ( 0.000000000000000000, 0.000000000000000000, -1.000000000000000000 ) ) ;
#40496=ORIENTED_EDGE ( 'NONE', *, *, #23669, .T. ) ;
#40499=DIRECTION ( 'NONE',  ( -1.000000000000000000, -0.000000000000000000, -0.000000000000000000 ) ) ;
#40503=CARTESIAN_POINT ( 'NONE',  ( -3.000000000000000000, -11.95096189432312350, -23.69967320028773372 ) ) ;
#40508=LINE ( 'NONE', #21888, #22327 ) ;
#40513=CARTESIAN_POINT ( 'NONE',  ( -3.000000000000000000, 20.85821328998741109, 10.92862929874522315 ) ) ;
#40520=DIRECTION ( 'NONE',  ( 1.000000000000000000, 0.000000000000000000, -0.000000000000000000 ) ) ;
#40525=ORIENTED_EDGE ( 'NONE', *, *, #11460, .F. ) ;
#40532=CARTESIAN_POINT ( 'NONE',  ( 10.00000000000000000, 35.38097989696512968, 12.42422080174651100 ) ) ;
#40539=ORIENTED_EDGE ( 'NONE', *, *, #38249, .F. ) ;
#40545=ORIENTED_EDGE ( 'NONE', *, *, #37862, .F. ) ;
#40554=LINE ( 'NONE', #25128, #26848 ) ;
#40571=CARTESIAN_POINT ( 'NONE',  ( 10.00000000000000000, 4.992566952384984269, 37.16516213103279398 ) ) ;
#40573=DIRECTION ( 'NONE',  ( -1.000000000000000000, 0.000000000000000000, 0.000000000000000000 ) ) ;
#40574=ADVANCED_FACE ( 'NONE', ( #13980 ), #18119, .T. ) ;
#40575=FILL_AREA_STYLE ('',( #10726 ) ) ;
#40579=ORIENTED_EDGE ( 'NONE', *, *, #9558, .F. ) ;
#40584=AXIS2_PLACEMENT_3D ( 'NONE', #21866, #40260, #6716 ) ;
#40592=ORIENTED_EDGE ( 'NONE', *, *, #24195, .T. ) ;
#40595=LINE ( 'NONE', #25652, #7982 ) ;
#40610=VERTEX_POINT ( 'NONE', #43608 ) ;
#40613=CYLINDRICAL_SURFACE ( 'NONE', #15220, 16.00000000000000000 ) ;
#40623=ORIENTED_EDGE ( 'NONE', *, *, #5997, .T. ) ;
#40629=EDGE_CURVE ( 'NONE', #5281, #23433, #39120, .T. ) ;
#40642=ORIENTED_EDGE ( 'NONE', *, *, #1779, .F. ) ;
#40643=ORIENTED_EDGE ( 'NONE', *, *, #1035, .T. ) ;
#40649=ORIENTED_EDGE ( 'NONE', *, *, #16026, .F. ) ;
#40650=ORIENTED_EDGE ( 'NONE', *, *, #23415, .F. ) ;
#40656=EDGE_CURVE ( 'NONE', #19341, #22651, #2955, .T. ) ;
#40657=ORIENTED_EDGE ( 'NONE', *, *, #34922, .T. ) ;
#40663=CARTESIAN_POINT ( 'NONE',  ( 10.00000000000000000, -38.55633173627023069, 16.65560815589396526 ) ) ;
#40664=VERTEX_POINT ( 'NONE', #36008 ) ;
#40668=CARTESIAN_POINT ( 'NONE',  ( 5.000000000000000000, -26.79245525562690844, -32.34446384430000876 ) ) ;
#40671=CARTESIAN_POINT ( 'NONE',  ( 10.00000000000000000, 37.22597642581158084, -5.202137450156524068 ) ) ;
#40677=EDGE_CURVE ( 'NONE', #34210, #45280, #42261, .T. ) ;
#40682=EDGE_CURVE ( 'NONE', #31490, #24228, #39712, .T. ) ;
#40696=AXIS2_PLACEMENT_3D ( 'NONE', #24232, #35969, #17126 ) ;
#40707=EDGE_CURVE ( 'NONE', #9216, #43358, #14899, .T. ) ;
#40710=AXIS2_PLACEMENT_3D ( 'NONE', #8636, #31915, #35567 ) ;
#40714=LINE ( 'NONE', #2534, #34808 ) ;
#40715=ORIENTED_EDGE ( 'NONE', *, *, #22295, .T. ) ;
#40716=EDGE_CURVE ( 'NONE', #32005, #31590, #21138, .T. ) ;
#40722=CYLINDRICAL_SURFACE ( 'NONE', #2291, 16.00000000000000000 ) ;
#40724=ADVANCED_FACE ( 'NONE', ( #48237 ), #15668, .F. ) ;
#40735=CARTESIAN_POINT ( 'NONE',  ( 10.00000000000000000, -33.00180498840035170, -17.80606268964575278 ) ) ;
#40736=DIRECTION ( 'NONE',  ( 0.000000000000000000, 0.000000000000000000, 1.000000000000000000 ) ) ;
#40740=CARTESIAN_POINT ( 'NONE',  ( 10.00000000000000000, -35.53030884539077050, -12.26510123303296851 ) ) ;
#40742=DIRECTION ( 'NONE',  ( 0.000000000000000000, 0.9510565162951546414, -0.3090169943749442871 ) ) ;
#40743=CARTESIAN_POINT ( 'NONE',  ( 0.000000000000000000, 35.53030884539102630, -12.26510123303222599 ) ) ;
#40744=LINE ( 'NONE', #40513, #35451 ) ;
#40752=CARTESIAN_POINT ( 'NONE',  ( -3.000000000000000000, 20.85821328998756385, -10.92862929874494959 ) ) ;
#40753=VECTOR ( 'NONE', #23271, 1000.000000000000000 ) ;
#40759=ORIENTED_EDGE ( 'NONE', *, *, #42777, .F. ) ;
#40764=VECTOR ( 'NONE', #16401, 1000.000000000000000 ) ;
#40766=DIRECTION ( 'NONE',  ( 0.000000000000000000, 1.000000000000000000, 3.469446951953614189E-15 ) ) ;
#40769=CARTESIAN_POINT ( 'NONE',  ( -3.000000000000000000, 0.000000000000000000, 0.000000000000000000 ) ) ;
#40773=ORIENTED_EDGE ( 'NONE', *, *, #33706, .T. ) ;
#40774=FACE_OUTER_BOUND ( 'NONE', #20332, .T. ) ;
#40787=EDGE_CURVE ( 'NONE', #8228, #13990, #6315, .T. ) ;
#40789=DIRECTION ( 'NONE',  ( 0.000000000000000000, 0.9945218953682729568, 0.1045284632676578424 ) ) ;
#40791=DIRECTION ( 'NONE',  ( -1.000000000000000000, 0.000000000000000000, 0.000000000000000000 ) ) ;
#40792=CARTESIAN_POINT ( 'NONE',  ( 0.000000000000000000, -10.41901085202050581, -40.68715046381939970 ) ) ;
#40813=ORIENTED_EDGE ( 'NONE', *, *, #1069, .T. ) ;
#40815=( NAMED_UNIT ( * ) SI_UNIT ( $, .STERADIAN. ) SOLID_ANGLE_UNIT ( ) );
#40826=ORIENTED_EDGE ( 'NONE', *, *, #26364, .T. ) ;
#40850=DIRECTION ( 'NONE',  ( 0.000000000000000000, 0.000000000000000000, 1.000000000000000000 ) ) ;
#40851=AXIS2_PLACEMENT_3D ( 'NONE', #12277, #19577, #41638 ) ;
#40867=CARTESIAN_POINT ( 'NONE',  ( 10.00000000000000000, -2.663952781845854378, -41.91543099594820632 ) ) ;
#40871=DIRECTION ( 'NONE',  ( 0.000000000000000000, 0.000000000000000000, 1.000000000000000000 ) ) ;
#40873=CARTESIAN_POINT ( 'NONE',  ( 0.000000000000000000, 30.84782396557217865, 21.32104025579125306 ) ) ;
#40901=AXIS2_PLACEMENT_3D ( 'NONE', #33865, #340, #15291 ) ;
#40904=FACE_OUTER_BOUND ( 'NONE', #16085, .T. ) ;
#40912=DIRECTION ( 'NONE',  ( -1.000000000000000000, 0.000000000000000000, -0.000000000000000000 ) ) ;
#40914=EDGE_CURVE ( 'NONE', #28215, #22790, #19552, .T. ) ;
#40922=CARTESIAN_POINT ( 'NONE',  ( -3.000000000000000000, -4.261787119644969479, -26.19803753235780519 ) ) ;
#40933=CARTESIAN_POINT ( 'NONE',  ( 0.000000000000000000, 0.000000000000000000, 0.000000000000000000 ) ) ;
#40935=DIRECTION ( 'NONE',  ( 0.000000000000000000, 0.000000000000000000, 1.000000000000000000 ) ) ;
#40938=AXIS2_PLACEMENT_3D ( 'NONE', #42386, #46793, #17150 ) ;
#40945=DIRECTION ( 'NONE',  ( -1.000000000000000000, 0.000000000000000000, 0.000000000000000000 ) ) ;
#40947=ORIENTED_EDGE ( 'NONE', *, *, #11751, .F. ) ;
#40959=EDGE_CURVE ( 'NONE', #10988, #27800, #42344, .T. ) ;
#40965=DIRECTION ( 'NONE',  ( -0.000000000000000000, 0.7431448254773946882, -0.6691306063588577935 ) ) ;
#40984=ORIENTED_EDGE ( 'NONE', *, *, #19012, .F. ) ;
#40995=CARTESIAN_POINT ( 'NONE',  ( -3.000000000000000000, -10.45096189432314837, -21.10159698893440350 ) ) ;
#40996=CYLINDRICAL_SURFACE ( 'NONE', #26181, 16.00000000000000000 ) ;
#40997=ORIENTED_EDGE ( 'NONE', *, *, #36734, .F. ) ;
#41000=CARTESIAN_POINT ( 'NONE',  ( 10.00000000000000000, 37.16516213103285082, -4.992566952384588141 ) ) ;
#41005=CARTESIAN_POINT ( 'NONE',  ( 10.00000000000000000, -4.992566952385247170, 37.16516213103275845 ) ) ;
#41008=CIRCLE ( 'NONE', #35547, 16.00000000000000000 ) ;
#41010=VECTOR ( 'NONE', #27772, 1000.000000000000114 ) ;
#41033=VERTEX_POINT ( 'NONE', #6828 ) ;
#41045=CYLINDRICAL_SURFACE ( 'NONE', #17724, 37.49900000000000233 ) ;
#41061=CIRCLE ( 'NONE', #7430, 16.00000000000000000 ) ;
#41065=CIRCLE ( 'NONE', #21512, 37.49900000000000233 ) ;
#41067=ORIENTED_EDGE ( 'NONE', *, *, #40410, .F. ) ;
#41074=FACE_OUTER_BOUND ( 'NONE', #32333, .T. ) ;
#41095=AXIS2_PLACEMENT_3D ( 'NONE', #12736, #35239, #16889 ) ;
#41098=VECTOR ( 'NONE', #47319, 1000.000000000000000 ) ;
#41100=DIRECTION ( 'NONE',  ( -1.000000000000000000, -0.000000000000000000, -0.000000000000000000 ) ) ;
#41101=VERTEX_POINT ( 'NONE', #47923 ) ;
#41106=AXIS2_PLACEMENT_3D ( 'NONE', #23559, #30933, #35303 ) ;
#41111=ORIENTED_EDGE ( 'NONE', *, *, #18687, .T. ) ;
#41113=CYLINDRICAL_SURFACE ( 'NONE', #29127, 37.49900000000000233 ) ;
#41118=CARTESIAN_POINT ( 'NONE',  ( 0.000000000000000000, 35.38097989696528600, -12.42422080174602605 ) ) ;
#41125=CARTESIAN_POINT ( 'NONE',  ( -10.00000000000000000, 0.000000000000000000, 0.000000000000000000 ) ) ;
#41127=EDGE_CURVE ( 'NONE', #5676, #20033, #5542, .T. ) ;
#41129=DIRECTION ( 'NONE',  ( -1.000000000000000000, 0.000000000000000000, 0.000000000000000000 ) ) ;
#41137=VECTOR ( 'NONE', #21836, 999.9999999999998863 ) ;
#41141=CARTESIAN_POINT ( 'NONE',  ( -3.000000000000000000, -23.29833615347109443, 3.418703333116492438 ) ) ;
#41145=ORIENTED_EDGE ( 'NONE', *, *, #37012, .F. ) ;
#41148=VERTEX_POINT ( 'NONE', #17341 ) ;
#41149=ORIENTED_EDGE ( 'NONE', *, *, #45164, .F. ) ;
#41150=LINE ( 'NONE', #7605, #20635 ) ;
#41177=EDGE_CURVE ( 'NONE', #44922, #47549, #7874, .T. ) ;
#41182=ADVANCED_FACE ( 'NONE', ( #14893 ), #48412, .F. ) ;
#41193=LINE ( 'NONE', #25993, #14699 ) ;
#41204=CIRCLE ( 'NONE', #16219, 42.00000000000000000 ) ;
#41207=LINE ( 'NONE', #10852, #36321 ) ;
#41222=ORIENTED_EDGE ( 'NONE', *, *, #10364, .T. ) ;
#41223=LINE ( 'NONE', #4968, #19327 ) ;
#41224=ORIENTED_EDGE ( 'NONE', *, *, #9196, .T. ) ;
#41226=DIRECTION ( 'NONE',  ( -1.000000000000000000, 0.000000000000000000, -0.000000000000000000 ) ) ;
#41244=LINE ( 'NONE', #7211, #3389 ) ;
#41254=ORIENTED_EDGE ( 'NONE', *, *, #6264, .F. ) ;
#41255=EDGE_CURVE ( 'NONE', #37523, #14949, #7296, .T. ) ;
#41262=ORIENTED_EDGE ( 'NONE', *, *, #16403, .T. ) ;
#41268=DIRECTION ( 'NONE',  ( 1.000000000000000000, 0.000000000000000000, 0.000000000000000000 ) ) ;
#41270=ORIENTED_EDGE ( 'NONE', *, *, #40677, .T. ) ;
#41284=CARTESIAN_POINT ( 'NONE',  ( 0.000000000000000000, 0.000000000000000000, 0.000000000000000000 ) ) ;
#41293=ORIENTED_EDGE ( 'NONE', *, *, #21484, .T. ) ;
#41296=VERTEX_POINT ( 'NONE', #21981 ) ;
#41297=EDGE_CURVE ( 'NONE', #38237, #14425, #44628, .T. ) ;
#41298=FACE_OUTER_BOUND ( 'NONE', #1250, .T. ) ;
#41322=FACE_OUTER_BOUND ( 'NONE', #47940, .T. ) ;
#41323=AXIS2_PLACEMENT_3D ( 'NONE', #18300, #14401, #25399 ) ;
#41335=ORIENTED_EDGE ( 'NONE', *, *, #36284, .F. ) ;
#41340=DIRECTION ( 'NONE',  ( -0.000000000000000000, 0.8090169943749426773, 0.5877852522924797984 ) ) ;
#41346=CARTESIAN_POINT ( 'NONE',  ( 10.00000000000000000, -25.88420570971381807, -27.13269053701123212 ) ) ;
#41347=DIRECTION ( 'NONE',  ( -1.000000000000000000, -0.000000000000000000, 0.000000000000000000 ) ) ;
#41348=EDGE_LOOP ( 'NONE', ( #25119, #42979, #35420, #7955 ) ) ;
#41350=EDGE_CURVE ( 'NONE', #44417, #39726, #42053, .T. ) ;
#41352=VERTEX_POINT ( 'NONE', #16117 ) ;
#41363=ORIENTED_EDGE ( 'NONE', *, *, #47943, .F. ) ;
#41375=DIRECTION ( 'NONE',  ( -1.000000000000000000, 0.000000000000000000, 0.000000000000000000 ) ) ;
#41376=EDGE_LOOP ( 'NONE', ( #20005, #27529, #23636, #13725 ) ) ;
#41378=EDGE_LOOP ( 'NONE', ( #33202, #19735, #32414, #20343 ) ) ;
#41392=ADVANCED_FACE ( 'NONE', ( #4842 ), #20483, .T. ) ;
#41397=ORIENTED_EDGE ( 'NONE', *, *, #1455, .T. ) ;
#41407=DIRECTION ( 'NONE',  ( -1.000000000000000000, -0.000000000000000000, 0.000000000000000000 ) ) ;
#41414=CARTESIAN_POINT ( 'NONE',  ( 0.000000000000000000, 17.80606268964585226, -33.00180498840028775 ) ) ;
#41415=CARTESIAN_POINT ( 'NONE',  ( 0.000000000000000000, -30.00120703465222149, 22.64427369931158296 ) ) ;
#41421=CARTESIAN_POINT ( 'NONE',  ( -3.000000000000000000, 5.835314593368772229, -22.81335362449846826 ) ) ;
#41422=VERTEX_POINT ( 'NONE', #45967 ) ;
#41433=AXIS2_PLACEMENT_3D ( 'NONE', #6305, #21217, #2607 ) ;
#41436=ORIENTED_EDGE ( 'NONE', *, *, #36737, .F. ) ;
#41441=DIRECTION ( 'NONE',  ( -1.000000000000000000, -0.000000000000000000, -0.000000000000000000 ) ) ;
#41444=EDGE_CURVE ( 'NONE', #8400, #390, #47757, .T. ) ;
#41456=ADVANCED_FACE ( 'NONE', ( #17537 ), #13154, .F. ) ;
#41459=AXIS2_PLACEMENT_3D ( 'NONE', #11529, #26454, #30374 ) ;
#41461=EDGE_CURVE ( 'NONE', #5896, #12471, #36831, .T. ) ;
#41488=EDGE_CURVE ( 'NONE', #16291, #38706, #11058, .T. ) ;
#41490=AXIS2_PLACEMENT_3D ( 'NONE', #8019, #30540, #7052 ) ;
#41495=CIRCLE ( 'NONE', #845, 42.00000000000000000 ) ;
#41497=DIRECTION ( 'NONE',  ( 0.000000000000000000, 0.9135454576426005335, 0.4067366430758010409 ) ) ;
#41509=DIRECTION ( 'NONE',  ( 0.000000000000000000, 0.000000000000000000, 1.000000000000000000 ) ) ;
#41514=EDGE_LOOP ( 'NONE', ( #4131, #17323, #43180, #35309 ) ) ;
#41517=PLANE ( 'NONE',  #7438 ) ;
#41521=CARTESIAN_POINT ( 'NONE',  ( 4.999999999999999112, -40.68715046381921496, -10.41901085202121280 ) ) ;
#41522=LINE ( 'NONE', #4076, #27621 ) ;
#41523=DIRECTION ( 'NONE',  ( -1.000000000000000000, 0.000000000000000000, -0.000000000000000000 ) ) ;
#41527=ORIENTED_EDGE ( 'NONE', *, *, #19379, .F. ) ;
#41559=VERTEX_POINT ( 'NONE', #13881 ) ;
#41562=VECTOR ( 'NONE', #41712, 1000.000000000000000 ) ;
#41567=DIRECTION ( 'NONE',  ( 0.000000000000000000, 0.1564344650402244852, 0.9876883405951387696 ) ) ;
#41576=VECTOR ( 'NONE', #34264, 1000.000000000000000 ) ;
#41577=DIRECTION ( 'NONE',  ( -0.000000000000000000, 0.5000000000000031086, -0.8660254037844369313 ) ) ;
#41587=DIRECTION ( 'NONE',  ( -1.000000000000000000, -0.000000000000000000, -0.000000000000000000 ) ) ;
#41592=DIRECTION ( 'NONE',  ( -1.000000000000000000, 0.000000000000000000, 0.000000000000000000 ) ) ;
#41601=AXIS2_PLACEMENT_3D ( 'NONE', #32901, #43928, #3044 ) ;
#41604=ADVANCED_FACE ( 'NONE', ( #33198 ), #48125, .T. ) ;
#41605=DIRECTION ( 'NONE',  ( 0.000000000000000000, -0.5877852522924803536, 0.8090169943749422332 ) ) ;
#41606=DIRECTION ( 'NONE',  ( 0.000000000000000000, 0.7071067811865437980, 0.7071067811865512365 ) ) ;
#41613=DIRECTION ( 'NONE',  ( -1.000000000000000000, -0.000000000000000000, -0.000000000000000000 ) ) ;
#41618=AXIS2_PLACEMENT_3D ( 'NONE', #29161, #14973, #44346 ) ;
#41628=CARTESIAN_POINT ( 'NONE',  ( 10.00000000000000000, 12.26510123303308752, -35.53030884539072787 ) ) ;
#41637=ORIENTED_EDGE ( 'NONE', *, *, #24195, .F. ) ;
#41638=DIRECTION ( 'NONE',  ( 0.000000000000000000, 0.3090169943749411230, 0.9510565162951555296 ) ) ;
#41641=CIRCLE ( 'NONE', #25977, 42.00000000000000000 ) ;
#41649=DIRECTION ( 'NONE',  ( 1.000000000000000000, 0.000000000000000000, -0.000000000000000000 ) ) ;
#41650=DIRECTION ( 'NONE',  ( -1.000000000000000000, -0.000000000000000000, 0.000000000000000000 ) ) ;
#41651=CARTESIAN_POINT ( 'NONE',  ( 0.000000000000000000, 40.68715046381943523, -10.41901085202036370 ) ) ;
#41652=VECTOR ( 'NONE', #9306, 1000.000000000000114 ) ;
#41653=ORIENTED_EDGE ( 'NONE', *, *, #41127, .T. ) ;
#41657=LINE ( 'NONE', #1275, #9262 ) ;
#41659=ORIENTED_EDGE ( 'NONE', *, *, #35882, .T. ) ;
#41662=DIRECTION ( 'NONE',  ( -1.000000000000000000, 0.000000000000000000, 0.000000000000000000 ) ) ;
#41668=AXIS2_PLACEMENT_3D ( 'NONE', #45735, #41577, #30081 ) ;
#41672=ORIENTED_EDGE ( 'NONE', *, *, #1505, .T. ) ;
#41681=CARTESIAN_POINT ( 'NONE',  ( 0.000000000000000000, -22.32062822937489344, 14.36278369418800160 ) ) ;
#41686=CARTESIAN_POINT ( 'NONE',  ( 0.000000000000000000, 25.88420570971400991, 27.13269053701105449 ) ) ;
#41704=CARTESIAN_POINT ( 'NONE',  ( 0.000000000000000000, 2.663952781846149254, 41.91543099594818500 ) ) ;
#41708=EDGE_CURVE ( 'NONE', #25783, #31111, #35552, .T. ) ;
#41712=DIRECTION ( 'NONE',  ( -1.000000000000000000, 0.000000000000000000, -0.000000000000000000 ) ) ;
#41714=VECTOR ( 'NONE', #46534, 1000.000000000000000 ) ;
#41716=DIRECTION ( 'NONE',  ( -1.000000000000000000, -0.000000000000000000, -0.000000000000000000 ) ) ;
#41725=EDGE_CURVE ( 'NONE', #28319, #41768, #27521, .T. ) ;
#41727=VERTEX_POINT ( 'NONE', #1303 ) ;
#41754=ORIENTED_EDGE ( 'NONE', *, *, #43988, .F. ) ;
#41759=DIRECTION ( 'NONE',  ( -0.000000000000000000, 0.1045284632676570929, -0.9945218953682730678 ) ) ;
#41760=DIRECTION ( 'NONE',  ( -1.000000000000000000, 0.000000000000000000, 0.000000000000000000 ) ) ;
#41761=LINE ( 'NONE', #27080, #33097 ) ;
#41768=VERTEX_POINT ( 'NONE', #38754 ) ;
#41779=VECTOR ( 'NONE', #12797, 1000.000000000000000 ) ;
#41790=AXIS2_PLACEMENT_3D ( 'NONE', #24907, #39623, #20996 ) ;
#41794=LINE ( 'NONE', #12415, #4880 ) ;
#41801=ORIENTED_EDGE ( 'NONE', *, *, #24692, .T. ) ;
#41802=VERTEX_POINT ( 'NONE', #32818 ) ;
#41810=VERTEX_POINT ( 'NONE', #14481 ) ;
#41811=ORIENTED_EDGE ( 'NONE', *, *, #13970, .F. ) ;
#41820=CIRCLE ( 'NONE', #8197, 16.00000000000000000 ) ;
#41825=AXIS2_PLACEMENT_3D ( 'NONE', #35628, #25078, #28763 ) ;
#41839=AXIS2_PLACEMENT_3D ( 'NONE', #34470, #42817, #8306 ) ;
#41854=ADVANCED_FACE ( 'NONE', ( #36732 ), #14230, .T. ) ;
#41858=AXIS2_PLACEMENT_3D ( 'NONE', #32880, #13823, #47805 ) ;
#41860=CARTESIAN_POINT ( 'NONE',  ( -3.000000000000000000, 9.615535125378775305, 24.73947219025917121 ) ) ;
#41867=EDGE_CURVE ( 'NONE', #45054, #5880, #8733, .T. ) ;
#41877=ORIENTED_EDGE ( 'NONE', *, *, #42715, .F. ) ;
#41882=CARTESIAN_POINT ( 'NONE',  ( 10.00000000000000000, 0.000000000000000000, 0.000000000000000000 ) ) ;
#41889=AXIS2_PLACEMENT_3D ( 'NONE', #29090, #9290, #24222 ) ;
#41890=VERTEX_POINT ( 'NONE', #29411 ) ;
#41896=ORIENTED_EDGE ( 'NONE', *, *, #26376, .F. ) ;
#41899=AXIS2_PLACEMENT_3D ( 'NONE', #10156, #21410, #6490 ) ;
#41901=LINE ( 'NONE', #42622, #15163 ) ;
#41904=ADVANCED_FACE ( 'NONE', ( #3197 ), #29639, .T. ) ;
#41906=DIRECTION ( 'NONE',  ( -1.000000000000000000, -0.000000000000000000, 0.000000000000000000 ) ) ;
#41907=ORIENTED_EDGE ( 'NONE', *, *, #42437, .T. ) ;
#41923=CARTESIAN_POINT ( 'NONE',  ( 5.000000000000000000, 2.663952781846149254, 41.91543099594818500 ) ) ;
#41953=CARTESIAN_POINT ( 'NONE',  ( 10.00000000000000000, 6.555932627142418312, 37.01155633439060466 ) ) ;
#41954=VERTEX_POINT ( 'NONE', #23269 ) ;
#41955=EDGE_CURVE ( 'NONE', #41296, #37915, #37473, .T. ) ;
#41959=EDGE_LOOP ( 'NONE', ( #35248, #8331, #23790, #1774, #21702, #12376, #742, #1466, #36539, #35218, #13276, #8574, #465, #7492, #39467, #41254, #24111, #32955, #14110, #8550, #35344, #39520, #19354, #23282, #24880, #45843, #34302, #8163, #23184, #6956, #30657, #35551, #16887, #38620, #681, #8160, #35176, #36655, #28355, #28572, #46333, #23613, #43631, #18889, #38533, #4389, #26173, #17772, #21968, #12902, #18194, #37503, #17315, #34241, #26857, #21474, #3594, #9012, #40241, #1865, #13002, #8741, #10972, #6331, #26625, #35075, #43480, #40579, #5438, #21883, #30996, #46821, #9282, #30489, #14470, #19777, #16814, #14718, #40446, #22852, #44579, #32205, #17813, #9250, #26863, #16111, #33073, #5797, #30057, #5874, #22647, #36557, #31259, #11812, #47348, #19331, #21850, #48427, #22244, #25947, #17042, #16825, #23047, #8038, #32810, #28372, #18917, #38686, #32805, #3685, #12241, #43335, #25972, #34873, #48176, #47086, #21815, #18487, #23494, #885, #3229, #31526, #44285, #47196, #6435, #41363, #13007, #37212, #45629, #29581, #46583, #9712, #36717, #28867, #38171, #4378, #10170, #1426, #29473, #43621, #13316, #8628, #18600, #39593, #20086, #32030, #29017, #38136, #25188, #39144, #16820, #3317, #11648, #7712, #8919, #30719, #35550, #45509, #45407, #4883, #18800, #2856, #6505, #25036, #21527 ) ) ;
#41961=FACE_OUTER_BOUND ( 'NONE', #5551, .T. ) ;
#41970=DIRECTION ( 'NONE',  ( 0.000000000000000000, -0.9510565162951565288, 0.3090169943749384029 ) ) ;
#41972=FACE_OUTER_BOUND ( 'NONE', #22470, .T. ) ;
#41974=ORIENTED_EDGE ( 'NONE', *, *, #24553, .T. ) ;
#41975=ORIENTED_EDGE ( 'NONE', *, *, #38597, .T. ) ;
#41981=LINE ( 'NONE', #26556, #12750 ) ;
#41983=VECTOR ( 'NONE', #32269, 1000.000000000000000 ) ;
#41987=CARTESIAN_POINT ( 'NONE',  ( 0.000000000000000000, 33.17418723428333749, -17.67226234102790272 ) ) ;
#41993=VERTEX_POINT ( 'NONE', #22544 ) ;
#41995=CARTESIAN_POINT ( 'NONE',  ( 10.00000000000000000, 33.79645857604513992, 16.45098606841138178 ) ) ;
#42002=VERTEX_POINT ( 'NONE', #7848 ) ;
#42008=DIRECTION ( 'NONE',  ( -1.000000000000000000, 0.000000000000000000, -0.000000000000000000 ) ) ;
#42011=EDGE_CURVE ( 'NONE', #22253, #23219, #30141, .T. ) ;
#42014=ORIENTED_EDGE ( 'NONE', *, *, #10678, .F. ) ;
#42021=DIRECTION ( 'NONE',  ( 0.000000000000000000, 0.000000000000000000, 1.000000000000000000 ) ) ;
#42025=CARTESIAN_POINT ( 'NONE',  ( -3.000000000000000000, -0.9646360437375307573, 23.52805723605590060 ) ) ;
#42027=LINE ( 'NONE', #7987, #45082 ) ;
#42033=EDGE_CURVE ( 'NONE', #32185, #23315, #739, .T. ) ;
#42044=LINE ( 'NONE', #30789, #46844 ) ;
#42045=DIRECTION ( 'NONE',  ( -1.000000000000000000, 0.000000000000000000, 0.000000000000000000 ) ) ;
#42053=LINE ( 'NONE', #31050, #27488 ) ;
#42054=ORIENTED_EDGE ( 'NONE', *, *, #46555, .T. ) ;
#42059=CYLINDRICAL_SURFACE ( 'NONE', #8474, 16.00000000000000000 ) ;
#42067=EDGE_CURVE ( 'NONE', #40235, #31834, #29106, .T. ) ;
#42069=DIRECTION ( 'NONE',  ( -1.000000000000000000, -0.000000000000000000, 0.000000000000000000 ) ) ;
#42071=ORIENTED_EDGE ( 'NONE', *, *, #37539, .F. ) ;
#42078=CARTESIAN_POINT ( 'NONE',  ( 10.00000000000000000, 40.68715046381944234, -10.41901085202036192 ) ) ;
#42080=CARTESIAN_POINT ( 'NONE',  ( 0.000000000000000000, 16.23288003029497162, 33.80338159004289622 ) ) ;
#42088=CARTESIAN_POINT ( 'NONE',  ( -3.000000000000000000, 22.07842321921492612, -8.187992925817130896 ) ) ;
#42096=DIRECTION ( 'NONE',  ( 1.000000000000000000, 0.000000000000000000, 0.000000000000000000 ) ) ;
#42102=ORIENTED_EDGE ( 'NONE', *, *, #37311, .T. ) ;
#42106=ORIENTED_EDGE ( 'NONE', *, *, #16026, .T. ) ;
#42114=ADVANCED_FACE ( 'NONE', ( #5633 ), #16405, .T. ) ;
#42129=DIRECTION ( 'NONE',  ( 0.000000000000000000, 0.4067366430758000417, -0.9135454576426009776 ) ) ;
#42131=AXIS2_PLACEMENT_3D ( 'NONE', #25855, #36154, #18273 ) ;
#42133=DIRECTION ( 'NONE',  ( -1.000000000000000000, 0.000000000000000000, -0.000000000000000000 ) ) ;
#42143=ORIENTED_EDGE ( 'NONE', *, *, #5024, .F. ) ;
#42148=ORIENTED_EDGE ( 'NONE', *, *, #34429, .T. ) ;
#42152=LINE ( 'NONE', #34079, #9735 ) ;
#42156=EDGE_CURVE ( 'NONE', #13285, #36037, #28308, .T. ) ;
#42160=ORIENTED_EDGE ( 'NONE', *, *, #30753, .T. ) ;
#42163=VERTEX_POINT ( 'NONE', #4899 ) ;
#42166=DIRECTION ( 'NONE',  ( -1.000000000000000000, 0.000000000000000000, 0.000000000000000000 ) ) ;
#42176=CARTESIAN_POINT ( 'NONE',  ( 0.000000000000000000, 16.83928648764923253, 16.46020748918050458 ) ) ;
#42197=ORIENTED_EDGE ( 'NONE', *, *, #33598, .F. ) ;
#42201=ORIENTED_EDGE ( 'NONE', *, *, #36084, .F. ) ;
#42204=EDGE_CURVE ( 'NONE', #38800, #5676, #8774, .T. ) ;
#42213=EDGE_CURVE ( 'NONE', #10349, #37347, #35365, .T. ) ;
#42214=CARTESIAN_POINT ( 'NONE',  ( 10.00000000000000000, 27.75498641678786527, -31.52238457039571173 ) ) ;
#42239=CARTESIAN_POINT ( 'NONE',  ( -3.000000000000000000, -20.55727247249748046, 16.78983467731285018 ) ) ;
#42241=DIRECTION ( 'NONE',  ( -1.000000000000000000, -0.000000000000000000, 0.000000000000000000 ) ) ;
#42252=DIRECTION ( 'NONE',  ( -0.000000000000000000, -0.4067366430757898277, -0.9135454576426055295 ) ) ;
#42254=AXIS2_PLACEMENT_3D ( 'NONE', #26336, #41268, #7723 ) ;
#42261=CIRCLE ( 'NONE', #44601, 42.00000000000000000 ) ;
#42269=AXIS2_PLACEMENT_3D ( 'NONE', #46466, #27376, #23692 ) ;
#42272=DIRECTION ( 'NONE',  ( -1.000000000000000000, 0.000000000000000000, 0.000000000000000000 ) ) ;
#42274=ORIENTED_EDGE ( 'NONE', *, *, #14746, .T. ) ;
#42281=CARTESIAN_POINT ( 'NONE',  ( 10.00000000000000000, -35.53030884539077050, -12.26510123303296851 ) ) ;
#42283=ORIENTED_EDGE ( 'NONE', *, *, #2874, .F. ) ;
#42285=DIRECTION ( 'NONE',  ( 0.000000000000000000, 0.000000000000000000, 1.000000000000000000 ) ) ;
#42287=AXIS2_PLACEMENT_3D ( 'NONE', #7781, #184, #41567 ) ;
#42292=DIRECTION ( 'NONE',  ( 1.000000000000000000, 0.000000000000000000, -0.000000000000000000 ) ) ;
#42293=AXIS2_PLACEMENT_3D ( 'NONE', #9297, #39416, #46992 ) ;
#42295=CARTESIAN_POINT ( 'NONE',  ( -3.000000000000000000, -3.948201729842038432, -23.21447184625298021 ) ) ;
#42297=CARTESIAN_POINT ( 'NONE',  ( 0.000000000000000000, -33.80338159004273280, -16.23288003029533044 ) ) ;
#42309=ORIENTED_EDGE ( 'NONE', *, *, #13825, .F. ) ;
#42312=CARTESIAN_POINT ( 'NONE',  ( -3.000000000000000000, -18.13022148937243472, -15.02647892043568767 ) ) ;
#42318=ORIENTED_EDGE ( 'NONE', *, *, #35146, .T. ) ;
#42319=DIRECTION ( 'NONE',  ( -1.000000000000000000, 0.000000000000000000, 0.000000000000000000 ) ) ;
#42331=VERTEX_POINT ( 'NONE', #21031 ) ;
#42342=EDGE_CURVE ( 'NONE', #29523, #13751, #12734, .T. ) ;
#42344=LINE ( 'NONE', #28135, #10240 ) ;
#42352=DIRECTION ( 'NONE',  ( -1.000000000000000000, -0.000000000000000000, 0.000000000000000000 ) ) ;
#42369=DIRECTION ( 'NONE',  ( 0.000000000000000000, 0.9510565162951544194, -0.3090169943749446757 ) ) ;
#42378=AXIS2_PLACEMENT_3D ( 'NONE', #687, #44747, #30805 ) ;
#42382=DIRECTION ( 'NONE',  ( 0.000000000000000000, -0.8090169943749531134, 0.5877852522924653655 ) ) ;
#42386=CARTESIAN_POINT ( 'NONE',  ( 0.000000000000000000, 21.53537804866081373, 30.80686688397018358 ) ) ;
#42391=LINE ( 'NONE', #10291, #25306 ) ;
#42414=CARTESIAN_POINT ( 'NONE',  ( 0.000000000000000000, -6.555932627142143865, -37.01155633439065440 ) ) ;
#42424=VERTEX_POINT ( 'NONE', #44511 ) ;
#42430=DIRECTION ( 'NONE',  ( -1.000000000000000000, -0.000000000000000000, -0.000000000000000000 ) ) ;
#42434=DIRECTION ( 'NONE',  ( 0.000000000000000000, -0.3090169943749548342, 0.9510565162951511997 ) ) ;
#42435=CARTESIAN_POINT ( 'NONE',  ( -3.000000000000000000, -13.04903810567647682, -19.60159698893442481 ) ) ;
#42437=EDGE_CURVE ( 'NONE', #30863, #7503, #196, .T. ) ;
#42438=VECTOR ( 'NONE', #27371, 1000.000000000000000 ) ;
#42439=CARTESIAN_POINT ( 'NONE',  ( 0.000000000000000000, -25.60904388321916514, -6.976881207771517879 ) ) ;
#42447=LINE ( 'NONE', #5728, #11151 ) ;
#42456=ORIENTED_EDGE ( 'NONE', *, *, #15758, .T. ) ;
#42464=EDGE_LOOP ( 'NONE', ( #15997, #11892, #38474, #7979 ) ) ;
#42473=VECTOR ( 'NONE', #12114, 1000.000000000000000 ) ;
#42477=ORIENTED_EDGE ( 'NONE', *, *, #48043, .F. ) ;
#42478=DIRECTION ( 'NONE',  ( 0.000000000000000000, 0.000000000000000000, 1.000000000000000000 ) ) ;
#42486=DIRECTION ( 'NONE',  ( -0.000000000000000000, 0.9781476007338069101, -0.2079116908177532363 ) ) ;
#42489=CARTESIAN_POINT ( 'NONE',  ( 10.00000000000000000, -0.6853352020793173072, 37.58145647212453611 ) ) ;
#42490=DIRECTION ( 'NONE',  ( 0.000000000000000000, -0.7431448254773954654, 0.6691306063588569053 ) ) ;
#42494=EDGE_CURVE ( 'NONE', #24283, #42613, #35399, .T. ) ;
#42495=DIRECTION ( 'NONE',  ( 1.000000000000000000, -0.000000000000000000, -0.000000000000000000 ) ) ;
#42501=CIRCLE ( 'NONE', #33088, 42.00000000000000000 ) ;
#42510=ORIENTED_EDGE ( 'NONE', *, *, #4372, .T. ) ;
#42520=AXIS2_PLACEMENT_3D ( 'NONE', #11519, #41375, #41606 ) ;
#42524=VERTEX_POINT ( 'NONE', #39349 ) ;
#42535=CIRCLE ( 'NONE', #26111, 16.00000000000000355 ) ;
#42539=CARTESIAN_POINT ( 'NONE',  ( 0.000000000000000000, -33.17418723428319538, 17.67226234102814431 ) ) ;
#42541=VERTEX_POINT ( 'NONE', #31060 ) ;
#42542=DIRECTION ( 'NONE',  ( -1.000000000000000000, -0.000000000000000000, -0.000000000000000000 ) ) ;
#42548=CARTESIAN_POINT ( 'NONE',  ( 10.00000000000000000, -26.08949754953005495, -27.05870788708258701 ) ) ;
#42557=VECTOR ( 'NONE', #23227, 1000.000000000000000 ) ;
#42560=ORIENTED_EDGE ( 'NONE', *, *, #29612, .T. ) ;
#42567=AXIS2_PLACEMENT_3D ( 'NONE', #3837, #7976, #38098 ) ;
#42569=LINE ( 'NONE', #46481, #11850 ) ;
#42612=CARTESIAN_POINT ( 'NONE',  ( -3.000000000000000000, 0.000000000000000000, 0.000000000000000000 ) ) ;
#42613=VERTEX_POINT ( 'NONE', #21469 ) ;
#42622=CARTESIAN_POINT ( 'NONE',  ( 10.00000000000000000, 35.92658777277511462, 10.74501242461295014 ) ) ;
#42625=CARTESIAN_POINT ( 'NONE',  ( 10.00000000000000000, 33.80338159004307386, -16.23288003029461279 ) ) ;
#42632=ADVANCED_FACE ( 'NONE', ( #28581 ), #47417, .T. ) ;
#42634=EDGE_CURVE ( 'NONE', #29332, #42541, #19729, .T. ) ;
#42642=DIRECTION ( 'NONE',  ( -1.000000000000000000, 0.000000000000000000, 0.000000000000000000 ) ) ;
#42652=ADVANCED_FACE ( 'NONE', ( #47883 ), #6074, .T. ) ;
#42683=EDGE_CURVE ( 'NONE', #34175, #6187, #40554, .T. ) ;
#42690=DIRECTION ( 'NONE',  ( 0.000000000000000000, 1.000000000000000000, 7.228014483236689653E-16 ) ) ;
#42691=DIRECTION ( 'NONE',  ( -1.000000000000000000, 0.000000000000000000, 0.000000000000000000 ) ) ;
#42693=CIRCLE ( 'NONE', #15332, 37.49900000000000233 ) ;
#42702=CLOSED_SHELL ( 'NONE', ( #41456, #26479, #15976, #32741, #26511, #7172, #32348, #6321, #24359, #45093, #47888, #29510, #36208, #9393, #20408, #27687, #17013, #5928, #33118, #15262, #45363, #16867, #44197, #43159, #38643, #23368, #26302, #42632, #13380, #24429, #21861, #48224, #19817, #36303, #7332, #24865, #17573, #44885, #41854, #5919, #46127, #37143, #15816, #36797, #27828, #22494, #27278, #16322, #45047, #27778, #25694, #8131, #34608, #46597, #32272, #31880, #41904, #26324, #42652, #28696, #43705, #20781, #21724, #19124, #9132, #1899, #2279, #38532, #11137, #8545, #7993, #13202, #36642, #18110, #30243, #16100, #23310, #30436, #4329, #27297, #30736, #41392, #32479, #38020, #34014, #7812, #25133, #32113, #5485, #1522, #36310, #10196, #7940, #10002, #21454, #19279, #3744, #7466, #25736, #9560, #48406, #8850, #30237, #7111, #26624, #45423, #48058, #27405, #11517, #34362, #10057, #35761, #2416, #28634, #6274, #11463, #41604, #3420, #36724, #29383, #30329, #24167, #24914, #31818, #46981, #17268, #22598, #13873, #42114, #10453, #3253, #32170, #15641, #18178, #13241, #38516, #30666, #20990, #31854, #29825, #43172, #44157, #17334, #18836, #29841, #39288, #47790, #30131, #31949, #835, #35845, #36178, #21308, #4055, #23394, #29180, #277, #32626, #20118, #45153, #40141, #40574, #20608, #21220, #47831, #14944, #13247, #920, #8836, #37890, #15855, #608, #34459, #8095, #47030, #10901, #10810, #43936, #3119, #43815, #9272, #31250, #12300, #19333, #31649, #9162, #27973, #28558, #5875, #38918, #5440, #48293, #29402, #28330, #31278, #477, #35806, #7833, #40282, #9224, #21173, #20658, #39240, #25965, #39906, #38941, #15625, #37518, #43714, #41182, #17874, #20001, #36122, #26490, #2459, #34419, #11288, #13268, #7778, #8838, #3493, #40724, #43983, #46029, #29359, #752, #33317, #2267, #19066, #32037, #29814, #17792, #29014, #23044, #11367, #14235, #10667, #35346, #18100, #26637, #18408, #21624, #20961, #39848 ) ) ;
#42713=LINE ( 'NONE', #46374, #27779 ) ;
#42715=EDGE_CURVE ( 'NONE', #29358, #44403, #5719, .T. ) ;
#42728=DIRECTION ( 'NONE',  ( -1.000000000000000000, -0.000000000000000000, 0.000000000000000000 ) ) ;
#42734=CYLINDRICAL_SURFACE ( 'NONE', #19845, 16.00000000000000000 ) ;
#42737=FACE_OUTER_BOUND ( 'NONE', #18385, .T. ) ;
#42743=CARTESIAN_POINT ( 'NONE',  ( 10.00000000000000000, -6.555932627142143865, -37.01155633439065440 ) ) ;
#42765=EDGE_LOOP ( 'NONE', ( #37014, #7900, #19796, #7602, #22676, #44493, #4783, #31601, #15430, #4770, #29590, #4639, #45413, #35431, #12990, #18972, #13895, #46437, #3446, #25657, #10322, #17124, #34268, #41111, #35709, #9164, #20502, #27046, #39331, #35119, #13382, #46845, #11944, #42510, #34514, #48357, #41877, #41801, #28450, #45305, #35861, #16871, #7443, #20672, #15632, #19096, #33909, #31857, #28961, #17407, #5735, #46440, #23380, #18117, #31781, #14065, #23127, #39080, #28676, #8724, #17924, #26645, #16450, #43400, #2695, #17530, #8956, #16676, #559, #42808, #14891, #16581, #36272, #39545, #14708, #20615, #33621, #20311, #16172, #48143, #9264, #20267, #36661, #27263, #15718, #46977, #41974, #10252, #1647, #18044, #23212, #7048, #37664, #48401, #6831, #427, #27985, #5788, #4340, #17398, #24452, #35936, #14220, #43873, #11087, #8828, #12435, #21378, #46929, #22488, #11668, #1710, #27369, #22716, #4056, #40813, #31115, #17669, #26941, #39809, #37438, #19284, #14088, #21782, #3457, #27300, #39880, #19506, #16303, #5803, #3072, #11170, #36438, #27416, #15137, #16952, #31950, #19667, #47695, #2397, #20171, #16598, #21332, #42274, #8498, #46692, #37776, #20212, #26209, #27719, #5522, #32207, #7943, #34750, #18684, #10951, #36777, #13882, #11212, #2336, #32764, #18370, #34791, #1363, #9965 ) ) ;
#42775=ORIENTED_EDGE ( 'NONE', *, *, #33801, .F. ) ;
#42777=EDGE_CURVE ( 'NONE', #2211, #41993, #41522, .T. ) ;
#42779=CARTESIAN_POINT ( 'NONE',  ( -3.000000000000000000, -22.32062822937469804, -14.36278369418829826 ) ) ;
#42803=ORIENTED_EDGE ( 'NONE', *, *, #43324, .T. ) ;
#42805=CIRCLE ( 'NONE', #24038, 16.00000000000000000 ) ;
#42808=ORIENTED_EDGE ( 'NONE', *, *, #1153, .T. ) ;
#42810=DIRECTION ( 'NONE',  ( 1.000000000000000000, 0.000000000000000000, 0.000000000000000000 ) ) ;
#42811=DIRECTION ( 'NONE',  ( -1.000000000000000000, 0.000000000000000000, -0.000000000000000000 ) ) ;
#42812=EDGE_CURVE ( 'NONE', #12381, #4718, #22909, .T. ) ;
#42816=PLANE ( 'NONE',  #37819 ) ;
#42817=DIRECTION ( 'NONE',  ( -1.000000000000000000, -0.000000000000000000, -0.000000000000000000 ) ) ;
#42826=AXIS2_PLACEMENT_3D ( 'NONE', #48255, #14732, #7380 ) ;
#42827=EDGE_CURVE ( 'NONE', #9644, #16667, #30275, .T. ) ;
#42840=ORIENTED_EDGE ( 'NONE', *, *, #45031, .T. ) ;
#42841=DIRECTION ( 'NONE',  ( 0.000000000000000000, 0.8910065241883656784, 0.4539904997395510788 ) ) ;
#42845=ORIENTED_EDGE ( 'NONE', *, *, #42494, .F. ) ;
#42853=ORIENTED_EDGE ( 'NONE', *, *, #41708, .T. ) ;
#42863=DIRECTION ( 'NONE',  ( 0.000000000000000000, 0.000000000000000000, 1.000000000000000000 ) ) ;
#42866=DIRECTION ( 'NONE',  ( 0.000000000000000000, 0.8910065241883688980, -0.4539904997395445840 ) ) ;
#42875=DIRECTION ( 'NONE',  ( -1.000000000000000000, -0.000000000000000000, 0.000000000000000000 ) ) ;
#42886=DIRECTION ( 'NONE',  ( 0.000000000000000000, -0.9945218953682730678, -0.1045284632676570929 ) ) ;
#42891=EDGE_CURVE ( 'NONE', #46797, #13463, #13539, .T. ) ;
#42898=AXIS2_PLACEMENT_3D ( 'NONE', #17543, #17296, #2602 ) ;
#42915=CARTESIAN_POINT ( 'NONE',  ( 0.000000000000000000, -1.278221433540502217, 26.51162292216071847 ) ) ;
#42919=LINE ( 'NONE', #2051, #27591 ) ;
#42920=DIRECTION ( 'NONE',  ( 1.000000000000000000, 0.000000000000000000, 0.000000000000000000 ) ) ;
#42922=CARTESIAN_POINT ( 'NONE',  ( 10.00000000000000000, -22.64427369931148348, -30.00120703465229965 ) ) ;
#42927=FACE_OUTER_BOUND ( 'NONE', #46511, .T. ) ;
#42934=EDGE_CURVE ( 'NONE', #36833, #7751, #38552, .T. ) ;
#42956=EDGE_LOOP ( 'NONE', ( #16293, #12102, #4201, #5704 ) ) ;
#42966=FACE_BOUND ( 'NONE', #27547, .T. ) ;
#42975=DIRECTION ( 'NONE',  ( -1.000000000000000000, -0.000000000000000000, -0.000000000000000000 ) ) ;
#42979=ORIENTED_EDGE ( 'NONE', *, *, #2303, .T. ) ;
#42988=DIRECTION ( 'NONE',  ( -1.000000000000000000, 0.000000000000000000, 0.000000000000000000 ) ) ;
#43004=EDGE_CURVE ( 'NONE', #994, #45324, #4219, .T. ) ;
#43009=CARTESIAN_POINT ( 'NONE',  ( 10.00000000000000000, -12.42422080174663712, 35.38097989696507994 ) ) ;
#43015=DIRECTION ( 'NONE',  ( 0.000000000000000000, 0.8090169943749432324, 0.5877852522924789103 ) ) ;
#43022=CARTESIAN_POINT ( 'NONE',  ( 10.00000000000000000, -5.202137450156655518, 37.22597642581156663 ) ) ;
#43027=VERTEX_POINT ( 'NONE', #43685 ) ;
#43037=CARTESIAN_POINT ( 'NONE',  ( 10.00000000000000000, 30.00120703465236716, -22.64427369931138756 ) ) ;
#43041=VECTOR ( 'NONE', #19705, 999.9999999999998863 ) ;
#43044=ORIENTED_EDGE ( 'NONE', *, *, #33335, .T. ) ;
#43047=DIRECTION ( 'NONE',  ( -1.000000000000000000, -0.000000000000000000, 0.000000000000000000 ) ) ;
#43063=CIRCLE ( 'NONE', #7873, 37.49900000000001654 ) ;
#43077=CARTESIAN_POINT ( 'NONE',  ( 0.000000000000000000, 0.000000000000000000, 0.000000000000000000 ) ) ;
#43097=DIRECTION ( 'NONE',  ( -1.000000000000000000, -0.000000000000000000, -0.000000000000000000 ) ) ;
#43105=CARTESIAN_POINT ( 'NONE',  ( 0.000000000000000000, -3.948201729842037544, -23.21447184625298021 ) ) ;
#43114=DIRECTION ( 'NONE',  ( 0.000000000000000000, 0.000000000000000000, 1.000000000000000000 ) ) ;
#43122=CARTESIAN_POINT ( 'NONE',  ( 10.00000000000000000, -41.81611651403859042, -3.925862922256606602 ) ) ;
#43127=AXIS2_PLACEMENT_3D ( 'NONE', #30888, #45815, #6800 ) ;
#43142=EDGE_CURVE ( 'NONE', #45887, #45280, #44648, .T. ) ;
#43154=ORIENTED_EDGE ( 'NONE', *, *, #35601, .F. ) ;
#43157=FACE_OUTER_BOUND ( 'NONE', #31201, .T. ) ;
#43159=ADVANCED_FACE ( 'NONE', ( #22614 ), #4022, .T. ) ;
#43162=SURFACE_STYLE_FILL_AREA ( #46604 ) ;
#43167=CARTESIAN_POINT ( 'NONE',  ( 0.000000000000000000, 0.000000000000000000, 0.000000000000000000 ) ) ;
#43172=ADVANCED_FACE ( 'NONE', ( #18461 ), #48317, .T. ) ;
#43176=VERTEX_POINT ( 'NONE', #40735 ) ;
#43177=CIRCLE ( 'NONE', #951, 16.00000000000000000 ) ;
#43180=ORIENTED_EDGE ( 'NONE', *, *, #36586, .T. ) ;
#43188=DIRECTION ( 'NONE',  ( 0.000000000000000000, 0.000000000000000000, 1.000000000000000000 ) ) ;
#43189=ORIENTED_EDGE ( 'NONE', *, *, #30786, .F. ) ;
#43196=ORIENTED_EDGE ( 'NONE', *, *, #32178, .F. ) ;
#43201=DIRECTION ( 'NONE',  ( -1.000000000000000000, 0.000000000000000000, 0.000000000000000000 ) ) ;
#43206=DIRECTION ( 'NONE',  ( 0.000000000000000000, -0.2079116908177664758, 0.9781476007338042455 ) ) ;
#43223=ORIENTED_EDGE ( 'NONE', *, *, #22179, .T. ) ;
#43224=EDGE_CURVE ( 'NONE', #26631, #41727, #47971, .T. ) ;
#43225=CARTESIAN_POINT ( 'NONE',  ( 0.000000000000000000, -18.13022148937243472, -15.02647892043568767 ) ) ;
#43229=DIRECTION ( 'NONE',  ( 0.000000000000000000, 0.9510565162951521989, 0.3090169943749515591 ) ) ;
#43232=AXIS2_PLACEMENT_3D ( 'NONE', #27457, #19370, #16204 ) ;
#43238=CARTESIAN_POINT ( 'NONE',  ( 0.000000000000000000, 23.59884966291538433, -12.14883922797231719 ) ) ;
#43261=FACE_OUTER_BOUND ( 'NONE', #4590, .T. ) ;
#43265=CIRCLE ( 'NONE', #15901, 15.99999999999999822 ) ;
#43268=AXIS2_PLACEMENT_3D ( 'NONE', #9268, #46733, #31565 ) ;
#43275=CARTESIAN_POINT ( 'NONE',  ( -10.00000000000000000, 0.000000000000000000, 0.000000000000000000 ) ) ;
#43277=PLANE ( 'NONE',  #5213 ) ;
#43280=EDGE_CURVE ( 'NONE', #22836, #44307, #6964, .T. ) ;
#43287=CIRCLE ( 'NONE', #24512, 37.49900000000000944 ) ;
#43294=DIRECTION ( 'NONE',  ( 0.000000000000000000, 0.000000000000000000, 1.000000000000000000 ) ) ;
#43296=AXIS2_PLACEMENT_3D ( 'NONE', #32871, #40246, #40482 ) ;
#43306=DIRECTION ( 'NONE',  ( 1.000000000000000000, 0.000000000000000000, 0.000000000000000000 ) ) ;
#43311=ORIENTED_EDGE ( 'NONE', *, *, #33981, .T. ) ;
#43314=DIRECTION ( 'NONE',  ( -1.000000000000000000, 0.000000000000000000, -0.000000000000000000 ) ) ;
#43323=VECTOR ( 'NONE', #29801, 1000.000000000000000 ) ;
#43324=EDGE_CURVE ( 'NONE', #46585, #22321, #20379, .T. ) ;
#43328=AXIS2_PLACEMENT_3D ( 'NONE', #6707, #25532, #3254 ) ;
#43335=ORIENTED_EDGE ( 'NONE', *, *, #14816, .F. ) ;
#43342=CIRCLE ( 'NONE', #1117, 37.49900000000000944 ) ;
#43345=EDGE_CURVE ( 'NONE', #22843, #29358, #27264, .T. ) ;
#43356=ORIENTED_EDGE ( 'NONE', *, *, #32178, .T. ) ;
#43358=VERTEX_POINT ( 'NONE', #27028 ) ;
#43371=ORIENTED_EDGE ( 'NONE', *, *, #41867, .T. ) ;
#43372=CARTESIAN_POINT ( 'NONE',  ( 0.000000000000000000, 41.91543099594818500, -2.663952781846294915 ) ) ;
#43375=AXIS2_PLACEMENT_3D ( 'NONE', #43275, #32260, #15044 ) ;
#43381=EDGE_CURVE ( 'NONE', #38831, #25953, #3421, .T. ) ;
#43384=EDGE_CURVE ( 'NONE', #33558, #960, #9683, .T. ) ;
#43392=ORIENTED_EDGE ( 'NONE', *, *, #22820, .T. ) ;
#43397=AXIS2_PLACEMENT_3D ( 'NONE', #20559, #5645, #39425 ) ;
#43399=DIRECTION ( 'NONE',  ( 0.000000000000000000, -0.5877852522924801315, 0.8090169943749421222 ) ) ;
#43400=ORIENTED_EDGE ( 'NONE', *, *, #35915, .T. ) ;
#43403=CARTESIAN_POINT ( 'NONE',  ( 0.000000000000000000, 0.000000000000000000, 0.000000000000000000 ) ) ;
#43408=DIRECTION ( 'NONE',  ( -1.000000000000000000, 0.000000000000000000, 0.000000000000000000 ) ) ;
#43415=CARTESIAN_POINT ( 'NONE',  ( -3.000000000000000000, -10.45096189432344147, 21.10159698893426494 ) ) ;
#43419=ORIENTED_EDGE ( 'NONE', *, *, #43345, .T. ) ;
#43420=VECTOR ( 'NONE', #4746, 1000.000000000000000 ) ;
#43421=CARTESIAN_POINT ( 'NONE',  ( -3.000000000000000000, 22.07842321921481243, 8.187992925817422218 ) ) ;
#43423=CARTESIAN_POINT ( 'NONE',  ( 10.00000000000000000, 10.96151621346540317, -35.95386929396244113 ) ) ;
#43428=AXIS2_PLACEMENT_3D ( 'NONE', #40429, #17654, #48243 ) ;
#43458=FACE_OUTER_BOUND ( 'NONE', #32057, .T. ) ;
#43459=DIRECTION ( 'NONE',  ( -1.000000000000000000, -0.000000000000000000, 0.000000000000000000 ) ) ;
#43462=DIRECTION ( 'NONE',  ( -1.000000000000000000, -0.000000000000000000, 0.000000000000000000 ) ) ;
#43464=DIRECTION ( 'NONE',  ( 0.000000000000000000, 0.000000000000000000, 1.000000000000000000 ) ) ;
#43466=LINE ( 'NONE', #36102, #45769 ) ;
#43471=DIRECTION ( 'NONE',  ( 0.000000000000000000, 0.000000000000000000, 1.000000000000000000 ) ) ;
#43479=LINE ( 'NONE', #43225, #33216 ) ;
#43480=ORIENTED_EDGE ( 'NONE', *, *, #40677, .F. ) ;
#43481=CIRCLE ( 'NONE', #30979, 16.00000000000000355 ) ;
#43486=VERTEX_POINT ( 'NONE', #6431 ) ;
#43489=AXIS2_PLACEMENT_3D ( 'NONE', #31744, #20698, #35633 ) ;
#43497=ORIENTED_EDGE ( 'NONE', *, *, #5826, .F. ) ;
#43514=DIRECTION ( 'NONE',  ( 0.000000000000000000, 0.000000000000000000, 1.000000000000000000 ) ) ;
#43518=ORIENTED_EDGE ( 'NONE', *, *, #1224, .F. ) ;
#43523=CARTESIAN_POINT ( 'NONE',  ( -3.000000000000000000, -22.67460108101783334, 6.353146135317912169 ) ) ;
#43529=ORIENTED_EDGE ( 'NONE', *, *, #1153, .F. ) ;
#43540=PLANE ( 'NONE',  #18667 ) ;
#43545=AXIS2_PLACEMENT_3D ( 'NONE', #21670, #36357, #33168 ) ;
#43560=EDGE_CURVE ( 'NONE', #1910, #39296, #30806, .T. ) ;
#43566=FACE_OUTER_BOUND ( 'NONE', #12865, .T. ) ;
#43574=CARTESIAN_POINT ( 'NONE',  ( 10.00000000000000000, 33.79645857604513992, -16.45098606841138178 ) ) ;
#43577=CARTESIAN_POINT ( 'NONE',  ( 0.000000000000000000, 10.74501242461333028, -35.92658777277499382 ) ) ;
#43581=LINE ( 'NONE', #5909, #7449 ) ;
#43588=ORIENTED_EDGE ( 'NONE', *, *, #30985, .T. ) ;
#43599=DIRECTION ( 'NONE',  ( 0.000000000000000000, 0.000000000000000000, -1.000000000000000000 ) ) ;
#43601=CYLINDRICAL_SURFACE ( 'NONE', #8895, 16.00000000000000000 ) ;
#43605=EDGE_CURVE ( 'NONE', #40065, #7437, #19079, .T. ) ;
#43608=CARTESIAN_POINT ( 'NONE',  ( 10.00000000000000000, 4.992566952385523393, -37.16516213103272293 ) ) ;
#43615=PLANE ( 'NONE',  #20584 ) ;
#43618=VECTOR ( 'NONE', #30153, 1000.000000000000227 ) ;
#43621=ORIENTED_EDGE ( 'NONE', *, *, #46112, .F. ) ;
#43625=DIRECTION ( 'NONE',  ( 0.000000000000000000, 0.4067366430757887730, 0.9135454576426059736 ) ) ;
#43627=AXIS2_PLACEMENT_3D ( 'NONE', #37263, #19138, #11801 ) ;
#43631=ORIENTED_EDGE ( 'NONE', *, *, #17674, .F. ) ;
#43634=CARTESIAN_POINT ( 'NONE',  ( 10.00000000000000000, 0.000000000000000000, 0.000000000000000000 ) ) ;
#43647=VECTOR ( 'NONE', #45191, 1000.000000000000227 ) ;
#43652=DIRECTION ( 'NONE',  ( -1.000000000000000000, 0.000000000000000000, 0.000000000000000000 ) ) ;
#43656=VERTEX_POINT ( 'NONE', #34226 ) ;
#43658=CARTESIAN_POINT ( 'NONE',  ( 0.000000000000000000, 41.81611651403861885, 3.925862922256313503 ) ) ;
#43659=ORIENTED_EDGE ( 'NONE', *, *, #32978, .F. ) ;
#43662=ORIENTED_EDGE ( 'NONE', *, *, #629, .T. ) ;
#43667=EDGE_CURVE ( 'NONE', #44212, #47865, #29258, .T. ) ;
#43671=DIRECTION ( 'NONE',  ( 0.000000000000000000, 0.3090169943749412340, 0.9510565162951556406 ) ) ;
#43685=CARTESIAN_POINT ( 'NONE',  ( 0.000000000000000000, -4.992566952385247170, 37.16516213103275845 ) ) ;
#43686=CARTESIAN_POINT ( 'NONE',  ( 0.000000000000000000, -29.81001611431024045, 22.74946021919122430 ) ) ;
#43692=VECTOR ( 'NONE', #45230, 1000.000000000000000 ) ;
#43698=DIRECTION ( 'NONE',  ( 0.000000000000000000, 0.000000000000000000, 1.000000000000000000 ) ) ;
#43705=ADVANCED_FACE ( 'NONE', ( #7803 ), #18584, .T. ) ;
#43714=ADVANCED_FACE ( 'NONE', ( #10426 ), #6764, .F. ) ;
#43715=ORIENTED_EDGE ( 'NONE', *, *, #42204, .T. ) ;
#43727=ORIENTED_EDGE ( 'NONE', *, *, #35148, .T. ) ;
#43737=CIRCLE ( 'NONE', #10124, 42.00000000000000000 ) ;
#43752=FACE_OUTER_BOUND ( 'NONE', #29454, .T. ) ;
#43770=FACE_OUTER_BOUND ( 'NONE', #12778, .T. ) ;
#43777=VERTEX_POINT ( 'NONE', #21444 ) ;
#43793=ORIENTED_EDGE ( 'NONE', *, *, #39997, .T. ) ;
#43809=CARTESIAN_POINT ( 'NONE',  ( 10.00000000000000178, 0.000000000000000000, 0.000000000000000000 ) ) ;
#43815=ADVANCED_FACE ( 'NONE', ( #29516 ), #44206, .F. ) ;
#43818=EDGE_CURVE ( 'NONE', #28645, #38352, #25590, .T. ) ;
#43819=VERTEX_POINT ( 'NONE', #33186 ) ;
#43822=FACE_OUTER_BOUND ( 'NONE', #28734, .T. ) ;
#43829=VECTOR ( 'NONE', #14249, 1000.000000000000000 ) ;
#43830=ORIENTED_EDGE ( 'NONE', *, *, #40716, .T. ) ;
#43834=LINE ( 'NONE', #29623, #29994 ) ;
#43836=DIRECTION ( 'NONE',  ( 0.000000000000000000, 0.000000000000000000, 1.000000000000000000 ) ) ;
#43838=ORIENTED_EDGE ( 'NONE', *, *, #22823, .F. ) ;
#43844=VERTEX_POINT ( 'NONE', #27060 ) ;
#43846=DIRECTION ( 'NONE',  ( -1.000000000000000000, 0.000000000000000000, -0.000000000000000000 ) ) ;
#43849=VECTOR ( 'NONE', #42133, 1000.000000000000000 ) ;
#43856=ORIENTED_EDGE ( 'NONE', *, *, #18687, .F. ) ;
#43872=DIRECTION ( 'NONE',  ( 0.000000000000000000, 0.9876883405951372152, 0.1564344650402347547 ) ) ;
#43873=ORIENTED_EDGE ( 'NONE', *, *, #11174, .T. ) ;
#43878=CARTESIAN_POINT ( 'NONE',  ( -3.000000000000000000, -22.32062822937469804, -14.36278369418829826 ) ) ;
#43880=DIRECTION ( 'NONE',  ( 1.000000000000000000, -0.000000000000000000, 0.000000000000000000 ) ) ;
#43902=ORIENTED_EDGE ( 'NONE', *, *, #48330, .F. ) ;
#43909=CARTESIAN_POINT ( 'NONE',  ( 0.000000000000000000, -22.67460108101782978, 6.353146135317912169 ) ) ;
#43927=AXIS2_PLACEMENT_3D ( 'NONE', #4516, #41716, #15300 ) ;
#43928=DIRECTION ( 'NONE',  ( -1.000000000000000000, 0.000000000000000000, 0.000000000000000000 ) ) ;
#43932=FACE_OUTER_BOUND ( 'NONE', #29755, .T. ) ;
#43936=ADVANCED_FACE ( 'NONE', ( #8205 ), #7717, .F. ) ;
#43939=DIRECTION ( 'NONE',  ( -1.000000000000000000, 0.000000000000000000, 0.000000000000000000 ) ) ;
#43946=ORIENTED_EDGE ( 'NONE', *, *, #3992, .T. ) ;
#43947=EDGE_CURVE ( 'NONE', #8149, #46255, #1853, .T. ) ;
#43956=CARTESIAN_POINT ( 'NONE',  ( -3.000000000000000000, 22.07842321921492612, -8.187992925817130896 ) ) ;
#43976=EDGE_CURVE ( 'NONE', #38352, #23166, #41008, .T. ) ;
#43977=DIRECTION ( 'NONE',  ( 0.000000000000000000, 0.000000000000000000, 1.000000000000000000 ) ) ;
#43983=ADVANCED_FACE ( 'NONE', ( #43458 ), #24839, .F. ) ;
#43988=EDGE_CURVE ( 'NONE', #9394, #19028, #13108, .T. ) ;
#43997=DIRECTION ( 'NONE',  ( 0.000000000000000000, -0.9876883405951361050, -0.1564344650402419989 ) ) ;
#44011=DIRECTION ( 'NONE',  ( -1.000000000000000000, 0.000000000000000000, -0.000000000000000000 ) ) ;
#44032=ORIENTED_EDGE ( 'NONE', *, *, #24717, .T. ) ;
#44041=EDGE_CURVE ( 'NONE', #6044, #5383, #28491, .T. ) ;
#44046=EDGE_LOOP ( 'NONE', ( #34866, #25237, #43419, #31885 ) ) ;
#44055=CYLINDRICAL_SURFACE ( 'NONE', #31719, 16.00000000000000000 ) ;
#44056=FACE_OUTER_BOUND ( 'NONE', #5229, .T. ) ;
#44060=VERTEX_POINT ( 'NONE', #23878 ) ;
#44061=AXIS2_PLACEMENT_3D ( 'NONE', #30967, #8909, #38539 ) ;
#44081=DIRECTION ( 'NONE',  ( 0.000000000000000000, 0.000000000000000000, -1.000000000000000000 ) ) ;
#44091=PLANE ( 'NONE',  #45684 ) ;
#44098=ORIENTED_EDGE ( 'NONE', *, *, #13923, .F. ) ;
#44104=ORIENTED_EDGE ( 'NONE', *, *, #6599, .T. ) ;
#44111=VECTOR ( 'NONE', #8869, 1000.000000000000000 ) ;
#44126=CARTESIAN_POINT ( 'NONE',  ( -3.000000000000000000, -11.95096189432312350, -23.69967320028773372 ) ) ;
#44134=PLANE ( 'NONE',  #8856 ) ;
#44152=DIRECTION ( 'NONE',  ( -1.000000000000000000, 0.000000000000000000, -0.000000000000000000 ) ) ;
#44157=ADVANCED_FACE ( 'NONE', ( #44167 ), #33391, .T. ) ;
#44162=CARTESIAN_POINT ( 'NONE',  ( 0.000000000000000000, -0.8828120875898013420, -37.48860685352291711 ) ) ;
#44167=FACE_OUTER_BOUND ( 'NONE', #910, .T. ) ;
#44172=DIRECTION ( 'NONE',  ( 0.000000000000000000, 0.000000000000000000, -1.000000000000000000 ) ) ;
#44175=CIRCLE ( 'NONE', #27771, 37.49900000000000944 ) ;
#44177=ORIENTED_EDGE ( 'NONE', *, *, #35320, .T. ) ;
#44179=AXIS2_PLACEMENT_3D ( 'NONE', #24607, #5285, #20430 ) ;
#44186=DIRECTION ( 'NONE',  ( -1.000000000000000000, 0.000000000000000000, -0.000000000000000000 ) ) ;
#44197=ADVANCED_FACE ( 'NONE', ( #3272 ), #29236, .T. ) ;
#44199=EDGE_CURVE ( 'NONE', #1910, #27382, #14476, .T. ) ;
#44202=VERTEX_POINT ( 'NONE', #15033 ) ;
#44204=ORIENTED_EDGE ( 'NONE', *, *, #9339, .F. ) ;
#44206=PLANE ( 'NONE',  #11312 ) ;
#44212=VERTEX_POINT ( 'NONE', #3037 ) ;
#44214=VERTEX_POINT ( 'NONE', #18202 ) ;
#44229=ORIENTED_EDGE ( 'NONE', *, *, #47314, .F. ) ;
#44236=CARTESIAN_POINT ( 'NONE',  ( 0.000000000000000000, 24.81905959214261514, 9.408202855044827118 ) ) ;
#44238=CIRCLE ( 'NONE', #24701, 37.49900000000000944 ) ;
#44239=CARTESIAN_POINT ( 'NONE',  ( -3.000000000000000000, -3.948201729842038432, -23.21447184625298021 ) ) ;
#44247=VECTOR ( 'NONE', #37255, 1000.000000000000000 ) ;
#44252=FACE_OUTER_BOUND ( 'NONE', #41376, .T. ) ;
#44254=VERTEX_POINT ( 'NONE', #45867 ) ;
#44258=AXIS2_PLACEMENT_3D ( 'NONE', #20634, #43408, #43872 ) ;
#44271=VERTEX_POINT ( 'NONE', #42176 ) ;
#44283=AXIS2_PLACEMENT_3D ( 'NONE', #14119, #29041, #7734 ) ;
#44285=ORIENTED_EDGE ( 'NONE', *, *, #40787, .F. ) ;
#44300=CYLINDRICAL_SURFACE ( 'NONE', #5710, 16.00000000000000000 ) ;
#44305=ORIENTED_EDGE ( 'NONE', *, *, #15905, .T. ) ;
#44307=VERTEX_POINT ( 'NONE', #45603 ) ;
#44310=EDGE_CURVE ( 'NONE', #13250, #27191, #34769, .T. ) ;
#44312=EDGE_CURVE ( 'NONE', #27800, #28663, #30680, .T. ) ;
#44327=DIRECTION ( 'NONE',  ( 0.000000000000000000, 0.000000000000000000, 1.000000000000000000 ) ) ;
#44330=CARTESIAN_POINT ( 'NONE',  ( 0.000000000000000000, 9.188173127307290855, 40.98264845739752360 ) ) ;
#44344=EDGE_LOOP ( 'NONE', ( #35437, #48435, #7396, #29889 ) ) ;
#44346=DIRECTION ( 'NONE',  ( 0.000000000000000000, 0.9510565162951521989, 0.3090169943749515591 ) ) ;
#44361=CARTESIAN_POINT ( 'NONE',  ( 10.00000000000000000, -37.01155633439053361, -6.555932627142825986 ) ) ;
#44363=LINE ( 'NONE', #36761, #14584 ) ;
#44370=ORIENTED_EDGE ( 'NONE', *, *, #36639, .F. ) ;
#44380=VERTEX_POINT ( 'NONE', #45358 ) ;
#44381=VECTOR ( 'NONE', #31874, 1000.000000000000000 ) ;
#44385=EDGE_CURVE ( 'NONE', #3134, #41559, #38035, .T. ) ;
#44397=FACE_OUTER_BOUND ( 'NONE', #36526, .T. ) ;
#44403=VERTEX_POINT ( 'NONE', #5233 ) ;
#44404=ORIENTED_EDGE ( 'NONE', *, *, #16774, .F. ) ;
#44411=CARTESIAN_POINT ( 'NONE',  ( 10.00000000000000000, 0.000000000000000000, 0.000000000000000000 ) ) ;
#44412=DIRECTION ( 'NONE',  ( -1.000000000000000000, -0.000000000000000000, 0.000000000000000000 ) ) ;
#44416=CARTESIAN_POINT ( 'NONE',  ( -3.000000000000000000, -3.948201729842348850, 23.21447184625293048 ) ) ;
#44417=VERTEX_POINT ( 'NONE', #35564 ) ;
#44438=DIRECTION ( 'NONE',  ( 0.000000000000000000, 0.000000000000000000, 1.000000000000000000 ) ) ;
#44443=CARTESIAN_POINT ( 'NONE',  ( 10.00000000000000000, -37.58145647212453611, -0.6853352020794456489 ) ) ;
#44457=FACE_OUTER_BOUND ( 'NONE', #10640, .T. ) ;
#44460=AXIS2_PLACEMENT_3D ( 'NONE', #9974, #10212, #32965 ) ;
#44465=CARTESIAN_POINT ( 'NONE',  ( 0.000000000000000000, 21.40280677340421889, -36.13751322684397138 ) ) ;
#44478=EDGE_CURVE ( 'NONE', #12245, #21082, #14375, .T. ) ;
#44483=DIRECTION ( 'NONE',  ( -0.000000000000000000, 0.9945218953682731788, 0.1045284632676559550 ) ) ;
#44489=EDGE_CURVE ( 'NONE', #17130, #6467, #31616, .T. ) ;
#44493=ORIENTED_EDGE ( 'NONE', *, *, #17999, .T. ) ;
#44502=ORIENTED_EDGE ( 'NONE', *, *, #2813, .F. ) ;
#44511=CARTESIAN_POINT ( 'NONE',  ( 10.00000000000000000, 0.000000000000000000, 37.49900000000000233 ) ) ;
#44519=AXIS2_PLACEMENT_3D ( 'NONE', #47400, #13874, #47621 ) ;
#44528=CYLINDRICAL_SURFACE ( 'NONE', #18481, 37.49900000000000233 ) ;
#44541=EDGE_CURVE ( 'NONE', #40027, #21200, #42535, .T. ) ;
#44552=CARTESIAN_POINT ( 'NONE',  ( 0.000000000000000000, -2.663952781845850826, -41.91543099594819921 ) ) ;
#44566=CARTESIAN_POINT ( 'NONE',  ( 10.00000000000000000, 17.67226234102826510, 33.17418723428314564 ) ) ;
#44575=CARTESIAN_POINT ( 'NONE',  ( 10.00000000000000000, 30.84782396557218931, 21.32104025579126017 ) ) ;
#44579=ORIENTED_EDGE ( 'NONE', *, *, #11570, .F. ) ;
#44594=AXIS2_PLACEMENT_3D ( 'NONE', #16229, #45851, #13039 ) ;
#44601=AXIS2_PLACEMENT_3D ( 'NONE', #13505, #28433, #21573 ) ;
#44624=CIRCLE ( 'NONE', #32873, 16.00000000000000000 ) ;
#44628=CIRCLE ( 'NONE', #14938, 37.49900000000000233 ) ;
#44632=AXIS2_PLACEMENT_3D ( 'NONE', #35496, #36452, #17356 ) ;
#44634=CARTESIAN_POINT ( 'NONE',  ( 10.00000000000000000, 0.000000000000000000, 0.000000000000000000 ) ) ;
#44644=DIRECTION ( 'NONE',  ( 0.000000000000000000, 0.000000000000000000, 1.000000000000000000 ) ) ;
#44646=DIRECTION ( 'NONE',  ( 0.000000000000000000, 0.8090169943749447867, 0.5877852522924769119 ) ) ;
#44647=EDGE_LOOP ( 'NONE', ( #22376, #21456, #13853, #40773 ) ) ;
#44648=LINE ( 'NONE', #37544, #8116 ) ;
#44649=CARTESIAN_POINT ( 'NONE',  ( 10.00000000000000000, -37.22597642581153821, -5.202137450156795850 ) ) ;
#44660=LINE ( 'NONE', #33164, #1844 ) ;
#44666=CARTESIAN_POINT ( 'NONE',  ( -3.000000000000000000, 22.07842321921481243, 8.187992925817422218 ) ) ;
#44675=FACE_OUTER_BOUND ( 'NONE', #23806, .T. ) ;
#44685=CARTESIAN_POINT ( 'NONE',  ( 0.000000000000000000, 15.48615015657637883, -39.04073710021327770 ) ) ;
#44698=CYLINDRICAL_SURFACE ( 'NONE', #10798, 37.49900000000000233 ) ;
#44720=DIRECTION ( 'NONE',  ( 0.000000000000000000, 0.000000000000000000, -1.000000000000000000 ) ) ;
#44721=CYLINDRICAL_SURFACE ( 'NONE', #36290, 16.00000000000000000 ) ;
#44731=DIRECTION ( 'NONE',  ( 0.000000000000000000, 0.000000000000000000, 1.000000000000000000 ) ) ;
#44741=VERTEX_POINT ( 'NONE', #7630 ) ;
#44747=DIRECTION ( 'NONE',  ( 0.000000000000000000, -0.9945218953682730678, -0.1045284632676570791 ) ) ;
#44749=CARTESIAN_POINT ( 'NONE',  ( 0.000000000000000000, 6.736453364083555329, 36.88895765772635116 ) ) ;
#44753=ORIENTED_EDGE ( 'NONE', *, *, #22436, .F. ) ;
#44762=FACE_OUTER_BOUND ( 'NONE', #31803, .T. ) ;
#44766=VECTOR ( 'NONE', #5103, 1000.000000000000000 ) ;
#44773=EDGE_CURVE ( 'NONE', #40664, #23509, #1908, .T. ) ;
#44782=EDGE_LOOP ( 'NONE', ( #7225, #7597, #8448, #5020 ) ) ;
#44793=AXIS2_PLACEMENT_3D ( 'NONE', #4558, #46399, #27083 ) ;
#44799=EDGE_LOOP ( 'NONE', ( #19047, #10527, #15423, #34138 ) ) ;
#44825=ORIENTED_EDGE ( 'NONE', *, *, #38405, .F. ) ;
#44832=DIRECTION ( 'NONE',  ( 0.000000000000000000, 0.7431448254773862505, 0.6691306063588672304 ) ) ;
#44837=DIRECTION ( 'NONE',  ( 0.000000000000000000, 0.000000000000000000, -1.000000000000000000 ) ) ;
#44838=LINE ( 'NONE', #11073, #34191 ) ;
#44844=CARTESIAN_POINT ( 'NONE',  ( 0.000000000000000000, -35.92658777277502935, -10.74501242461320594 ) ) ;
#44846=VERTEX_POINT ( 'NONE', #9542 ) ;
#44849=AXIS2_PLACEMENT_3D ( 'NONE', #24275, #21071, #2469 ) ;
#44869=LINE ( 'NONE', #15267, #35155 ) ;
#44879=FACE_OUTER_BOUND ( 'NONE', #32068, .T. ) ;
#44880=VECTOR ( 'NONE', #33229, 1000.000000000000000 ) ;
#44883=VERTEX_POINT ( 'NONE', #2212 ) ;
#44885=ADVANCED_FACE ( 'NONE', ( #20316 ), #17136, .T. ) ;
#44892=VERTEX_POINT ( 'NONE', #9080 ) ;
#44901=DIRECTION ( 'NONE',  ( -1.000000000000000000, -0.000000000000000000, 0.000000000000000000 ) ) ;
#44913=CARTESIAN_POINT ( 'NONE',  ( 0.000000000000000000, -15.48615015657556171, -39.04073710021360455 ) ) ;
#44914=CIRCLE ( 'NONE', #2687, 37.49900000000000233 ) ;
#44917=ORIENTED_EDGE ( 'NONE', *, *, #27180, .T. ) ;
#44922=VERTEX_POINT ( 'NONE', #12751 ) ;
#44932=DIRECTION ( 'NONE',  ( 0.000000000000000000, -0.2079116908177532363, -0.9781476007338069101 ) ) ;
#44933=DIRECTION ( 'NONE',  ( -1.000000000000000000, -0.000000000000000000, -0.000000000000000000 ) ) ;
#44937=VERTEX_POINT ( 'NONE', #36924 ) ;
#44948=CARTESIAN_POINT ( 'NONE',  ( -3.000000000000000000, -3.948201729842348850, 23.21447184625293048 ) ) ;
#44965=CARTESIAN_POINT ( 'NONE',  ( 0.000000000000000000, -38.55633173627022359, 16.65560815589396526 ) ) ;
#44983=ORIENTED_EDGE ( 'NONE', *, *, #45035, .F. ) ;
#44988=ORIENTED_EDGE ( 'NONE', *, *, #19399, .T. ) ;
#44990=CIRCLE ( 'NONE', #38745, 15.99999999999999822 ) ;
#44991=EDGE_CURVE ( 'NONE', #34977, #21133, #36692, .T. ) ;
#44994=CIRCLE ( 'NONE', #23895, 15.99999999999999822 ) ;
#44996=ORIENTED_EDGE ( 'NONE', *, *, #14535, .F. ) ;
#44999=DIRECTION ( 'NONE',  ( 1.000000000000000000, 0.000000000000000000, 0.000000000000000000 ) ) ;
#45000=CARTESIAN_POINT ( 'NONE',  ( 10.00000000000000000, -33.80338159004273280, -16.23288003029533044 ) ) ;
#45002=DIRECTION ( 'NONE',  ( -0.000000000000000000, -0.9135454576426004225, -0.4067366430758009854 ) ) ;
#45007=DIRECTION ( 'NONE',  ( -1.000000000000000000, 0.000000000000000000, -0.000000000000000000 ) ) ;
#45014=AXIS2_PLACEMENT_3D ( 'NONE', #31377, #27949, #42866 ) ;
#45015=LINE ( 'NONE', #11489, #45440 ) ;
#45022=CARTESIAN_POINT ( 'NONE',  ( 10.00000000000000000, 0.000000000000000000, 0.000000000000000000 ) ) ;
#45028=CIRCLE ( 'NONE', #35631, 16.00000000000000000 ) ;
#45031=EDGE_CURVE ( 'NONE', #22790, #29332, #29254, .T. ) ;
#45035=EDGE_CURVE ( 'NONE', #2188, #20236, #32555, .T. ) ;
#45037=LINE ( 'NONE', #11987, #21696 ) ;
#45047=ADVANCED_FACE ( 'NONE', ( #6607 ), #40613, .T. ) ;
#45053=ORIENTED_EDGE ( 'NONE', *, *, #37085, .T. ) ;
#45054=VERTEX_POINT ( 'NONE', #6372 ) ;
#45065=DIRECTION ( 'NONE',  ( 1.000000000000000000, -0.000000000000000000, -0.000000000000000000 ) ) ;
#45067=DIRECTION ( 'NONE',  ( -1.000000000000000000, -0.000000000000000000, -0.000000000000000000 ) ) ;
#45070=CARTESIAN_POINT ( 'NONE',  ( 0.000000000000000000, 0.000000000000000000, 0.000000000000000000 ) ) ;
#45071=DIRECTION ( 'NONE',  ( 0.000000000000000000, 0.9781476007338041345, 0.2079116908177664480 ) ) ;
#45075=ORIENTED_EDGE ( 'NONE', *, *, #29629, .T. ) ;
#45076=CYLINDRICAL_SURFACE ( 'NONE', #38522, 37.49900000000000233 ) ;
#45082=VECTOR ( 'NONE', #42252, 1000.000000000000000 ) ;
#45083=DIRECTION ( 'NONE',  ( 1.000000000000000000, -0.000000000000000000, 0.000000000000000000 ) ) ;
#45084=LINE ( 'NONE', #3717, #25089 ) ;
#45086=CARTESIAN_POINT ( 'NONE',  ( 0.000000000000000000, 26.08949754953024325, 27.05870788708241648 ) ) ;
#45087=ORIENTED_EDGE ( 'NONE', *, *, #14203, .F. ) ;
#45093=ADVANCED_FACE ( 'NONE', ( #11249 ), #11729, .T. ) ;
#45095=DIRECTION ( 'NONE',  ( 0.000000000000000000, 0.9945218953682730678, 0.1045284632676570929 ) ) ;
#45097=DIRECTION ( 'NONE',  ( 1.000000000000000000, -0.000000000000000000, -0.000000000000000000 ) ) ;
#45102=ORIENTED_EDGE ( 'NONE', *, *, #35422, .T. ) ;
#45108=EDGE_CURVE ( 'NONE', #5144, #34646, #3454, .T. ) ;
#45127=CARTESIAN_POINT ( 'NONE',  ( 0.000000000000000000, -35.95386929396248377, -10.96151621346525751 ) ) ;
#45139=DIRECTION ( 'NONE',  ( 0.000000000000000000, 0.000000000000000000, 1.000000000000000000 ) ) ;
#45149=DIRECTION ( 'NONE',  ( -1.000000000000000000, 0.000000000000000000, 0.000000000000000000 ) ) ;
#45150=EDGE_CURVE ( 'NONE', #26165, #25953, #33991, .T. ) ;
#45151=DIRECTION ( 'NONE',  ( 0.000000000000000000, -0.5000000000000046629, 0.8660254037844359321 ) ) ;
#45152=DIRECTION ( 'NONE',  ( -1.000000000000000000, 0.000000000000000000, 0.000000000000000000 ) ) ;
#45153=ADVANCED_FACE ( 'NONE', ( #18585 ), #15409, .T. ) ;
#45164=EDGE_CURVE ( 'NONE', #5635, #30321, #33506, .T. ) ;
#45167=ORIENTED_EDGE ( 'NONE', *, *, #20315, .F. ) ;
#45169=AXIS2_PLACEMENT_3D ( 'NONE', #15609, #11948, #45465 ) ;
#45178=CARTESIAN_POINT ( 'NONE',  ( 10.00000000000000000, 0.000000000000000000, 0.000000000000000000 ) ) ;
#45186=ORIENTED_EDGE ( 'NONE', *, *, #43224, .F. ) ;
#45187=ORIENTED_EDGE ( 'NONE', *, *, #12780, .T. ) ;
#45188=LINE ( 'NONE', #19951, #37268 ) ;
#45191=DIRECTION ( 'NONE',  ( 0.000000000000000000, 0.9135454576426003115, 0.4067366430758017071 ) ) ;
#45198=DIRECTION ( 'NONE',  ( 0.000000000000000000, 0.4539904997395414754, 0.8910065241883706744 ) ) ;
#45200=FACE_OUTER_BOUND ( 'NONE', #27880, .T. ) ;
#45202=ORIENTED_EDGE ( 'NONE', *, *, #17618, .T. ) ;
#45223=ORIENTED_EDGE ( 'NONE', *, *, #25907, .T. ) ;
#45230=DIRECTION ( 'NONE',  ( -1.000000000000000000, -0.000000000000000000, 0.000000000000000000 ) ) ;
#45232=ORIENTED_EDGE ( 'NONE', *, *, #37138, .T. ) ;
#45252=EDGE_CURVE ( 'NONE', #38854, #27962, #44175, .T. ) ;
#45253=LINE ( 'NONE', #15406, #13489 ) ;
#45259=EDGE_CURVE ( 'NONE', #25953, #9753, #47281, .T. ) ;
#45279=VERTEX_POINT ( 'NONE', #20030 ) ;
#45280=VERTEX_POINT ( 'NONE', #45746 ) ;
#45281=DIRECTION ( 'NONE',  ( 0.000000000000000000, 0.000000000000000000, -1.000000000000000000 ) ) ;
#45292=VECTOR ( 'NONE', #6050, 1000.000000000000000 ) ;
#45296=DIRECTION ( 'NONE',  ( 0.000000000000000000, 0.3090169943749482839, -0.9510565162951533091 ) ) ;
#45298=ORIENTED_EDGE ( 'NONE', *, *, #6147, .F. ) ;
#45305=ORIENTED_EDGE ( 'NONE', *, *, #13963, .T. ) ;
#45322=FACE_OUTER_BOUND ( 'NONE', #6588, .T. ) ;
#45324=VERTEX_POINT ( 'NONE', #20506 ) ;
#45328=AXIS2_PLACEMENT_3D ( 'NONE', #12251, #42096, #45281 ) ;
#45340=CARTESIAN_POINT ( 'NONE',  ( -10.00000000000000000, 0.000000000000000000, 0.000000000000000000 ) ) ;
#45342=EDGE_CURVE ( 'NONE', #11474, #24209, #33630, .T. ) ;
#45349=DIRECTION ( 'NONE',  ( -1.000000000000000000, 0.000000000000000000, 0.000000000000000000 ) ) ;
#45352=CARTESIAN_POINT ( 'NONE',  ( 10.00000000000000000, 21.53537804866126137, -30.80686688396986028 ) ) ;
#45358=CARTESIAN_POINT ( 'NONE',  ( 0.000000000000000000, 9.615535125379096826, -24.73947219025904687 ) ) ;
#45360=CARTESIAN_POINT ( 'NONE',  ( 0.000000000000000000, 0.000000000000000000, 0.000000000000000000 ) ) ;
#45363=ADVANCED_FACE ( 'NONE', ( #11128 ), #17559, .T. ) ;
#45376=DIRECTION ( 'NONE',  ( 1.000000000000000000, 0.000000000000000000, 0.000000000000000000 ) ) ;
#45384=DIRECTION ( 'NONE',  ( 1.000000000000000000, -0.000000000000000000, -0.000000000000000000 ) ) ;
#45390=AXIS2_PLACEMENT_3D ( 'NONE', #10496, #43314, #25413 ) ;
#45392=DIRECTION ( 'NONE',  ( -1.000000000000000000, -0.000000000000000000, -0.000000000000000000 ) ) ;
#45398=AXIS2_PLACEMENT_3D ( 'NONE', #10259, #28859, #39892 ) ;
#45407=ORIENTED_EDGE ( 'NONE', *, *, #27267, .F. ) ;
#45409=CARTESIAN_POINT ( 'NONE',  ( 0.000000000000000000, 0.000000000000000000, 0.000000000000000000 ) ) ;
#45413=ORIENTED_EDGE ( 'NONE', *, *, #46106, .T. ) ;
#45417=DIRECTION ( 'NONE',  ( -1.000000000000000000, -0.000000000000000000, -0.000000000000000000 ) ) ;
#45422=CYLINDRICAL_SURFACE ( 'NONE', #4115, 42.00000000000000000 ) ;
#45423=ADVANCED_FACE ( 'NONE', ( #47184 ), #40996, .T. ) ;
#45430=CARTESIAN_POINT ( 'NONE',  ( 10.00000000000000000, 0.000000000000000000, 0.000000000000000000 ) ) ;
#45436=AXIS2_PLACEMENT_3D ( 'NONE', #21697, #17287, #13393 ) ;
#45439=CARTESIAN_POINT ( 'NONE',  ( 10.00000000000000000, -22.74946021919153694, 29.81001611431000597 ) ) ;
#45440=VECTOR ( 'NONE', #41347, 1000.000000000000000 ) ;
#45447=DIRECTION ( 'NONE',  ( -1.000000000000000000, -0.000000000000000000, -0.000000000000000000 ) ) ;
#45452=DIRECTION ( 'NONE',  ( 0.000000000000000000, 0.000000000000000000, 1.000000000000000000 ) ) ;
#45465=DIRECTION ( 'NONE',  ( 0.000000000000000000, 0.000000000000000000, 1.000000000000000000 ) ) ;
#45466=DIRECTION ( 'NONE',  ( 0.000000000000000000, 0.3090169943749580539, -0.9510565162951499785 ) ) ;
#45472=ORIENTED_EDGE ( 'NONE', *, *, #23984, .F. ) ;
#45479=EDGE_CURVE ( 'NONE', #48002, #5896, #27799, .T. ) ;
#45498=LINE ( 'NONE', #16557, #29308 ) ;
#45503=LINE ( 'NONE', #42088, #6594 ) ;
#45504=AXIS2_PLACEMENT_3D ( 'NONE', #12903, #27841, #43229 ) ;
#45507=AXIS2_PLACEMENT_3D ( 'NONE', #27895, #42810, #39128 ) ;
#45509=ORIENTED_EDGE ( 'NONE', *, *, #1495, .F. ) ;
#45516=ORIENTED_EDGE ( 'NONE', *, *, #11751, .T. ) ;
#45520=CARTESIAN_POINT ( 'NONE',  ( 0.000000000000000000, 22.64427369931212297, -30.00120703465181293 ) ) ;
#45522=LINE ( 'NONE', #22365, #27852 ) ;
#45523=EDGE_CURVE ( 'NONE', #35361, #46530, #32471, .T. ) ;
#45526=ORIENTED_EDGE ( 'NONE', *, *, #14746, .F. ) ;
#45532=LINE ( 'NONE', #38701, #40753 ) ;
#45535=DIRECTION ( 'NONE',  ( -1.000000000000000000, -0.000000000000000000, -0.000000000000000000 ) ) ;
#45542=VECTOR ( 'NONE', #45384, 1000.000000000000000 ) ;
#45544=FACE_OUTER_BOUND ( 'NONE', #18627, .T. ) ;
#45562=VECTOR ( 'NONE', #11781, 1000.000000000000000 ) ;
#45564=ORIENTED_EDGE ( 'NONE', *, *, #37346, .T. ) ;
#45576=CARTESIAN_POINT ( 'NONE',  ( -3.000000000000000000, 16.83928648764945279, -16.46020748918028076 ) ) ;
#45588=ORIENTED_EDGE ( 'NONE', *, *, #25908, .F. ) ;
#45596=ORIENTED_EDGE ( 'NONE', *, *, #1069, .F. ) ;
#45603=CARTESIAN_POINT ( 'NONE',  ( 0.000000000000000000, -11.95096189432312350, -23.69967320028773372 ) ) ;
#45619=CIRCLE ( 'NONE', #21400, 15.99999999999999822 ) ;
#45620=LINE ( 'NONE', #30696, #28342 ) ;
#45621=CARTESIAN_POINT ( 'NONE',  ( 0.000000000000000000, 0.000000000000000000, 0.000000000000000000 ) ) ;
#45629=ORIENTED_EDGE ( 'NONE', *, *, #7745, .F. ) ;
#45630=EDGE_CURVE ( 'NONE', #45913, #42163, #15523, .T. ) ;
#45635=AXIS2_PLACEMENT_3D ( 'NONE', #22734, #33505, #14914 ) ;
#45643=VERTEX_POINT ( 'NONE', #13791 ) ;
#45648=CYLINDRICAL_SURFACE ( 'NONE', #731, 37.49900000000000233 ) ;
#45649=VECTOR ( 'NONE', #22525, 1000.000000000000000 ) ;
#45651=DIRECTION ( 'NONE',  ( -1.000000000000000000, -0.000000000000000000, -0.000000000000000000 ) ) ;
#45654=DIRECTION ( 'NONE',  ( -1.000000000000000000, 0.000000000000000000, 0.000000000000000000 ) ) ;
#45665=CARTESIAN_POINT ( 'NONE',  ( 0.000000000000000000, -0.9646360437375309793, 23.52805723605590416 ) ) ;
#45671=DIRECTION ( 'NONE',  ( -1.000000000000000000, 0.000000000000000000, 0.000000000000000000 ) ) ;
#45675=DIRECTION ( 'NONE',  ( 0.000000000000000000, 0.000000000000000000, 1.000000000000000000 ) ) ;
#45681=VECTOR ( 'NONE', #35621, 1000.000000000000000 ) ;
#45684=AXIS2_PLACEMENT_3D ( 'NONE', #10572, #46814, #25483 ) ;
#45693=CIRCLE ( 'NONE', #25378, 37.49900000000000944 ) ;
#45696=AXIS2_PLACEMENT_3D ( 'NONE', #36430, #36894, #29566 ) ;
#45704=ORIENTED_EDGE ( 'NONE', *, *, #9280, .T. ) ;
#45716=AXIS2_PLACEMENT_3D ( 'NONE', #33896, #41497, #34369 ) ;
#45720=CARTESIAN_POINT ( 'NONE',  ( 10.00000000000000000, 35.95386929396241271, 10.96151621346552751 ) ) ;
#45727=ORIENTED_EDGE ( 'NONE', *, *, #46665, .T. ) ;
#45728=DIRECTION ( 'NONE',  ( -1.000000000000000000, 0.000000000000000000, 0.000000000000000000 ) ) ;
#45735=CARTESIAN_POINT ( 'NONE',  ( -3.000000000000000000, -11.95096189432345390, 23.69967320028757385 ) ) ;
#45737=AXIS2_PLACEMENT_3D ( 'NONE', #46164, #5047, #1377 ) ;
#45739=ORIENTED_EDGE ( 'NONE', *, *, #10038, .F. ) ;
#45746=CARTESIAN_POINT ( 'NONE',  ( 10.00000000000000000, -27.75498641678720446, -31.52238457039628727 ) ) ;
#45751=VERTEX_POINT ( 'NONE', #16969 ) ;
#45765=CIRCLE ( 'NONE', #34041, 42.00000000000000000 ) ;
#45769=VECTOR ( 'NONE', #2560, 999.9999999999998863 ) ;
#45790=CARTESIAN_POINT ( 'NONE',  ( 0.000000000000000000, 9.615535125378773529, 24.73947219025917121 ) ) ;
#45793=ORIENTED_EDGE ( 'NONE', *, *, #25417, .F. ) ;
#45799=DIRECTION ( 'NONE',  ( -1.000000000000000000, 0.000000000000000000, -0.000000000000000000 ) ) ;
#45804=ORIENTED_EDGE ( 'NONE', *, *, #25743, .T. ) ;
#45811=DIRECTION ( 'NONE',  ( 0.000000000000000000, -0.9135454576426009776, -0.4067366430758000417 ) ) ;
#45815=DIRECTION ( 'NONE',  ( -1.000000000000000000, 0.000000000000000000, -0.000000000000000000 ) ) ;
#45840=AXIS2_PLACEMENT_3D ( 'NONE', #11448, #30284, #42021 ) ;
#45841=ORIENTED_EDGE ( 'NONE', *, *, #39997, .F. ) ;
#45843=ORIENTED_EDGE ( 'NONE', *, *, #33243, .F. ) ;
#45848=DIRECTION ( 'NONE',  ( -1.000000000000000000, -0.000000000000000000, 0.000000000000000000 ) ) ;
#45851=DIRECTION ( 'NONE',  ( -1.000000000000000000, 0.000000000000000000, 0.000000000000000000 ) ) ;
#45858=CARTESIAN_POINT ( 'NONE',  ( 10.00000000000000000, -37.58145647212455032, 0.6853352020789044152 ) ) ;
#45862=DIRECTION ( 'NONE',  ( -1.000000000000000000, -0.000000000000000000, -0.000000000000000000 ) ) ;
#45867=CARTESIAN_POINT ( 'NONE',  ( 10.00000000000000000, -16.23288003029473359, -33.80338159004301701 ) ) ;
#45877=AXIS2_PLACEMENT_3D ( 'NONE', #35118, #9909, #1847 ) ;
#45878=DIRECTION ( 'NONE',  ( -1.000000000000000000, -0.000000000000000000, -0.000000000000000000 ) ) ;
#45881=EDGE_CURVE ( 'NONE', #44202, #41727, #31765, .T. ) ;
#45885=EDGE_CURVE ( 'NONE', #36640, #25973, #17915, .T. ) ;
#45887=VERTEX_POINT ( 'NONE', #36758 ) ;
#45888=LINE ( 'NONE', #24971, #599 ) ;
#45894=CARTESIAN_POINT ( 'NONE',  ( 10.00000000000000000, -30.00120703465189465, -22.64427369931201639 ) ) ;
#45905=AXIS2_PLACEMENT_3D ( 'NONE', #8769, #37672, #5123 ) ;
#45906=FACE_OUTER_BOUND ( 'NONE', #46998, .T. ) ;
#45913=VERTEX_POINT ( 'NONE', #33576 ) ;
#45917=ORIENTED_EDGE ( 'NONE', *, *, #17674, .T. ) ;
#45918=CYLINDRICAL_SURFACE ( 'NONE', #27009, 16.00000000000000000 ) ;
#45927=FACE_OUTER_BOUND ( 'NONE', #34308, .T. ) ;
#45928=CIRCLE ( 'NONE', #2178, 37.49900000000001654 ) ;
#45931=VERTEX_POINT ( 'NONE', #2754 ) ;
#45945=VERTEX_POINT ( 'NONE', #37495 ) ;
#45958=CIRCLE ( 'NONE', #24846, 16.00000000000000000 ) ;
#45964=CARTESIAN_POINT ( 'NONE',  ( 10.00000000000000000, 32.34446384429971744, 26.79245525562727082 ) ) ;
#45966=VECTOR ( 'NONE', #1487, 999.9999999999998863 ) ;
#45967=CARTESIAN_POINT ( 'NONE',  ( 0.000000000000000000, 26.79245525562714292, 32.34446384429980981 ) ) ;
#45975=LINE ( 'NONE', #20254, #14737 ) ;
#45985=FACE_OUTER_BOUND ( 'NONE', #11545, .T. ) ;
#45987=ORIENTED_EDGE ( 'NONE', *, *, #26310, .F. ) ;
#46000=DIRECTION ( 'NONE',  ( 1.000000000000000000, -0.000000000000000000, 0.000000000000000000 ) ) ;
#46001=CYLINDRICAL_SURFACE ( 'NONE', #9126, 37.49900000000000233 ) ;
#46004=CYLINDRICAL_SURFACE ( 'NONE', #21375, 16.00000000000000000 ) ;
#46012=CARTESIAN_POINT ( 'NONE',  ( 10.00000000000000000, 30.84782396557248418, -21.32104025579081252 ) ) ;
#46019=ORIENTED_EDGE ( 'NONE', *, *, #27267, .T. ) ;
#46024=VERTEX_POINT ( 'NONE', #41414 ) ;
#46029=ADVANCED_FACE ( 'NONE', ( #7869 ), #22805, .F. ) ;
#46030=CARTESIAN_POINT ( 'NONE',  ( 0.000000000000000000, 8.688484142253939169, 21.88630264137371029 ) ) ;
#46032=EDGE_CURVE ( 'NONE', #16667, #9910, #30951, .T. ) ;
#46034=CARTESIAN_POINT ( 'NONE',  ( 0.000000000000000000, 0.000000000000000000, 0.000000000000000000 ) ) ;
#46035=ORIENTED_EDGE ( 'NONE', *, *, #2013, .F. ) ;
#46041=ORIENTED_EDGE ( 'NONE', *, *, #6875, .F. ) ;
#46045=VECTOR ( 'NONE', #44011, 1000.000000000000000 ) ;
#46054=EDGE_CURVE ( 'NONE', #11693, #42163, #34291, .T. ) ;
#46062=DIRECTION ( 'NONE',  ( 1.000000000000000000, -0.000000000000000000, -0.000000000000000000 ) ) ;
#46079=CARTESIAN_POINT ( 'NONE',  ( 0.000000000000000000, 16.61724383029390140, -20.69703378468903665 ) ) ;
#46100=DIRECTION ( 'NONE',  ( 0.000000000000000000, 0.000000000000000000, 1.000000000000000000 ) ) ;
#46103=DIRECTION ( 'NONE',  ( -1.000000000000000000, -0.000000000000000000, -0.000000000000000000 ) ) ;
#46106=EDGE_CURVE ( 'NONE', #22551, #7678, #28602, .T. ) ;
#46112=EDGE_CURVE ( 'NONE', #15338, #25280, #9056, .T. ) ;
#46127=ADVANCED_FACE ( 'NONE', ( #20825 ), #1743, .T. ) ;
#46139=VERTEX_POINT ( 'NONE', #20323 ) ;
#46152=VECTOR ( 'NONE', #29355, 1000.000000000000000 ) ;
#46154=ORIENTED_EDGE ( 'NONE', *, *, #27877, .T. ) ;
#46157=LINE ( 'NONE', #8943, #11611 ) ;
#46164=CARTESIAN_POINT ( 'NONE',  ( 10.00000000000000000, 16.45098606841173705, -33.79645857604496229 ) ) ;
#46170=LINE ( 'NONE', #12641, #21269 ) ;
#46173=DIRECTION ( 'NONE',  ( 0.000000000000000000, 0.9510565162951521989, 0.3090169943749517256 ) ) ;
#46176=CARTESIAN_POINT ( 'NONE',  ( 0.000000000000000000, 0.000000000000000000, 0.000000000000000000 ) ) ;
#46179=VECTOR ( 'NONE', #24073, 1000.000000000000000 ) ;
#46185=ORIENTED_EDGE ( 'NONE', *, *, #16699, .T. ) ;
#46192=ORIENTED_EDGE ( 'NONE', *, *, #30842, .T. ) ;
#46205=VERTEX_POINT ( 'NONE', #29371 ) ;
#46207=CARTESIAN_POINT ( 'NONE',  ( 5.000000000000000000, -22.48208911017474065, -35.47612816024548721 ) ) ;
#46208=CIRCLE ( 'NONE', #19626, 37.49900000000000233 ) ;
#46210=PLANE ( 'NONE',  #28017 ) ;
#46214=CARTESIAN_POINT ( 'NONE',  ( 5.000000000000000000, -31.52238457039579345, -27.75498641678775158 ) ) ;
#46215=DIRECTION ( 'NONE',  ( 0.000000000000000000, 0.000000000000000000, 1.000000000000000000 ) ) ;
#46219=AXIS2_PLACEMENT_3D ( 'NONE', #20317, #35255, #30628 ) ;
#46241=CARTESIAN_POINT ( 'NONE',  ( 0.000000000000000000, -37.22597642581153821, 10.79786254984320415 ) ) ;
#46244=AXIS2_PLACEMENT_3D ( 'NONE', #29036, #3081, #28087 ) ;
#46250=AXIS2_PLACEMENT_3D ( 'NONE', #6308, #17074, #36152 ) ;
#46255=VERTEX_POINT ( 'NONE', #10039 ) ;
#46257=EDGE_CURVE ( 'NONE', #11877, #11522, #12218, .T. ) ;
#46270=VERTEX_POINT ( 'NONE', #40867 ) ;
#46278=VERTEX_POINT ( 'NONE', #7329 ) ;
#46294=DIRECTION ( 'NONE',  ( 0.000000000000000000, -0.9510565162951500895, -0.3090169943749581649 ) ) ;
#46295=CARTESIAN_POINT ( 'NONE',  ( 4.999999999999999112, 40.98264845739749518, 9.188173127307448951 ) ) ;
#46300=CYLINDRICAL_SURFACE ( 'NONE', #33891, 37.49900000000000233 ) ;
#46306=EDGE_CURVE ( 'NONE', #48285, #26114, #11455, .T. ) ;
#46318=FACE_OUTER_BOUND ( 'NONE', #19557, .T. ) ;
#46323=DIRECTION ( 'NONE',  ( -1.000000000000000000, 0.000000000000000000, 0.000000000000000000 ) ) ;
#46325=CARTESIAN_POINT ( 'NONE',  ( 10.00000000000000000, 27.13269053701096922, 25.88420570971410228 ) ) ;
#46332=CYLINDRICAL_SURFACE ( 'NONE', #10621, 16.00000000000000000 ) ;
#46333=ORIENTED_EDGE ( 'NONE', *, *, #29022, .F. ) ;
#46338=DIRECTION ( 'NONE',  ( 0.000000000000000000, -0.4539904997395541320, 0.8910065241883640130 ) ) ;
#46342=DIRECTION ( 'NONE',  ( -1.000000000000000000, -0.000000000000000000, 0.000000000000000000 ) ) ;
#46344=VECTOR ( 'NONE', #28155, 1000.000000000000000 ) ;
#46352=ORIENTED_EDGE ( 'NONE', *, *, #965, .F. ) ;
#46358=CARTESIAN_POINT ( 'NONE',  ( 10.00000000000000000, -37.22597642581153821, 10.79786254984320415 ) ) ;
#46371=DIRECTION ( 'NONE',  ( 0.000000000000000000, 0.7071067811865439090, 0.7071067811865512365 ) ) ;
#46373=AXIS2_PLACEMENT_3D ( 'NONE', #42548, #39108, #5580 ) ;
#46374=CARTESIAN_POINT ( 'NONE',  ( -3.000000000000000000, -26.23277895567245821, -4.042438405570103477 ) ) ;
#46385=ORIENTED_EDGE ( 'NONE', *, *, #26144, .T. ) ;
#46399=DIRECTION ( 'NONE',  ( -1.000000000000000000, -0.000000000000000000, -0.000000000000000000 ) ) ;
#46414=CARTESIAN_POINT ( 'NONE',  ( -3.000000000000000000, -4.261787119644969479, -26.19803753235780519 ) ) ;
#46419=VECTOR ( 'NONE', #12339, 1000.000000000000000 ) ;
#46428=EDGE_LOOP ( 'NONE', ( #15341, #6981, #32549, #27851 ) ) ;
#46437=ORIENTED_EDGE ( 'NONE', *, *, #22816, .T. ) ;
#46440=ORIENTED_EDGE ( 'NONE', *, *, #36084, .T. ) ;
#46441=EDGE_LOOP ( 'NONE', ( #37835, #41335, #43311, #22031 ) ) ;
#46459=CARTESIAN_POINT ( 'NONE',  ( -3.000000000000000000, -10.45096189432344147, 21.10159698893426494 ) ) ;
#46466=CARTESIAN_POINT ( 'NONE',  ( 10.00000000000000000, 0.000000000000000000, 0.000000000000000000 ) ) ;
#46471=ORIENTED_EDGE ( 'NONE', *, *, #47028, .F. ) ;
#46473=CARTESIAN_POINT ( 'NONE',  ( -3.000000000000000000, -3.948201729842038432, -23.21447184625298021 ) ) ;
#46476=DIRECTION ( 'NONE',  ( -1.000000000000000000, 0.000000000000000000, 0.000000000000000000 ) ) ;
#46481=CARTESIAN_POINT ( 'NONE',  ( -3.000000000000000000, -18.13022148937263012, 15.02647892043544608 ) ) ;
#46486=EDGE_LOOP ( 'NONE', ( #8572, #13324, #16074, #27477 ) ) ;
#46487=EDGE_CURVE ( 'NONE', #15615, #40367, #39581, .T. ) ;
#46504=ORIENTED_EDGE ( 'NONE', *, *, #40410, .T. ) ;
#46506=ORIENTED_EDGE ( 'NONE', *, *, #4707, .F. ) ;
#46511=EDGE_LOOP ( 'NONE', ( #39945, #38742, #35797, #20029 ) ) ;
#46514=VERTEX_POINT ( 'NONE', #9747 ) ;
#46525=EDGE_LOOP ( 'NONE', ( #32950, #4887, #41262, #46154 ) ) ;
#46529=DIRECTION ( 'NONE',  ( -1.000000000000000000, 0.000000000000000000, 0.000000000000000000 ) ) ;
#46530=VERTEX_POINT ( 'NONE', #28112 ) ;
#46534=DIRECTION ( 'NONE',  ( -1.000000000000000000, 0.000000000000000000, -0.000000000000000000 ) ) ;
#46535=DIRECTION ( 'NONE',  ( -1.000000000000000000, -0.000000000000000000, -0.000000000000000000 ) ) ;
#46542=AXIS2_PLACEMENT_3D ( 'NONE', #5898, #46529, #17360 ) ;
#46547=LINE ( 'NONE', #35032, #7715 ) ;
#46554=CARTESIAN_POINT ( 'NONE',  ( -3.000000000000000000, 23.59884966291521380, 12.14883922797262805 ) ) ;
#46555=EDGE_CURVE ( 'NONE', #15600, #32221, #9031, .T. ) ;
#46559=CARTESIAN_POINT ( 'NONE',  ( 10.00000000000000000, 0.000000000000000000, 0.000000000000000000 ) ) ;
#46569=ORIENTED_EDGE ( 'NONE', *, *, #2636, .F. ) ;
#46573=ORIENTED_EDGE ( 'NONE', *, *, #27768, .T. ) ;
#46580=DIRECTION ( 'NONE',  ( 0.000000000000000000, 0.7431448254773954654, -0.6691306063588569053 ) ) ;
#46582=EDGE_CURVE ( 'NONE', #41890, #18915, #16374, .T. ) ;
#46583=ORIENTED_EDGE ( 'NONE', *, *, #42213, .F. ) ;
#46585=VERTEX_POINT ( 'NONE', #13187 ) ;
#46591=AXIS2_PLACEMENT_3D ( 'NONE', #2790, #6236, #6008 ) ;
#46597=ADVANCED_FACE ( 'NONE', ( #31561 ), #46001, .T. ) ;
#46600=DIRECTION ( 'NONE',  ( -0.000000000000000000, -0.7431448254773870277, -0.6691306063588662312 ) ) ;
#46601=AXIS2_PLACEMENT_3D ( 'NONE', #9088, #43097, #35752 ) ;
#46604=FILL_AREA_STYLE ('',( #16736 ) ) ;
#46634=EDGE_CURVE ( 'NONE', #7136, #6044, #20054, .T. ) ;
#46636=AXIS2_PLACEMENT_3D ( 'NONE', #42539, #16347, #4603 ) ;
#46637=EDGE_CURVE ( 'NONE', #26953, #11582, #536, .T. ) ;
#46665=EDGE_CURVE ( 'NONE', #24209, #1357, #36647, .T. ) ;
#46670=FACE_OUTER_BOUND ( 'NONE', #23382, .T. ) ;
#46673=DIRECTION ( 'NONE',  ( 0.000000000000000000, -0.8090169943749422332, -0.5877852522924803536 ) ) ;
#46680=EDGE_CURVE ( 'NONE', #1027, #18777, #10473, .T. ) ;
#46683=ORIENTED_EDGE ( 'NONE', *, *, #17736, .T. ) ;
#46690=ORIENTED_EDGE ( 'NONE', *, *, #16699, .F. ) ;
#46692=ORIENTED_EDGE ( 'NONE', *, *, #42342, .T. ) ;
#46699=VERTEX_POINT ( 'NONE', #28604 ) ;
#46708=EDGE_CURVE ( 'NONE', #29332, #44202, #25630, .T. ) ;
#46713=CARTESIAN_POINT ( 'NONE',  ( 10.00000000000000000, 3.925862922256769583, -41.81611651403858332 ) ) ;
#46717=EDGE_CURVE ( 'NONE', #6187, #15600, #2392, .T. ) ;
#46721=CIRCLE ( 'NONE', #20919, 16.00000000000000000 ) ;
#46723=FACE_OUTER_BOUND ( 'NONE', #6988, .T. ) ;
#46725=DIRECTION ( 'NONE',  ( -1.000000000000000000, 0.000000000000000000, 0.000000000000000000 ) ) ;
#46728=AXIS2_PLACEMENT_3D ( 'NONE', #10600, #32620, #47542 ) ;
#46729=CARTESIAN_POINT ( 'NONE',  ( -3.000000000000000000, 16.83928648764945279, -16.46020748918028076 ) ) ;
#46732=EDGE_CURVE ( 'NONE', #3614, #25227, #32733, .T. ) ;
#46733=DIRECTION ( 'NONE',  ( -1.000000000000000000, 0.000000000000000000, -0.000000000000000000 ) ) ;
#46748=ORIENTED_EDGE ( 'NONE', *, *, #23669, .F. ) ;
#46754=ORIENTED_EDGE ( 'NONE', *, *, #22465, .F. ) ;
#46767=CIRCLE ( 'NONE', #13911, 16.00000000000000000 ) ;
#46784=AXIS2_PLACEMENT_3D ( 'NONE', #9717, #40327, #39837 ) ;
#46786=CARTESIAN_POINT ( 'NONE',  ( 0.000000000000000000, 39.04073710021344112, 15.48615015657596672 ) ) ;
#46788=DIRECTION ( 'NONE',  ( 0.000000000000000000, 0.000000000000000000, 1.000000000000000000 ) ) ;
#46790=LINE ( 'NONE', #16920, #44381 ) ;
#46793=DIRECTION ( 'NONE',  ( -1.000000000000000000, 0.000000000000000000, -0.000000000000000000 ) ) ;
#46796=DIRECTION ( 'NONE',  ( -1.000000000000000000, -0.000000000000000000, 0.000000000000000000 ) ) ;
#46797=VERTEX_POINT ( 'NONE', #7991 ) ;
#46800=ORIENTED_EDGE ( 'NONE', *, *, #45342, .T. ) ;
#46801=CARTESIAN_POINT ( 'NONE',  ( -3.000000000000000000, -19.89357724625003598, 12.59942793731059574 ) ) ;
#46802=ORIENTED_EDGE ( 'NONE', *, *, #22093, .T. ) ;
#46805=ORIENTED_EDGE ( 'NONE', *, *, #8119, .F. ) ;
#46814=DIRECTION ( 'NONE',  ( 0.000000000000000000, -0.8660254037844437036, 0.4999999999999913403 ) ) ;
#46816=EDGE_CURVE ( 'NONE', #22498, #28068, #38113, .T. ) ;
#46821=ORIENTED_EDGE ( 'NONE', *, *, #30753, .F. ) ;
#46827=DIRECTION ( 'NONE',  ( -1.000000000000000000, 0.000000000000000000, -0.000000000000000000 ) ) ;
#46828=CARTESIAN_POINT ( 'NONE',  ( 10.00000000000000000, 37.22597642581150268, 5.202137450157037435 ) ) ;
#46835=DIRECTION ( 'NONE',  ( 0.000000000000000000, 0.000000000000000000, -1.000000000000000000 ) ) ;
#46844=VECTOR ( 'NONE', #34202, 1000.000000000000000 ) ;
#46845=ORIENTED_EDGE ( 'NONE', *, *, #43976, .F. ) ;
#46846=DIRECTION ( 'NONE',  ( -1.000000000000000000, 0.000000000000000000, 0.000000000000000000 ) ) ;
#46852=EDGE_CURVE ( 'NONE', #19636, #14109, #22410, .T. ) ;
#46865=ORIENTED_EDGE ( 'NONE', *, *, #953, .F. ) ;
#46869=EDGE_CURVE ( 'NONE', #14988, #15615, #7554, .T. ) ;
#46879=ORIENTED_EDGE ( 'NONE', *, *, #25502, .T. ) ;
#46880=CARTESIAN_POINT ( 'NONE',  ( 0.000000000000000000, 0.000000000000000000, 0.000000000000000000 ) ) ;
#46881=CIRCLE ( 'NONE', #19490, 16.00000000000000000 ) ;
#46882=DIRECTION ( 'NONE',  ( 0.000000000000000000, 0.000000000000000000, -1.000000000000000000 ) ) ;
#46889=DIRECTION ( 'NONE',  ( -1.000000000000000000, 0.000000000000000000, 0.000000000000000000 ) ) ;
#46902=EDGE_LOOP ( 'NONE', ( #16323, #31184, #33782, #44032 ) ) ;
#46904=ORIENTED_EDGE ( 'NONE', *, *, #47611, .F. ) ;
#46905=VECTOR ( 'NONE', #41592, 1000.000000000000000 ) ;
#46908=ORIENTED_EDGE ( 'NONE', *, *, #16239, .F. ) ;
#46909=AXIS2_PLACEMENT_3D ( 'NONE', #40418, #3925, #30850 ) ;
#46912=ORIENTED_EDGE ( 'NONE', *, *, #17877, .T. ) ;
#46925=FACE_OUTER_BOUND ( 'NONE', #18280, .T. ) ;
#46927=ORIENTED_EDGE ( 'NONE', *, *, #17736, .F. ) ;
#46929=ORIENTED_EDGE ( 'NONE', *, *, #26034, .F. ) ;
#46933=CARTESIAN_POINT ( 'NONE',  ( 0.000000000000000000, -6.736453364083817341, 36.88895765772630142 ) ) ;
#46934=CYLINDRICAL_SURFACE ( 'NONE', #651, 16.00000000000000000 ) ;
#46940=EDGE_CURVE ( 'NONE', #26532, #32853, #35640, .T. ) ;
#46945=DIRECTION ( 'NONE',  ( 1.000000000000000000, -0.000000000000000000, -0.000000000000000000 ) ) ;
#46950=DIRECTION ( 'NONE',  ( 0.000000000000000000, 0.3090169943749442316, 0.9510565162951545304 ) ) ;
#46952=DIRECTION ( 'NONE',  ( 1.000000000000000000, 0.000000000000000000, 0.000000000000000000 ) ) ;
#46953=DIRECTION ( 'NONE',  ( 0.000000000000000000, 0.000000000000000000, 1.000000000000000000 ) ) ;
#46961=DIRECTION ( 'NONE',  ( 0.000000000000000000, 0.000000000000000000, 1.000000000000000000 ) ) ;
#46968=CARTESIAN_POINT ( 'NONE',  ( 0.000000000000000000, -41.81611651403864727, 3.925862922256025289 ) ) ;
#46974=DIRECTION ( 'NONE',  ( 0.000000000000000000, -0.9781476007338070211, 0.2079116908177525425 ) ) ;
#46977=ORIENTED_EDGE ( 'NONE', *, *, #31921, .T. ) ;
#46978=EDGE_LOOP ( 'NONE', ( #26218, #31043, #5113, #46802 ) ) ;
#46981=ADVANCED_FACE ( 'NONE', ( #5307 ), #8968, .T. ) ;
#46984=EDGE_LOOP ( 'NONE', ( #18302, #1640, #27042, #25596 ) ) ;
#46985=DIRECTION ( 'NONE',  ( -1.000000000000000000, -0.000000000000000000, 0.000000000000000000 ) ) ;
#46992=DIRECTION ( 'NONE',  ( 0.000000000000000000, 0.000000000000000000, 1.000000000000000000 ) ) ;
#46994=FACE_OUTER_BOUND ( 'NONE', #10415, .T. ) ;
#46998=EDGE_LOOP ( 'NONE', ( #30599, #5268, #3869, #34970 ) ) ;
#47012=AXIS2_PLACEMENT_3D ( 'NONE', #38135, #4601, #909 ) ;
#47019=ORIENTED_EDGE ( 'NONE', *, *, #30077, .F. ) ;
#47028=EDGE_CURVE ( 'NONE', #28487, #2768, #563, .T. ) ;
#47030=ADVANCED_FACE ( 'NONE', ( #12647 ), #47129, .F. ) ;
#47038=CARTESIAN_POINT ( 'NONE',  ( 0.000000000000000000, -23.29833615347104825, -3.418703333116803744 ) ) ;
#47039=AXIS2_PLACEMENT_3D ( 'NONE', #42414, #4963, #5450 ) ;
#47043=AXIS2_PLACEMENT_3D ( 'NONE', #10570, #29151, #39946 ) ;
#47046=MECHANICAL_DESIGN_GEOMETRIC_PRESENTATION_REPRESENTATION('',(#26719),#11092);
#47047=DIRECTION ( 'NONE',  ( 0.000000000000000000, -0.8910065241883721177, 0.4539904997395382003 ) ) ;
#47065=DIRECTION ( 'NONE',  ( 0.000000000000000000, -0.9510565162951503115, -0.3090169943749573878 ) ) ;
#47066=FACE_OUTER_BOUND ( 'NONE', #24455, .T. ) ;
#47080=DIRECTION ( 'NONE',  ( 0.000000000000000000, -0.4539904997395351471, -0.8910065241883737830 ) ) ;
#47082=EDGE_CURVE ( 'NONE', #34673, #22551, #27947, .T. ) ;
#47086=ORIENTED_EDGE ( 'NONE', *, *, #7667, .F. ) ;
#47096=CARTESIAN_POINT ( 'NONE',  ( 10.00000000000000000, 39.04073710021366139, -15.48615015657542848 ) ) ;
#47097=ORIENTED_EDGE ( 'NONE', *, *, #19012, .T. ) ;
#47099=VERTEX_POINT ( 'NONE', #17505 ) ;
#47100=CARTESIAN_POINT ( 'NONE',  ( 50.00005079999999680, 0.000000000000000000, 0.000000000000000000 ) ) ;
#47129=PLANE ( 'NONE',  #34938 ) ;
#47143=AXIS2_PLACEMENT_3D ( 'NONE', #34698, #1180, #18853 ) ;
#47152=AXIS2_PLACEMENT_3D ( 'NONE', #38739, #46796, #5200 ) ;
#47153=CARTESIAN_POINT ( 'NONE',  ( 0.000000000000000000, -22.74946021919110706, -29.81001611431033282 ) ) ;
#47154=ORIENTED_EDGE ( 'NONE', *, *, #24364, .T. ) ;
#47156=ORIENTED_EDGE ( 'NONE', *, *, #2013, .T. ) ;
#47168=FACE_OUTER_BOUND ( 'NONE', #38881, .T. ) ;
#47172=CARTESIAN_POINT ( 'NONE',  ( -10.00000000000000000, 0.000000000000000000, 0.000000000000000000 ) ) ;
#47184=FACE_OUTER_BOUND ( 'NONE', #32373, .T. ) ;
#47186=CYLINDRICAL_SURFACE ( 'NONE', #41790, 16.00000000000000000 ) ;
#47189=CARTESIAN_POINT ( 'NONE',  ( 10.00000000000000000, 35.92658777277525672, -10.74501242461245809 ) ) ;
#47194=CARTESIAN_POINT ( 'NONE',  ( 4.999999999999999112, -9.188173127307004862, -40.98264845739759465 ) ) ;
#47196=ORIENTED_EDGE ( 'NONE', *, *, #7800, .F. ) ;
#47202=EDGE_CURVE ( 'NONE', #37915, #5067, #7591, .T. ) ;
#47207=CYLINDRICAL_SURFACE ( 'NONE', #45696, 16.00000000000000000 ) ;
#47214=CIRCLE ( 'NONE', #26116, 42.00000000000000000 ) ;
#47224=CARTESIAN_POINT ( 'NONE',  ( 0.000000000000000000, -41.81611651403859042, -3.925862922256606602 ) ) ;
#47229=CARTESIAN_POINT ( 'NONE',  ( 0.000000000000000000, -10.45096189432344147, 21.10159698893426494 ) ) ;
#47244=CARTESIAN_POINT ( 'NONE',  ( 0.000000000000000000, 6.555932627142418312, 37.01155633439060466 ) ) ;
#47245=CARTESIAN_POINT ( 'NONE',  ( 0.000000000000000000, -3.925862922255855647, -41.81611651403866858 ) ) ;
#47252=AXIS2_PLACEMENT_3D ( 'NONE', #10268, #47478, #39677 ) ;
#47255=AXIS2_PLACEMENT_3D ( 'NONE', #20685, #39050, #13839 ) ;
#47262=ORIENTED_EDGE ( 'NONE', *, *, #35874, .T. ) ;
#47269=AXIS2_PLACEMENT_3D ( 'NONE', #25384, #33932, #22455 ) ;
#47270=CARTESIAN_POINT ( 'NONE',  ( 0.000000000000000000, 26.50000000000000000, -1.500000000000001332 ) ) ;
#47281=CIRCLE ( 'NONE', #6644, 15.99999999999999645 ) ;
#47285=VECTOR ( 'NONE', #4975, 1000.000000000000000 ) ;
#47289=ORIENTED_EDGE ( 'NONE', *, *, #24103, .T. ) ;
#47290=FACE_OUTER_BOUND ( 'NONE', #4439, .T. ) ;
#47291=CARTESIAN_POINT ( 'NONE',  ( 0.000000000000000000, 37.58145647212453611, 0.6853352020791767529 ) ) ;
#47295=AXIS2_PLACEMENT_3D ( 'NONE', #10627, #22362, #2783 ) ;
#47296=CIRCLE ( 'NONE', #22281, 37.49900000000000233 ) ;
#47298=CARTESIAN_POINT ( 'NONE',  ( 10.00000000000000000, 0.000000000000000000, 0.000000000000000000 ) ) ;
#47312=AXIS2_PLACEMENT_3D ( 'NONE', #11175, #34630, #42478 ) ;
#47314=EDGE_CURVE ( 'NONE', #38352, #23243, #45928, .T. ) ;
#47319=DIRECTION ( 'NONE',  ( 1.000000000000000000, 0.000000000000000000, -0.000000000000000000 ) ) ;
#47321=LINE ( 'NONE', #36531, #19308 ) ;
#47329=EDGE_CURVE ( 'NONE', #8466, #43027, #11623, .T. ) ;
#47333=EDGE_LOOP ( 'NONE', ( #5686, #34558, #16894, #34195 ) ) ;
#47336=VECTOR ( 'NONE', #7473, 1000.000000000000000 ) ;
#47338=CIRCLE ( 'NONE', #5135, 42.00000000000000000 ) ;
#47344=CIRCLE ( 'NONE', #27010, 42.00000000000000000 ) ;
#47346=AXIS2_PLACEMENT_3D ( 'NONE', #21834, #9867, #6437 ) ;
#47348=ORIENTED_EDGE ( 'NONE', *, *, #28393, .F. ) ;
#47349=DIRECTION ( 'NONE',  ( -1.000000000000000000, 0.000000000000000000, -0.000000000000000000 ) ) ;
#47351=VERTEX_POINT ( 'NONE', #39195 ) ;
#47357=FACE_OUTER_BOUND ( 'NONE', #36326, .T. ) ;
#47376=CARTESIAN_POINT ( 'NONE',  ( 10.00000000000000000, 16.23288003029543347, -33.80338159004267595 ) ) ;
#47391=DIRECTION ( 'NONE',  ( -1.000000000000000000, 0.000000000000000000, 0.000000000000000000 ) ) ;
#47393=ORIENTED_EDGE ( 'NONE', *, *, #15985, .F. ) ;
#47400=CARTESIAN_POINT ( 'NONE',  ( -3.000000000000000000, 23.50000000000000000, 1.499999999999997780 ) ) ;
#47411=CARTESIAN_POINT ( 'NONE',  ( -3.000000000000000000, -22.32062822937489344, 14.36278369418800160 ) ) ;
#47417=CYLINDRICAL_SURFACE ( 'NONE', #24438, 42.00000000000000000 ) ;
#47429=EDGE_CURVE ( 'NONE', #14290, #31219, #45888, .T. ) ;
#47440=EDGE_LOOP ( 'NONE', ( #11635, #3580, #20260, #8594 ) ) ;
#47443=DIRECTION ( 'NONE',  ( 0.000000000000000000, 0.2079116908177664480, -0.9781476007338041345 ) ) ;
#47448=EDGE_CURVE ( 'NONE', #42424, #38396, #35989, .T. ) ;
#47454=EDGE_CURVE ( 'NONE', #24216, #3270, #9197, .T. ) ;
#47459=ORIENTED_EDGE ( 'NONE', *, *, #19923, .T. ) ;
#47465=EDGE_CURVE ( 'NONE', #13778, #11582, #46790, .T. ) ;
#47468=ORIENTED_EDGE ( 'NONE', *, *, #6753, .F. ) ;
#47474=CARTESIAN_POINT ( 'NONE',  ( 0.000000000000000000, 37.16516213103285082, -4.992566952384588141 ) ) ;
#47475=DIRECTION ( 'NONE',  ( 0.000000000000000000, 0.5000000000000039968, -0.8660254037844363761 ) ) ;
#47477=ORIENTED_EDGE ( 'NONE', *, *, #23695, .T. ) ;
#47478=DIRECTION ( 'NONE',  ( -1.000000000000000000, 0.000000000000000000, -0.000000000000000000 ) ) ;
#47502=DIRECTION ( 'NONE',  ( 0.000000000000000000, 0.3090169943749442316, 0.9510565162951545304 ) ) ;
#47503=FACE_OUTER_BOUND ( 'NONE', #48409, .T. ) ;
#47505=EDGE_LOOP ( 'NONE', ( #12259, #13657, #29865, #2696 ) ) ;
#47513=VERTEX_POINT ( 'NONE', #40873 ) ;
#47515=ORIENTED_EDGE ( 'NONE', *, *, #22385, .F. ) ;
#47518=CARTESIAN_POINT ( 'NONE',  ( 0.000000000000000000, 33.00180498840072829, -17.80606268964504935 ) ) ;
#47531=VECTOR ( 'NONE', #6385, 1000.000000000000000 ) ;
#47534=DIRECTION ( 'NONE',  ( -1.000000000000000000, 0.000000000000000000, 0.000000000000000000 ) ) ;
#47536=CARTESIAN_POINT ( 'NONE',  ( 0.000000000000000000, -19.89357724624987256, -12.59942793731086041 ) ) ;
#47542=DIRECTION ( 'NONE',  ( 0.000000000000000000, 0.8090169943749486725, -0.5877852522924714718 ) ) ;
#47549=VERTEX_POINT ( 'NONE', #40159 ) ;
#47553=CARTESIAN_POINT ( 'NONE',  ( 5.000000000000000000, -27.75498641678764855, 31.52238457039590358 ) ) ;
#47554=ORIENTED_EDGE ( 'NONE', *, *, #21547, .T. ) ;
#47573=CARTESIAN_POINT ( 'NONE',  ( 10.00000000000000000, 35.95386929396241271, 10.96151621346552751 ) ) ;
#47581=FACE_BOUND ( 'NONE', #17185, .T. ) ;
#47592=DIRECTION ( 'NONE',  ( 1.000000000000000000, 0.000000000000000000, -0.000000000000000000 ) ) ;
#47599=AXIS2_PLACEMENT_3D ( 'NONE', #44634, #4007, #34095 ) ;
#47611=EDGE_CURVE ( 'NONE', #31567, #11474, #3166, .T. ) ;
#47616=EDGE_CURVE ( 'NONE', #39296, #40664, #45037, .T. ) ;
#47621=DIRECTION ( 'NONE',  ( 0.000000000000000000, 1.000000000000000000, 7.228014483236689653E-16 ) ) ;
#47632=DIRECTION ( 'NONE',  ( -1.000000000000000000, 0.000000000000000000, 0.000000000000000000 ) ) ;
#47639=CARTESIAN_POINT ( 'NONE',  ( 0.000000000000000000, 0.000000000000000000, 0.000000000000000000 ) ) ;
#47642=CARTESIAN_POINT ( 'NONE',  ( 0.000000000000000000, -22.64427369931148348, -30.00120703465229965 ) ) ;
#47643=CARTESIAN_POINT ( 'NONE',  ( -3.000000000000000000, 0.000000000000000000, 0.000000000000000000 ) ) ;
#47644=CARTESIAN_POINT ( 'NONE',  ( -3.000000000000000000, -13.04903810567647682, -19.60159698893442481 ) ) ;
#47653=VECTOR ( 'NONE', #16909, 1000.000000000000000 ) ;
#47659=AXIS2_PLACEMENT_3D ( 'NONE', #23130, #19211, #40766 ) ;
#47661=SURFACE_STYLE_USAGE ( .BOTH. , #7035 ) ;
#47662=AXIS2_PLACEMENT_3D ( 'NONE', #47643, #18023, #2866 ) ;
#47695=ORIENTED_EDGE ( 'NONE', *, *, #40629, .F. ) ;
#47702=CYLINDRICAL_SURFACE ( 'NONE', #27710, 42.00000000000000000 ) ;
#47724=ORIENTED_EDGE ( 'NONE', *, *, #43947, .T. ) ;
#47737=DIRECTION ( 'NONE',  ( 1.000000000000000000, 0.000000000000000000, 0.000000000000000000 ) ) ;
#47740=ORIENTED_EDGE ( 'NONE', *, *, #24717, .F. ) ;
#47748=DIRECTION ( 'NONE',  ( 0.000000000000000000, 0.000000000000000000, 1.000000000000000000 ) ) ;
#47757=CIRCLE ( 'NONE', #47012, 42.00000000000000000 ) ;
#47763=CIRCLE ( 'NONE', #37618, 37.49900000000000233 ) ;
#47766=AXIS2_PLACEMENT_3D ( 'NONE', #38950, #35504, #8352 ) ;
#47771=LINE ( 'NONE', #17435, #6053 ) ;
#47790=ADVANCED_FACE ( 'NONE', ( #33673 ), #29766, .T. ) ;
#47805=DIRECTION ( 'NONE',  ( 0.000000000000000000, 0.000000000000000000, -1.000000000000000000 ) ) ;
#47818=DIRECTION ( 'NONE',  ( 0.000000000000000000, 0.000000000000000000, -1.000000000000000000 ) ) ;
#47820=ORIENTED_EDGE ( 'NONE', *, *, #43142, .F. ) ;
#47828=VERTEX_POINT ( 'NONE', #141 ) ;
#47831=ADVANCED_FACE ( 'NONE', ( #14619 ), #44698, .T. ) ;
#47836=DIRECTION ( 'NONE',  ( -1.000000000000000000, -0.000000000000000000, 0.000000000000000000 ) ) ;
#47842=AXIS2_PLACEMENT_3D ( 'NONE', #37411, #8024, #3880 ) ;
#47862=DIRECTION ( 'NONE',  ( -1.000000000000000000, -0.000000000000000000, -0.000000000000000000 ) ) ;
#47865=VERTEX_POINT ( 'NONE', #30018 ) ;
#47872=VECTOR ( 'NONE', #30501, 1000.000000000000000 ) ;
#47877=CARTESIAN_POINT ( 'NONE',  ( 5.000000000000000000, -39.04073710021332744, -15.48615015657624205 ) ) ;
#47883=FACE_OUTER_BOUND ( 'NONE', #18340, .T. ) ;
#47888=ADVANCED_FACE ( 'NONE', ( #48369 ), #7509, .T. ) ;
#47889=LINE ( 'NONE', #44239, #24893 ) ;
#47914=FACE_OUTER_BOUND ( 'NONE', #6284, .T. ) ;
#47918=ORIENTED_EDGE ( 'NONE', *, *, #5262, .F. ) ;
#47919=AXIS2_PLACEMENT_3D ( 'NONE', #27959, #23537, #38475 ) ;
#47923=CARTESIAN_POINT ( 'NONE',  ( 10.00000000000000000, -21.40280677340345505, -36.13751322684441902 ) ) ;
#47924=EDGE_LOOP ( 'NONE', ( #45087, #9924, #13526, #28333 ) ) ;
#47925=FACE_OUTER_BOUND ( 'NONE', #23429, .T. ) ;
#47932=CARTESIAN_POINT ( 'NONE',  ( 10.00000000000000000, 17.67226234102826510, 33.17418723428314564 ) ) ;
#47934=ORIENTED_EDGE ( 'NONE', *, *, #6454, .T. ) ;
#47935=ORIENTED_EDGE ( 'NONE', *, *, #38407, .F. ) ;
#47940=EDGE_LOOP ( 'NONE', ( #38084, #45298, #27068, #8807 ) ) ;
#47943=EDGE_CURVE ( 'NONE', #11046, #38237, #45958, .T. ) ;
#47946=ORIENTED_EDGE ( 'NONE', *, *, #35791, .T. ) ;
#47953=LINE ( 'NONE', #21768, #15846 ) ;
#47960=EDGE_CURVE ( 'NONE', #46530, #43176, #46767, .T. ) ;
#47964=DIRECTION ( 'NONE',  ( 0.000000000000000000, -0.9945218953682730678, -0.1045284632676570929 ) ) ;
#47971=CIRCLE ( 'NONE', #26887, 42.00000000000000000 ) ;
#47981=VECTOR ( 'NONE', #43462, 1000.000000000000000 ) ;
#47986=VECTOR ( 'NONE', #11356, 1000.000000000000000 ) ;
#48002=VERTEX_POINT ( 'NONE', #15344 ) ;
#48007=VECTOR ( 'NONE', #40945, 1000.000000000000000 ) ;
#48014=EDGE_CURVE ( 'NONE', #28097, #9186, #18981, .T. ) ;
#48019=CARTESIAN_POINT ( 'NONE',  ( 5.000000000000000000, -22.48208911017525580, 35.47612816024516036 ) ) ;
#48022=VECTOR ( 'NONE', #28880, 1000.000000000000000 ) ;
#48026=LINE ( 'NONE', #36048, #41137 ) ;
#48043=EDGE_CURVE ( 'NONE', #44937, #24691, #16297, .T. ) ;
#48049=EDGE_CURVE ( 'NONE', #39824, #43844, #46157, .T. ) ;
#48053=CYLINDRICAL_SURFACE ( 'NONE', #43296, 16.00000000000000000 ) ;
#48056=CARTESIAN_POINT ( 'NONE',  ( 0.000000000000000000, 0.000000000000000000, 37.49900000000000233 ) ) ;
#48058=ADVANCED_FACE ( 'NONE', ( #25749 ), #10606, .T. ) ;
#48064=AXIS2_PLACEMENT_3D ( 'NONE', #9195, #42241, #20439 ) ;
#48066=DIRECTION ( 'NONE',  ( 0.000000000000000000, 0.5877852522924683631, 0.8090169943749510040 ) ) ;
#48071=CARTESIAN_POINT ( 'NONE',  ( 0.000000000000000000, 22.74946021919133088, 29.81001611431016229 ) ) ;
#48072=ORIENTED_EDGE ( 'NONE', *, *, #20660, .F. ) ;
#48080=FACE_OUTER_BOUND ( 'NONE', #38878, .T. ) ;
#48091=CARTESIAN_POINT ( 'NONE',  ( 0.000000000000000000, 23.50000000000000000, -1.500000000000001332 ) ) ;
#48097=DIRECTION ( 'NONE',  ( 0.000000000000000000, 1.000000000000000000, 3.469446951953614189E-15 ) ) ;
#48102=DIRECTION ( 'NONE',  ( -1.000000000000000000, -0.000000000000000000, -0.000000000000000000 ) ) ;
#48117=ORIENTED_EDGE ( 'NONE', *, *, #36676, .T. ) ;
#48120=EDGE_LOOP ( 'NONE', ( #28856, #44404, #29777, #25300 ) ) ;
#48125=CYLINDRICAL_SURFACE ( 'NONE', #1698, 37.49900000000000233 ) ;
#48129=CARTESIAN_POINT ( 'NONE',  ( 10.00000000000000000, 0.000000000000000000, 0.000000000000000000 ) ) ;
#48133=LINE ( 'NONE', #14620, #26039 ) ;
#48141=CARTESIAN_POINT ( 'NONE',  ( 10.00000000000000000, -22.64427369931191336, 30.00120703465197280 ) ) ;
#48143=ORIENTED_EDGE ( 'NONE', *, *, #29339, .T. ) ;
#48159=DIRECTION ( 'NONE',  ( 0.000000000000000000, 1.000000000000000000, 3.469446951953614189E-15 ) ) ;
#48160=CIRCLE ( 'NONE', #5979, 37.49900000000000944 ) ;
#48171=CIRCLE ( 'NONE', #31013, 16.00000000000000000 ) ;
#48172=CARTESIAN_POINT ( 'NONE',  ( 10.00000000000000000, -37.22597642581153821, 10.79786254984320415 ) ) ;
#48173=EDGE_CURVE ( 'NONE', #24574, #19822, #29442, .T. ) ;
#48176=ORIENTED_EDGE ( 'NONE', *, *, #26791, .F. ) ;
#48185=ORIENTED_EDGE ( 'NONE', *, *, #6966, .T. ) ;
#48204=CARTESIAN_POINT ( 'NONE',  ( 0.000000000000000000, 27.75498641678742473, 31.52238457039609187 ) ) ;
#48208=EDGE_CURVE ( 'NONE', #25973, #9186, #41657, .T. ) ;
#48224=ADVANCED_FACE ( 'NONE', ( #16208 ), #11802, .T. ) ;
#48226=CIRCLE ( 'NONE', #31066, 16.00000000000000355 ) ;
#48231=CARTESIAN_POINT ( 'NONE',  ( 10.00000000000000000, -37.16516213103273714, -4.992566952385376844 ) ) ;
#48235=DIRECTION ( 'NONE',  ( -1.000000000000000000, -0.000000000000000000, -0.000000000000000000 ) ) ;
#48237=FACE_OUTER_BOUND ( 'NONE', #1051, .T. ) ;
#48243=DIRECTION ( 'NONE',  ( 0.000000000000000000, 0.000000000000000000, 1.000000000000000000 ) ) ;
#48255=CARTESIAN_POINT ( 'NONE',  ( 10.00000000000000000, 0.000000000000000000, 0.000000000000000000 ) ) ;
#48267=VECTOR ( 'NONE', #2973, 1000.000000000000000 ) ;
#48271=CARTESIAN_POINT ( 'NONE',  ( 0.000000000000000000, 0.000000000000000000, 0.000000000000000000 ) ) ;
#48285=VERTEX_POINT ( 'NONE', #27221 ) ;
#48287=EDGE_CURVE ( 'NONE', #10988, #44380, #4933, .T. ) ;
#48293=ADVANCED_FACE ( 'NONE', ( #37743 ), #26732, .F. ) ;
#48299=DIRECTION ( 'NONE',  ( -1.000000000000000000, 0.000000000000000000, 0.000000000000000000 ) ) ;
#48314=DIRECTION ( 'NONE',  ( -1.000000000000000000, 0.000000000000000000, 0.000000000000000000 ) ) ;
#48317=CYLINDRICAL_SURFACE ( 'NONE', #18232, 37.49900000000000233 ) ;
#48318=DIRECTION ( 'NONE',  ( 1.000000000000000000, 0.000000000000000000, 0.000000000000000000 ) ) ;
#48321=FACE_OUTER_BOUND ( 'NONE', #16181, .T. ) ;
#48324=ORIENTED_EDGE ( 'NONE', *, *, #32682, .F. ) ;
#48330=EDGE_CURVE ( 'NONE', #28663, #20905, #15247, .T. ) ;
#48334=LINE ( 'NONE', #40752, #47336 ) ;
#48337=CIRCLE ( 'NONE', #44460, 37.49900000000000233 ) ;
#48340=CARTESIAN_POINT ( 'NONE',  ( 0.000000000000000000, -26.79245525562738095, 32.34446384429961796 ) ) ;
#48343=LINE ( 'NONE', #14826, #14835 ) ;
#48356=ORIENTED_EDGE ( 'NONE', *, *, #1011, .F. ) ;
#48357=ORIENTED_EDGE ( 'NONE', *, *, #14266, .T. ) ;
#48369=FACE_OUTER_BOUND ( 'NONE', #29105, .T. ) ;
#48382=DIRECTION ( 'NONE',  ( 0.000000000000000000, 0.5877852522924797984, -0.8090169943749426773 ) ) ;
#48389=EDGE_CURVE ( 'NONE', #30863, #38628, #46547, .T. ) ;
#48401=ORIENTED_EDGE ( 'NONE', *, *, #41725, .T. ) ;
#48406=ADVANCED_FACE ( 'NONE', ( #1511 ), #24970, .T. ) ;
#48409=EDGE_LOOP ( 'NONE', ( #27658, #6848, #24162, #468 ) ) ;
#48412=PLANE ( 'NONE',  #41490 ) ;
#48416=VERTEX_POINT ( 'NONE', #43105 ) ;
#48424=DIRECTION ( 'NONE',  ( 0.000000000000000000, 1.000000000000000000, 3.491481338843133750E-15 ) ) ;
#48425=ORIENTED_EDGE ( 'NONE', *, *, #21114, .T. ) ;
#48427=ORIENTED_EDGE ( 'NONE', *, *, #45259, .F. ) ;
#48435=ORIENTED_EDGE ( 'NONE', *, *, #4137, .T. ) ;
#48436=CARTESIAN_POINT ( 'NONE',  ( -3.000000000000000000, 16.83928648764923253, 16.46020748918050458 ) ) ;
#48445=CARTESIAN_POINT ( 'NONE',  ( 10.00000000000000000, 36.88895765772642932, -6.736453364083163642 ) ) ;
ENDSEC;
END-ISO-10303-21;
